ISO-10303-21;
HEADER;
/* Generated by software containing ST-Developer
 * from STEP Tools, Inc. (www.steptools.com) 
 */

FILE_DESCRIPTION(
/* description */ ('Independent four-jaw lathe chuck,200mm body,40mm bore,36\X2\2013\X0\7
6mm nominal opposed jaw opening. Four shared machined T-jaws and model
ed partial M12x1.75 feed screws, native independent screw/slider links
, removable bolted bronze-bearing cartridges, fully captured ring/wash
er/head thrust stacks and registered bolted backplate. Custom spindle 
interface; no compatibility, speed, grip force or safety rating assign
ed.'),
/* implementation_level */ '2;1');

FILE_NAME(
/* name */ 'Jaw adjustment screw.step',
/* time_stamp */ '2026-11-09T20:24:54-08:00',
/* author */ (''),
/* organization */ (''),
/* preprocessor_version */ 'ST-DEVELOPER v20.2',
/* originating_system */ 'Autodesk Translation Framework v15.17.0.0',
/* authorisation */ '');

FILE_SCHEMA (('AUTOMOTIVE_DESIGN { 1 0 10303 214 3 1 1 }'));
ENDSEC;

DATA;
#10=MECHANICAL_DESIGN_GEOMETRIC_PRESENTATION_REPRESENTATION('',(#240),#69491);
#218=SHAPE_REPRESENTATION_RELATIONSHIP('SRR','None',#69575,#229);
#229=ADVANCED_BREP_SHAPE_REPRESENTATION('',(#251),#69484);
#240=STYLED_ITEM('',(#69639),#251);
#251=MANIFOLD_SOLID_BREP('Body1',#14735);
#292=B_SPLINE_SURFACE_WITH_KNOTS('',3,3,((#55167,#55168,#55169,#55170,#55171,
#55172,#55173,#55174,#55175,#55176,#55177,#55178,#55179,#55180,#55181,#55182,
#55183,#55184,#55185,#55186,#55187,#55188,#55189,#55190,#55191,#55192,#55193,
#55194,#55195,#55196,#55197,#55198,#55199,#55200,#55201,#55202,#55203,#55204,
#55205,#55206,#55207,#55208,#55209,#55210,#55211,#55212,#55213,#55214,#55215,
#55216,#55217,#55218,#55219,#55220,#55221,#55222,#55223,#55224,#55225,#55226,
#55227,#55228,#55229,#55230,#55231,#55232,#55233,#55234,#55235,#55236,#55237,
#55238,#55239,#55240,#55241,#55242,#55243,#55244,#55245,#55246,#55247,#55248,
#55249,#55250,#55251,#55252,#55253,#55254,#55255,#55256,#55257,#55258,#55259,
#55260,#55261,#55262,#55263,#55264,#55265,#55266,#55267,#55268,#55269,#55270,
#55271,#55272,#55273,#55274,#55275,#55276,#55277,#55278,#55279,#55280,#55281,
#55282,#55283,#55284,#55285,#55286,#55287,#55288,#55289,#55290,#55291,#55292,
#55293,#55294,#55295,#55296,#55297,#55298,#55299,#55300,#55301,#55302,#55303,
#55304,#55305,#55306,#55307,#55308,#55309,#55310,#55311,#55312,#55313,#55314,
#55315,#55316,#55317,#55318,#55319,#55320,#55321,#55322,#55323,#55324,#55325,
#55326,#55327,#55328,#55329,#55330,#55331,#55332,#55333,#55334,#55335,#55336,
#55337,#55338,#55339,#55340,#55341,#55342,#55343,#55344,#55345,#55346,#55347,
#55348,#55349,#55350,#55351,#55352,#55353,#55354,#55355,#55356,#55357,#55358,
#55359,#55360,#55361,#55362,#55363,#55364,#55365,#55366,#55367,#55368,#55369,
#55370,#55371,#55372,#55373,#55374,#55375,#55376,#55377,#55378,#55379,#55380,
#55381,#55382,#55383,#55384,#55385,#55386,#55387,#55388,#55389,#55390,#55391,
#55392,#55393,#55394,#55395,#55396,#55397,#55398,#55399,#55400,#55401,#55402,
#55403,#55404,#55405,#55406,#55407,#55408,#55409,#55410,#55411,#55412,#55413,
#55414,#55415,#55416,#55417,#55418,#55419,#55420,#55421,#55422,#55423,#55424,
#55425,#55426,#55427,#55428,#55429,#55430,#55431,#55432,#55433,#55434,#55435,
#55436,#55437,#55438,#55439,#55440,#55441,#55442,#55443,#55444,#55445,#55446,
#55447,#55448,#55449,#55450,#55451,#55452,#55453,#55454,#55455,#55456,#55457,
#55458,#55459,#55460,#55461,#55462,#55463,#55464,#55465,#55466,#55467,#55468,
#55469,#55470,#55471,#55472,#55473,#55474,#55475,#55476,#55477,#55478,#55479,
#55480,#55481,#55482,#55483,#55484,#55485,#55486,#55487,#55488,#55489,#55490,
#55491,#55492,#55493,#55494,#55495,#55496,#55497,#55498,#55499,#55500,#55501,
#55502,#55503,#55504,#55505,#55506,#55507,#55508,#55509,#55510,#55511,#55512,
#55513,#55514,#55515,#55516,#55517,#55518,#55519,#55520,#55521,#55522,#55523,
#55524,#55525,#55526,#55527,#55528,#55529,#55530,#55531,#55532,#55533,#55534,
#55535,#55536,#55537,#55538,#55539,#55540,#55541,#55542,#55543,#55544,#55545,
#55546,#55547,#55548,#55549,#55550,#55551,#55552,#55553,#55554,#55555,#55556,
#55557,#55558,#55559,#55560,#55561,#55562,#55563,#55564,#55565,#55566,#55567,
#55568,#55569,#55570,#55571,#55572,#55573,#55574,#55575,#55576,#55577,#55578,
#55579,#55580,#55581,#55582,#55583,#55584,#55585,#55586,#55587,#55588,#55589,
#55590,#55591,#55592,#55593,#55594,#55595,#55596,#55597,#55598,#55599,#55600,
#55601,#55602,#55603,#55604,#55605,#55606,#55607,#55608,#55609,#55610,#55611,
#55612,#55613,#55614,#55615,#55616,#55617,#55618,#55619,#55620,#55621,#55622,
#55623,#55624,#55625,#55626,#55627,#55628,#55629,#55630,#55631,#55632,#55633),
(#55634,#55635,#55636,#55637,#55638,#55639,#55640,#55641,#55642,#55643,
#55644,#55645,#55646,#55647,#55648,#55649,#55650,#55651,#55652,#55653,#55654,
#55655,#55656,#55657,#55658,#55659,#55660,#55661,#55662,#55663,#55664,#55665,
#55666,#55667,#55668,#55669,#55670,#55671,#55672,#55673,#55674,#55675,#55676,
#55677,#55678,#55679,#55680,#55681,#55682,#55683,#55684,#55685,#55686,#55687,
#55688,#55689,#55690,#55691,#55692,#55693,#55694,#55695,#55696,#55697,#55698,
#55699,#55700,#55701,#55702,#55703,#55704,#55705,#55706,#55707,#55708,#55709,
#55710,#55711,#55712,#55713,#55714,#55715,#55716,#55717,#55718,#55719,#55720,
#55721,#55722,#55723,#55724,#55725,#55726,#55727,#55728,#55729,#55730,#55731,
#55732,#55733,#55734,#55735,#55736,#55737,#55738,#55739,#55740,#55741,#55742,
#55743,#55744,#55745,#55746,#55747,#55748,#55749,#55750,#55751,#55752,#55753,
#55754,#55755,#55756,#55757,#55758,#55759,#55760,#55761,#55762,#55763,#55764,
#55765,#55766,#55767,#55768,#55769,#55770,#55771,#55772,#55773,#55774,#55775,
#55776,#55777,#55778,#55779,#55780,#55781,#55782,#55783,#55784,#55785,#55786,
#55787,#55788,#55789,#55790,#55791,#55792,#55793,#55794,#55795,#55796,#55797,
#55798,#55799,#55800,#55801,#55802,#55803,#55804,#55805,#55806,#55807,#55808,
#55809,#55810,#55811,#55812,#55813,#55814,#55815,#55816,#55817,#55818,#55819,
#55820,#55821,#55822,#55823,#55824,#55825,#55826,#55827,#55828,#55829,#55830,
#55831,#55832,#55833,#55834,#55835,#55836,#55837,#55838,#55839,#55840,#55841,
#55842,#55843,#55844,#55845,#55846,#55847,#55848,#55849,#55850,#55851,#55852,
#55853,#55854,#55855,#55856,#55857,#55858,#55859,#55860,#55861,#55862,#55863,
#55864,#55865,#55866,#55867,#55868,#55869,#55870,#55871,#55872,#55873,#55874,
#55875,#55876,#55877,#55878,#55879,#55880,#55881,#55882,#55883,#55884,#55885,
#55886,#55887,#55888,#55889,#55890,#55891,#55892,#55893,#55894,#55895,#55896,
#55897,#55898,#55899,#55900,#55901,#55902,#55903,#55904,#55905,#55906,#55907,
#55908,#55909,#55910,#55911,#55912,#55913,#55914,#55915,#55916,#55917,#55918,
#55919,#55920,#55921,#55922,#55923,#55924,#55925,#55926,#55927,#55928,#55929,
#55930,#55931,#55932,#55933,#55934,#55935,#55936,#55937,#55938,#55939,#55940,
#55941,#55942,#55943,#55944,#55945,#55946,#55947,#55948,#55949,#55950,#55951,
#55952,#55953,#55954,#55955,#55956,#55957,#55958,#55959,#55960,#55961,#55962,
#55963,#55964,#55965,#55966,#55967,#55968,#55969,#55970,#55971,#55972,#55973,
#55974,#55975,#55976,#55977,#55978,#55979,#55980,#55981,#55982,#55983,#55984,
#55985,#55986,#55987,#55988,#55989,#55990,#55991,#55992,#55993,#55994,#55995,
#55996,#55997,#55998,#55999,#56000,#56001,#56002,#56003,#56004,#56005,#56006,
#56007,#56008,#56009,#56010,#56011,#56012,#56013,#56014,#56015,#56016,#56017,
#56018,#56019,#56020,#56021,#56022,#56023,#56024,#56025,#56026,#56027,#56028,
#56029,#56030,#56031,#56032,#56033,#56034,#56035,#56036,#56037,#56038,#56039,
#56040,#56041,#56042,#56043,#56044,#56045,#56046,#56047,#56048,#56049,#56050,
#56051,#56052,#56053,#56054,#56055,#56056,#56057,#56058,#56059,#56060,#56061,
#56062,#56063,#56064,#56065,#56066,#56067,#56068,#56069,#56070,#56071,#56072,
#56073,#56074,#56075,#56076,#56077,#56078,#56079,#56080,#56081,#56082,#56083,
#56084,#56085,#56086,#56087,#56088,#56089,#56090,#56091,#56092,#56093,#56094,
#56095,#56096,#56097,#56098,#56099,#56100),(#56101,#56102,#56103,#56104,
#56105,#56106,#56107,#56108,#56109,#56110,#56111,#56112,#56113,#56114,#56115,
#56116,#56117,#56118,#56119,#56120,#56121,#56122,#56123,#56124,#56125,#56126,
#56127,#56128,#56129,#56130,#56131,#56132,#56133,#56134,#56135,#56136,#56137,
#56138,#56139,#56140,#56141,#56142,#56143,#56144,#56145,#56146,#56147,#56148,
#56149,#56150,#56151,#56152,#56153,#56154,#56155,#56156,#56157,#56158,#56159,
#56160,#56161,#56162,#56163,#56164,#56165,#56166,#56167,#56168,#56169,#56170,
#56171,#56172,#56173,#56174,#56175,#56176,#56177,#56178,#56179,#56180,#56181,
#56182,#56183,#56184,#56185,#56186,#56187,#56188,#56189,#56190,#56191,#56192,
#56193,#56194,#56195,#56196,#56197,#56198,#56199,#56200,#56201,#56202,#56203,
#56204,#56205,#56206,#56207,#56208,#56209,#56210,#56211,#56212,#56213,#56214,
#56215,#56216,#56217,#56218,#56219,#56220,#56221,#56222,#56223,#56224,#56225,
#56226,#56227,#56228,#56229,#56230,#56231,#56232,#56233,#56234,#56235,#56236,
#56237,#56238,#56239,#56240,#56241,#56242,#56243,#56244,#56245,#56246,#56247,
#56248,#56249,#56250,#56251,#56252,#56253,#56254,#56255,#56256,#56257,#56258,
#56259,#56260,#56261,#56262,#56263,#56264,#56265,#56266,#56267,#56268,#56269,
#56270,#56271,#56272,#56273,#56274,#56275,#56276,#56277,#56278,#56279,#56280,
#56281,#56282,#56283,#56284,#56285,#56286,#56287,#56288,#56289,#56290,#56291,
#56292,#56293,#56294,#56295,#56296,#56297,#56298,#56299,#56300,#56301,#56302,
#56303,#56304,#56305,#56306,#56307,#56308,#56309,#56310,#56311,#56312,#56313,
#56314,#56315,#56316,#56317,#56318,#56319,#56320,#56321,#56322,#56323,#56324,
#56325,#56326,#56327,#56328,#56329,#56330,#56331,#56332,#56333,#56334,#56335,
#56336,#56337,#56338,#56339,#56340,#56341,#56342,#56343,#56344,#56345,#56346,
#56347,#56348,#56349,#56350,#56351,#56352,#56353,#56354,#56355,#56356,#56357,
#56358,#56359,#56360,#56361,#56362,#56363,#56364,#56365,#56366,#56367,#56368,
#56369,#56370,#56371,#56372,#56373,#56374,#56375,#56376,#56377,#56378,#56379,
#56380,#56381,#56382,#56383,#56384,#56385,#56386,#56387,#56388,#56389,#56390,
#56391,#56392,#56393,#56394,#56395,#56396,#56397,#56398,#56399,#56400,#56401,
#56402,#56403,#56404,#56405,#56406,#56407,#56408,#56409,#56410,#56411,#56412,
#56413,#56414,#56415,#56416,#56417,#56418,#56419,#56420,#56421,#56422,#56423,
#56424,#56425,#56426,#56427,#56428,#56429,#56430,#56431,#56432,#56433,#56434,
#56435,#56436,#56437,#56438,#56439,#56440,#56441,#56442,#56443,#56444,#56445,
#56446,#56447,#56448,#56449,#56450,#56451,#56452,#56453,#56454,#56455,#56456,
#56457,#56458,#56459,#56460,#56461,#56462,#56463,#56464,#56465,#56466,#56467,
#56468,#56469,#56470,#56471,#56472,#56473,#56474,#56475,#56476,#56477,#56478,
#56479,#56480,#56481,#56482,#56483,#56484,#56485,#56486,#56487,#56488,#56489,
#56490,#56491,#56492,#56493,#56494,#56495,#56496,#56497,#56498,#56499,#56500,
#56501,#56502,#56503,#56504,#56505,#56506,#56507,#56508,#56509,#56510,#56511,
#56512,#56513,#56514,#56515,#56516,#56517,#56518,#56519,#56520,#56521,#56522,
#56523,#56524,#56525,#56526,#56527,#56528,#56529,#56530,#56531,#56532,#56533,
#56534,#56535,#56536,#56537,#56538,#56539,#56540,#56541,#56542,#56543,#56544,
#56545,#56546,#56547,#56548,#56549,#56550,#56551,#56552,#56553,#56554,#56555,
#56556,#56557,#56558,#56559,#56560,#56561,#56562,#56563,#56564,#56565,#56566,
#56567),(#56568,#56569,#56570,#56571,#56572,#56573,#56574,#56575,#56576,
#56577,#56578,#56579,#56580,#56581,#56582,#56583,#56584,#56585,#56586,#56587,
#56588,#56589,#56590,#56591,#56592,#56593,#56594,#56595,#56596,#56597,#56598,
#56599,#56600,#56601,#56602,#56603,#56604,#56605,#56606,#56607,#56608,#56609,
#56610,#56611,#56612,#56613,#56614,#56615,#56616,#56617,#56618,#56619,#56620,
#56621,#56622,#56623,#56624,#56625,#56626,#56627,#56628,#56629,#56630,#56631,
#56632,#56633,#56634,#56635,#56636,#56637,#56638,#56639,#56640,#56641,#56642,
#56643,#56644,#56645,#56646,#56647,#56648,#56649,#56650,#56651,#56652,#56653,
#56654,#56655,#56656,#56657,#56658,#56659,#56660,#56661,#56662,#56663,#56664,
#56665,#56666,#56667,#56668,#56669,#56670,#56671,#56672,#56673,#56674,#56675,
#56676,#56677,#56678,#56679,#56680,#56681,#56682,#56683,#56684,#56685,#56686,
#56687,#56688,#56689,#56690,#56691,#56692,#56693,#56694,#56695,#56696,#56697,
#56698,#56699,#56700,#56701,#56702,#56703,#56704,#56705,#56706,#56707,#56708,
#56709,#56710,#56711,#56712,#56713,#56714,#56715,#56716,#56717,#56718,#56719,
#56720,#56721,#56722,#56723,#56724,#56725,#56726,#56727,#56728,#56729,#56730,
#56731,#56732,#56733,#56734,#56735,#56736,#56737,#56738,#56739,#56740,#56741,
#56742,#56743,#56744,#56745,#56746,#56747,#56748,#56749,#56750,#56751,#56752,
#56753,#56754,#56755,#56756,#56757,#56758,#56759,#56760,#56761,#56762,#56763,
#56764,#56765,#56766,#56767,#56768,#56769,#56770,#56771,#56772,#56773,#56774,
#56775,#56776,#56777,#56778,#56779,#56780,#56781,#56782,#56783,#56784,#56785,
#56786,#56787,#56788,#56789,#56790,#56791,#56792,#56793,#56794,#56795,#56796,
#56797,#56798,#56799,#56800,#56801,#56802,#56803,#56804,#56805,#56806,#56807,
#56808,#56809,#56810,#56811,#56812,#56813,#56814,#56815,#56816,#56817,#56818,
#56819,#56820,#56821,#56822,#56823,#56824,#56825,#56826,#56827,#56828,#56829,
#56830,#56831,#56832,#56833,#56834,#56835,#56836,#56837,#56838,#56839,#56840,
#56841,#56842,#56843,#56844,#56845,#56846,#56847,#56848,#56849,#56850,#56851,
#56852,#56853,#56854,#56855,#56856,#56857,#56858,#56859,#56860,#56861,#56862,
#56863,#56864,#56865,#56866,#56867,#56868,#56869,#56870,#56871,#56872,#56873,
#56874,#56875,#56876,#56877,#56878,#56879,#56880,#56881,#56882,#56883,#56884,
#56885,#56886,#56887,#56888,#56889,#56890,#56891,#56892,#56893,#56894,#56895,
#56896,#56897,#56898,#56899,#56900,#56901,#56902,#56903,#56904,#56905,#56906,
#56907,#56908,#56909,#56910,#56911,#56912,#56913,#56914,#56915,#56916,#56917,
#56918,#56919,#56920,#56921,#56922,#56923,#56924,#56925,#56926,#56927,#56928,
#56929,#56930,#56931,#56932,#56933,#56934,#56935,#56936,#56937,#56938,#56939,
#56940,#56941,#56942,#56943,#56944,#56945,#56946,#56947,#56948,#56949,#56950,
#56951,#56952,#56953,#56954,#56955,#56956,#56957,#56958,#56959,#56960,#56961,
#56962,#56963,#56964,#56965,#56966,#56967,#56968,#56969,#56970,#56971,#56972,
#56973,#56974,#56975,#56976,#56977,#56978,#56979,#56980,#56981,#56982,#56983,
#56984,#56985,#56986,#56987,#56988,#56989,#56990,#56991,#56992,#56993,#56994,
#56995,#56996,#56997,#56998,#56999,#57000,#57001,#57002,#57003,#57004,#57005,
#57006,#57007,#57008,#57009,#57010,#57011,#57012,#57013,#57014,#57015,#57016,
#57017,#57018,#57019,#57020,#57021,#57022,#57023,#57024,#57025,#57026,#57027,
#57028,#57029,#57030,#57031,#57032,#57033,#57034)),.UNSPECIFIED.,.F.,.F.,
 .F.,(4,4),(4,1,1,1,1,1,1,1,1,1,1,1,1,1,1,1,1,1,1,1,1,1,1,1,1,1,1,1,1,1,
1,1,1,1,1,1,1,1,1,1,1,1,1,1,1,1,1,1,1,1,1,1,1,1,1,1,1,1,1,1,1,1,1,1,1,1,
1,1,1,1,1,1,1,1,1,1,1,1,1,1,1,1,1,1,1,1,1,1,1,1,1,1,1,1,1,1,1,1,1,1,1,1,
1,1,1,1,1,1,1,1,1,1,1,1,1,1,1,1,1,1,1,1,1,1,1,1,1,1,1,1,1,1,1,1,1,1,1,1,
1,1,1,1,1,1,1,1,1,1,1,1,1,1,1,1,1,1,1,1,1,1,1,1,1,1,1,1,1,1,1,1,1,1,1,1,
1,1,1,1,1,1,1,1,1,1,1,1,1,1,1,1,1,1,1,1,1,1,1,1,1,1,1,1,1,1,1,1,1,1,1,1,
1,1,1,1,1,1,1,1,1,1,1,1,1,1,1,1,1,1,1,1,1,1,1,1,1,1,1,1,1,1,1,1,1,1,1,1,
1,1,1,1,1,1,1,1,1,1,1,1,1,1,1,1,1,1,1,1,1,1,1,1,1,1,1,1,1,1,1,1,1,1,1,1,
1,1,1,1,1,1,1,1,1,1,1,1,1,1,1,1,1,1,1,1,1,1,1,1,1,1,1,1,1,1,1,1,1,1,1,1,
1,1,1,1,1,1,1,1,1,1,1,1,1,1,1,1,1,1,1,1,1,1,1,1,1,1,1,1,1,1,1,1,1,1,1,1,
1,1,1,1,1,1,1,1,1,1,1,1,1,1,1,1,1,1,1,1,1,1,1,1,1,1,1,1,1,1,1,1,1,1,1,1,
1,1,1,1,1,1,1,1,1,1,1,1,1,1,1,1,1,1,1,1,1,1,1,1,1,1,1,1,1,1,1,1,1,1,1,1,
1,1,1,1,1,1,1,1,1,1,1,1,1,1,1,1,1,1,1,1,1,1,1,1,1,1,1,1,1,1,1,1,1,1,1,1,
1,1,4),(0.,0.115296848757168),(8.30592286723195,8.80561008027367,9.30529729331538,
9.80498450635709,10.3046717193988,10.8043589324405,11.3040461454822,11.8037333585239,
12.3034205715656,12.8031077846074,13.3027949976491,13.8024822106908,14.3021694237325,
14.8018566367742,15.3015438498159,15.8012310628576,16.3009182758993,16.800605488941,
17.3002927019828,17.7999799150245,18.2996671280662,18.7993543411079,19.2990415541496,
19.7987287671913,20.298415980233,20.7981031932747,21.2977904063164,21.7974776193581,
22.2971648323999,22.7968520454416,23.2965392584833,23.796226471525,24.2959136845667,
24.7956008976084,25.2952881106501,25.7949753236918,26.2946625367335,26.7943497497753,
27.294036962817,27.7937241758587,28.2934113889004,28.7930986019421,29.2927858149838,
29.7924730280255,30.2921602410672,30.7918474541089,31.2915346671507,31.7912218801924,
32.2909090932341,32.7905963062758,33.2902835193175,33.7899707323592,34.2896579454009,
34.7893451584426,35.2890323714843,35.7887195845261,36.2884067975678,36.7880940106095,
37.2877812236512,37.7874684366929,38.2871556497346,38.7868428627763,39.286530075818,
39.7862172888597,40.2859045019015,40.7855917149432,41.2852789279849,41.7849661410266,
42.2846533540683,42.78434056711,43.2840277801517,43.7837149931934,44.2834022062351,
44.7830894192769,45.2827766323186,45.7824638453603,46.282151058402,46.7818382714437,
47.2815254844854,47.7812126975271,48.2808999105688,48.7805871236105,49.2802743366523,
49.779961549694,50.2796487627357,50.7793359757774,51.2790231888191,51.7787104018608,
52.2783976149025,52.7780848279442,53.2777720409859,53.7774592540276,54.2771464670694,
54.7768336801111,55.2765208931528,55.7762081061945,56.2758953192362,56.7755825322779,
57.2752697453196,57.7749569583613,58.274644171403,58.7743313844448,59.2740185974865,
59.7737058105282,60.2733930235699,60.7730802366116,61.2727674496533,61.772454662695,
62.2721418757367,62.7718290887784,63.2715163018202,63.7712035148619,64.2708907279036,
64.7705779409453,65.270265153987,65.7699523670287,66.2696395800704,66.7693267931121,
67.2690140061538,67.7687012191955,68.2683884322373,68.768075645279,69.2677628583207,
69.7674500713624,70.2671372844041,70.7668244974458,71.2665117104875,71.7661989235292,
72.265886136571,72.7655733496127,73.2652605626544,73.7649477756961,74.2646349887378,
74.7643222017795,75.2640094148212,75.7636966278629,76.2633838409046,76.7630710539463,
77.2627582669881,77.7624454800298,78.2621326930715,78.7618199061132,79.2615071191549,
79.7611943321966,80.2608815452383,80.76056875828,81.2602559713218,81.7599431843635,
82.2596303974052,82.7593176104469,83.2590048234886,83.7586920365303,84.258379249572,
84.7580664626137,85.2577536756554,85.7574408886971,86.2571281017389,86.7568153147806,
87.2565025278223,87.756189740864,88.2558769539057,88.7555641669474,89.2552513799891,
89.7549385930308,90.2546258060726,90.7543130191143,91.254000232156,91.7536874451977,
92.2533746582394,92.7530618712811,93.2527490843228,93.7524362973645,94.2521235104062,
94.7518107234479,95.2514979364897,95.7511851495314,96.2508723625731,96.7505595756148,
97.2502467886565,97.7499340016982,98.2496212147399,98.7493084277816,99.2489956408234,
99.7486828538651,100.248370066907,100.748057279948,101.24774449299,101.747431706032,
102.247118919074,102.746806132115,103.246493345157,103.746180558199,104.24586777124,
104.745554984282,105.245242197324,105.744929410366,106.244616623407,106.744303836449,
107.243991049491,107.743678262532,108.243365475574,108.743052688616,109.242739901658,
109.742427114699,110.242114327741,110.741801540783,111.241488753824,111.741175966866,
112.240863179908,112.74055039295,113.240237605991,113.739924819033,114.239612032075,
114.739299245116,115.238986458158,115.7386736712,116.238360884242,116.738048097283,
117.237735310325,117.737422523367,118.237109736408,118.73679694945,119.236484162492,
119.736171375533,120.235858588575,120.735545801617,121.235233014659,121.7349202277,
122.234607440742,122.734294653784,123.233981866825,123.733669079867,124.233356292909,
124.733043505951,125.232730718992,125.732417932034,126.232105145076,126.731792358117,
127.231479571159,127.731166784201,128.230853997243,128.730541210284,129.230228423326,
129.729915636368,130.229602849409,130.729290062451,131.228977275493,131.728664488535,
132.228351701576,132.728038914618,133.22772612766,133.727413340701,134.227100553743,
134.726787766785,135.226474979827,135.726162192868,136.22584940591,136.725536618952,
137.225223831993,137.724911045035,138.224598258077,138.724285471118,139.22397268416,
139.723659897202,140.223347110244,140.723034323285,141.222721536327,141.722408749369,
142.22209596241,142.721783175452,143.221470388494,143.721157601536,144.220844814577,
144.720532027619,145.220219240661,145.719906453702,146.219593666744,146.719280879786,
147.218968092828,147.718655305869,148.218342518911,148.718029731953,149.217716944994,
149.717404158036,150.217091371078,150.71677858412,151.216465797161,151.716153010203,
152.215840223245,152.715527436286,153.215214649328,153.71490186237,154.214589075412,
154.714276288453,155.213963501495,155.713650714537,156.213337927578,156.71302514062,
157.212712353662,157.712399566704,158.212086779745,158.711773992787,159.211461205829,
159.71114841887,160.210835631912,160.710522844954,161.210210057995,161.709897271037,
162.209584484079,162.709271697121,163.208958910162,163.708646123204,164.208333336246,
164.708020549287,165.207707762329,165.707394975371,166.207082188413,166.706769401454,
167.206456614496,167.706143827538,168.205831040579,168.705518253621,169.205205466663,
169.704892679705,170.204579892746,170.704267105788,171.20395431883,171.703641531871,
172.203328744913,172.703015957955,173.202703170997,173.702390384038,174.20207759708,
174.701764810122,175.201452023163,175.701139236205,176.200826449247,176.700513662289,
177.20020087533,177.699888088372,178.199575301414,178.699262514455,179.198949727497,
179.698636940539,180.198324153581,180.698011366622,181.197698579664,181.697385792706,
182.197073005747,182.696760218789,183.196447431831,183.696134644872,184.195821857914,
184.695509070956,185.195196283998,185.694883497039,186.194570710081,186.694257923123,
187.193945136164,187.693632349206,188.193319562248,188.69300677529,189.192693988331,
189.692381201373,190.192068414415,190.691755627456,191.191442840498,191.69113005354,
192.190817266582,192.690504479623,193.190191692665,193.689878905707,194.189566118748,
194.68925333179,195.188940544832,195.688627757874,196.188314970915,196.688002183957,
197.187689396999,197.68737661004,198.187063823082,198.686751036124,199.186438249166,
199.686125462207,200.185812675249,200.685499888291,201.185187101332,201.684874314374,
202.184561527416,202.684248740457,203.183935953499,203.683623166541,204.183310379583,
204.682997592624,205.182684805666,205.682372018708,206.182059231749,206.681746444791,
207.181433657833,207.681120870875,208.180808083916,208.680495296958,209.18018251,
209.679869723041,210.179556936083,210.679244149125,211.178931362167,211.678618575208,
212.17830578825,212.677993001292,213.177680214333,213.677367427375,214.177054640417,
214.676741853459,215.1764290665,215.676116279542,216.175803492584,216.675490705625,
217.175177918667,217.674865131709,218.174552344751,218.674239557792,219.173926770834,
219.673613983876,220.173301196917,220.672988409959,221.172675623001,221.672362836043,
222.172050049084,222.671737262126,223.171424475168,223.671111688209,224.170798901251,
224.670486114293,225.170173327334,225.669860540376,226.169547753418,226.66923496646,
227.168922179501,227.668609392543,228.168296605585,228.667983818626,229.167671031668,
229.66735824471,230.167045457752,230.666732670793,231.166419883835,231.666107096877,
232.165794309918,232.66548152296,233.165168736002,233.664855949044,234.164543162085,
234.664230375127,235.163917588169,235.66360480121,236.163292014252,236.662979227294,
237.162666440336,237.662353653377,238.162040866419,238.661728079461,239.161415292502,
239.661102505544,240.160789718586),.UNSPECIFIED.);
#293=B_SPLINE_SURFACE_WITH_KNOTS('',3,3,((#57211,#57212,#57213,#57214,#57215,
#57216,#57217,#57218,#57219,#57220,#57221,#57222,#57223,#57224,#57225,#57226,
#57227,#57228,#57229,#57230,#57231,#57232,#57233,#57234,#57235,#57236,#57237,
#57238,#57239,#57240,#57241,#57242,#57243,#57244,#57245,#57246,#57247,#57248,
#57249,#57250,#57251,#57252,#57253,#57254,#57255,#57256,#57257,#57258,#57259,
#57260,#57261,#57262,#57263,#57264,#57265,#57266,#57267,#57268,#57269,#57270,
#57271,#57272,#57273,#57274,#57275,#57276,#57277,#57278,#57279,#57280,#57281,
#57282,#57283,#57284,#57285,#57286,#57287,#57288,#57289,#57290,#57291,#57292,
#57293,#57294,#57295,#57296,#57297,#57298,#57299,#57300,#57301,#57302,#57303,
#57304,#57305,#57306,#57307,#57308,#57309,#57310,#57311,#57312,#57313,#57314,
#57315,#57316,#57317,#57318,#57319,#57320,#57321,#57322,#57323,#57324,#57325,
#57326,#57327,#57328,#57329,#57330,#57331,#57332,#57333,#57334,#57335,#57336,
#57337,#57338,#57339,#57340,#57341,#57342,#57343,#57344,#57345,#57346,#57347,
#57348,#57349,#57350,#57351,#57352,#57353,#57354,#57355,#57356,#57357,#57358,
#57359,#57360,#57361,#57362,#57363,#57364,#57365,#57366,#57367,#57368,#57369,
#57370,#57371,#57372,#57373,#57374,#57375,#57376,#57377,#57378,#57379,#57380,
#57381,#57382,#57383,#57384,#57385,#57386,#57387,#57388,#57389,#57390,#57391,
#57392,#57393,#57394,#57395,#57396,#57397,#57398,#57399,#57400,#57401,#57402,
#57403,#57404,#57405,#57406,#57407,#57408,#57409,#57410,#57411,#57412,#57413,
#57414,#57415,#57416,#57417,#57418,#57419,#57420,#57421,#57422,#57423,#57424,
#57425,#57426,#57427,#57428,#57429,#57430,#57431,#57432,#57433,#57434,#57435,
#57436,#57437,#57438,#57439,#57440,#57441,#57442,#57443,#57444,#57445,#57446,
#57447,#57448,#57449,#57450,#57451,#57452,#57453,#57454,#57455,#57456,#57457,
#57458,#57459,#57460,#57461,#57462,#57463,#57464,#57465,#57466,#57467,#57468,
#57469,#57470,#57471,#57472,#57473,#57474,#57475,#57476,#57477,#57478,#57479,
#57480,#57481,#57482,#57483,#57484,#57485,#57486,#57487,#57488,#57489,#57490,
#57491,#57492,#57493,#57494,#57495,#57496,#57497,#57498,#57499,#57500,#57501,
#57502,#57503,#57504,#57505,#57506,#57507,#57508,#57509,#57510,#57511,#57512,
#57513,#57514,#57515,#57516,#57517,#57518,#57519,#57520,#57521,#57522,#57523,
#57524,#57525,#57526,#57527,#57528,#57529,#57530,#57531,#57532,#57533,#57534,
#57535,#57536,#57537,#57538,#57539,#57540,#57541,#57542,#57543,#57544,#57545,
#57546,#57547,#57548,#57549,#57550,#57551,#57552,#57553,#57554,#57555,#57556,
#57557,#57558,#57559,#57560,#57561,#57562,#57563,#57564,#57565,#57566,#57567,
#57568,#57569,#57570,#57571,#57572,#57573,#57574,#57575,#57576,#57577,#57578,
#57579,#57580,#57581,#57582,#57583,#57584,#57585,#57586,#57587,#57588,#57589,
#57590,#57591,#57592,#57593,#57594,#57595,#57596,#57597,#57598,#57599,#57600,
#57601,#57602,#57603,#57604,#57605,#57606,#57607,#57608,#57609,#57610,#57611,
#57612,#57613,#57614,#57615,#57616,#57617,#57618,#57619,#57620,#57621,#57622,
#57623,#57624,#57625,#57626,#57627,#57628,#57629,#57630,#57631,#57632,#57633,
#57634,#57635,#57636,#57637,#57638,#57639,#57640,#57641,#57642,#57643,#57644,
#57645,#57646,#57647,#57648,#57649,#57650,#57651,#57652,#57653,#57654,#57655,
#57656,#57657,#57658,#57659,#57660,#57661,#57662,#57663,#57664,#57665,#57666,
#57667,#57668,#57669,#57670,#57671,#57672,#57673,#57674,#57675,#57676,#57677),
(#57678,#57679,#57680,#57681,#57682,#57683,#57684,#57685,#57686,#57687,
#57688,#57689,#57690,#57691,#57692,#57693,#57694,#57695,#57696,#57697,#57698,
#57699,#57700,#57701,#57702,#57703,#57704,#57705,#57706,#57707,#57708,#57709,
#57710,#57711,#57712,#57713,#57714,#57715,#57716,#57717,#57718,#57719,#57720,
#57721,#57722,#57723,#57724,#57725,#57726,#57727,#57728,#57729,#57730,#57731,
#57732,#57733,#57734,#57735,#57736,#57737,#57738,#57739,#57740,#57741,#57742,
#57743,#57744,#57745,#57746,#57747,#57748,#57749,#57750,#57751,#57752,#57753,
#57754,#57755,#57756,#57757,#57758,#57759,#57760,#57761,#57762,#57763,#57764,
#57765,#57766,#57767,#57768,#57769,#57770,#57771,#57772,#57773,#57774,#57775,
#57776,#57777,#57778,#57779,#57780,#57781,#57782,#57783,#57784,#57785,#57786,
#57787,#57788,#57789,#57790,#57791,#57792,#57793,#57794,#57795,#57796,#57797,
#57798,#57799,#57800,#57801,#57802,#57803,#57804,#57805,#57806,#57807,#57808,
#57809,#57810,#57811,#57812,#57813,#57814,#57815,#57816,#57817,#57818,#57819,
#57820,#57821,#57822,#57823,#57824,#57825,#57826,#57827,#57828,#57829,#57830,
#57831,#57832,#57833,#57834,#57835,#57836,#57837,#57838,#57839,#57840,#57841,
#57842,#57843,#57844,#57845,#57846,#57847,#57848,#57849,#57850,#57851,#57852,
#57853,#57854,#57855,#57856,#57857,#57858,#57859,#57860,#57861,#57862,#57863,
#57864,#57865,#57866,#57867,#57868,#57869,#57870,#57871,#57872,#57873,#57874,
#57875,#57876,#57877,#57878,#57879,#57880,#57881,#57882,#57883,#57884,#57885,
#57886,#57887,#57888,#57889,#57890,#57891,#57892,#57893,#57894,#57895,#57896,
#57897,#57898,#57899,#57900,#57901,#57902,#57903,#57904,#57905,#57906,#57907,
#57908,#57909,#57910,#57911,#57912,#57913,#57914,#57915,#57916,#57917,#57918,
#57919,#57920,#57921,#57922,#57923,#57924,#57925,#57926,#57927,#57928,#57929,
#57930,#57931,#57932,#57933,#57934,#57935,#57936,#57937,#57938,#57939,#57940,
#57941,#57942,#57943,#57944,#57945,#57946,#57947,#57948,#57949,#57950,#57951,
#57952,#57953,#57954,#57955,#57956,#57957,#57958,#57959,#57960,#57961,#57962,
#57963,#57964,#57965,#57966,#57967,#57968,#57969,#57970,#57971,#57972,#57973,
#57974,#57975,#57976,#57977,#57978,#57979,#57980,#57981,#57982,#57983,#57984,
#57985,#57986,#57987,#57988,#57989,#57990,#57991,#57992,#57993,#57994,#57995,
#57996,#57997,#57998,#57999,#58000,#58001,#58002,#58003,#58004,#58005,#58006,
#58007,#58008,#58009,#58010,#58011,#58012,#58013,#58014,#58015,#58016,#58017,
#58018,#58019,#58020,#58021,#58022,#58023,#58024,#58025,#58026,#58027,#58028,
#58029,#58030,#58031,#58032,#58033,#58034,#58035,#58036,#58037,#58038,#58039,
#58040,#58041,#58042,#58043,#58044,#58045,#58046,#58047,#58048,#58049,#58050,
#58051,#58052,#58053,#58054,#58055,#58056,#58057,#58058,#58059,#58060,#58061,
#58062,#58063,#58064,#58065,#58066,#58067,#58068,#58069,#58070,#58071,#58072,
#58073,#58074,#58075,#58076,#58077,#58078,#58079,#58080,#58081,#58082,#58083,
#58084,#58085,#58086,#58087,#58088,#58089,#58090,#58091,#58092,#58093,#58094,
#58095,#58096,#58097,#58098,#58099,#58100,#58101,#58102,#58103,#58104,#58105,
#58106,#58107,#58108,#58109,#58110,#58111,#58112,#58113,#58114,#58115,#58116,
#58117,#58118,#58119,#58120,#58121,#58122,#58123,#58124,#58125,#58126,#58127,
#58128,#58129,#58130,#58131,#58132,#58133,#58134,#58135,#58136,#58137,#58138,
#58139,#58140,#58141,#58142,#58143,#58144),(#58145,#58146,#58147,#58148,
#58149,#58150,#58151,#58152,#58153,#58154,#58155,#58156,#58157,#58158,#58159,
#58160,#58161,#58162,#58163,#58164,#58165,#58166,#58167,#58168,#58169,#58170,
#58171,#58172,#58173,#58174,#58175,#58176,#58177,#58178,#58179,#58180,#58181,
#58182,#58183,#58184,#58185,#58186,#58187,#58188,#58189,#58190,#58191,#58192,
#58193,#58194,#58195,#58196,#58197,#58198,#58199,#58200,#58201,#58202,#58203,
#58204,#58205,#58206,#58207,#58208,#58209,#58210,#58211,#58212,#58213,#58214,
#58215,#58216,#58217,#58218,#58219,#58220,#58221,#58222,#58223,#58224,#58225,
#58226,#58227,#58228,#58229,#58230,#58231,#58232,#58233,#58234,#58235,#58236,
#58237,#58238,#58239,#58240,#58241,#58242,#58243,#58244,#58245,#58246,#58247,
#58248,#58249,#58250,#58251,#58252,#58253,#58254,#58255,#58256,#58257,#58258,
#58259,#58260,#58261,#58262,#58263,#58264,#58265,#58266,#58267,#58268,#58269,
#58270,#58271,#58272,#58273,#58274,#58275,#58276,#58277,#58278,#58279,#58280,
#58281,#58282,#58283,#58284,#58285,#58286,#58287,#58288,#58289,#58290,#58291,
#58292,#58293,#58294,#58295,#58296,#58297,#58298,#58299,#58300,#58301,#58302,
#58303,#58304,#58305,#58306,#58307,#58308,#58309,#58310,#58311,#58312,#58313,
#58314,#58315,#58316,#58317,#58318,#58319,#58320,#58321,#58322,#58323,#58324,
#58325,#58326,#58327,#58328,#58329,#58330,#58331,#58332,#58333,#58334,#58335,
#58336,#58337,#58338,#58339,#58340,#58341,#58342,#58343,#58344,#58345,#58346,
#58347,#58348,#58349,#58350,#58351,#58352,#58353,#58354,#58355,#58356,#58357,
#58358,#58359,#58360,#58361,#58362,#58363,#58364,#58365,#58366,#58367,#58368,
#58369,#58370,#58371,#58372,#58373,#58374,#58375,#58376,#58377,#58378,#58379,
#58380,#58381,#58382,#58383,#58384,#58385,#58386,#58387,#58388,#58389,#58390,
#58391,#58392,#58393,#58394,#58395,#58396,#58397,#58398,#58399,#58400,#58401,
#58402,#58403,#58404,#58405,#58406,#58407,#58408,#58409,#58410,#58411,#58412,
#58413,#58414,#58415,#58416,#58417,#58418,#58419,#58420,#58421,#58422,#58423,
#58424,#58425,#58426,#58427,#58428,#58429,#58430,#58431,#58432,#58433,#58434,
#58435,#58436,#58437,#58438,#58439,#58440,#58441,#58442,#58443,#58444,#58445,
#58446,#58447,#58448,#58449,#58450,#58451,#58452,#58453,#58454,#58455,#58456,
#58457,#58458,#58459,#58460,#58461,#58462,#58463,#58464,#58465,#58466,#58467,
#58468,#58469,#58470,#58471,#58472,#58473,#58474,#58475,#58476,#58477,#58478,
#58479,#58480,#58481,#58482,#58483,#58484,#58485,#58486,#58487,#58488,#58489,
#58490,#58491,#58492,#58493,#58494,#58495,#58496,#58497,#58498,#58499,#58500,
#58501,#58502,#58503,#58504,#58505,#58506,#58507,#58508,#58509,#58510,#58511,
#58512,#58513,#58514,#58515,#58516,#58517,#58518,#58519,#58520,#58521,#58522,
#58523,#58524,#58525,#58526,#58527,#58528,#58529,#58530,#58531,#58532,#58533,
#58534,#58535,#58536,#58537,#58538,#58539,#58540,#58541,#58542,#58543,#58544,
#58545,#58546,#58547,#58548,#58549,#58550,#58551,#58552,#58553,#58554,#58555,
#58556,#58557,#58558,#58559,#58560,#58561,#58562,#58563,#58564,#58565,#58566,
#58567,#58568,#58569,#58570,#58571,#58572,#58573,#58574,#58575,#58576,#58577,
#58578,#58579,#58580,#58581,#58582,#58583,#58584,#58585,#58586,#58587,#58588,
#58589,#58590,#58591,#58592,#58593,#58594,#58595,#58596,#58597,#58598,#58599,
#58600,#58601,#58602,#58603,#58604,#58605,#58606,#58607,#58608,#58609,#58610,
#58611),(#58612,#58613,#58614,#58615,#58616,#58617,#58618,#58619,#58620,
#58621,#58622,#58623,#58624,#58625,#58626,#58627,#58628,#58629,#58630,#58631,
#58632,#58633,#58634,#58635,#58636,#58637,#58638,#58639,#58640,#58641,#58642,
#58643,#58644,#58645,#58646,#58647,#58648,#58649,#58650,#58651,#58652,#58653,
#58654,#58655,#58656,#58657,#58658,#58659,#58660,#58661,#58662,#58663,#58664,
#58665,#58666,#58667,#58668,#58669,#58670,#58671,#58672,#58673,#58674,#58675,
#58676,#58677,#58678,#58679,#58680,#58681,#58682,#58683,#58684,#58685,#58686,
#58687,#58688,#58689,#58690,#58691,#58692,#58693,#58694,#58695,#58696,#58697,
#58698,#58699,#58700,#58701,#58702,#58703,#58704,#58705,#58706,#58707,#58708,
#58709,#58710,#58711,#58712,#58713,#58714,#58715,#58716,#58717,#58718,#58719,
#58720,#58721,#58722,#58723,#58724,#58725,#58726,#58727,#58728,#58729,#58730,
#58731,#58732,#58733,#58734,#58735,#58736,#58737,#58738,#58739,#58740,#58741,
#58742,#58743,#58744,#58745,#58746,#58747,#58748,#58749,#58750,#58751,#58752,
#58753,#58754,#58755,#58756,#58757,#58758,#58759,#58760,#58761,#58762,#58763,
#58764,#58765,#58766,#58767,#58768,#58769,#58770,#58771,#58772,#58773,#58774,
#58775,#58776,#58777,#58778,#58779,#58780,#58781,#58782,#58783,#58784,#58785,
#58786,#58787,#58788,#58789,#58790,#58791,#58792,#58793,#58794,#58795,#58796,
#58797,#58798,#58799,#58800,#58801,#58802,#58803,#58804,#58805,#58806,#58807,
#58808,#58809,#58810,#58811,#58812,#58813,#58814,#58815,#58816,#58817,#58818,
#58819,#58820,#58821,#58822,#58823,#58824,#58825,#58826,#58827,#58828,#58829,
#58830,#58831,#58832,#58833,#58834,#58835,#58836,#58837,#58838,#58839,#58840,
#58841,#58842,#58843,#58844,#58845,#58846,#58847,#58848,#58849,#58850,#58851,
#58852,#58853,#58854,#58855,#58856,#58857,#58858,#58859,#58860,#58861,#58862,
#58863,#58864,#58865,#58866,#58867,#58868,#58869,#58870,#58871,#58872,#58873,
#58874,#58875,#58876,#58877,#58878,#58879,#58880,#58881,#58882,#58883,#58884,
#58885,#58886,#58887,#58888,#58889,#58890,#58891,#58892,#58893,#58894,#58895,
#58896,#58897,#58898,#58899,#58900,#58901,#58902,#58903,#58904,#58905,#58906,
#58907,#58908,#58909,#58910,#58911,#58912,#58913,#58914,#58915,#58916,#58917,
#58918,#58919,#58920,#58921,#58922,#58923,#58924,#58925,#58926,#58927,#58928,
#58929,#58930,#58931,#58932,#58933,#58934,#58935,#58936,#58937,#58938,#58939,
#58940,#58941,#58942,#58943,#58944,#58945,#58946,#58947,#58948,#58949,#58950,
#58951,#58952,#58953,#58954,#58955,#58956,#58957,#58958,#58959,#58960,#58961,
#58962,#58963,#58964,#58965,#58966,#58967,#58968,#58969,#58970,#58971,#58972,
#58973,#58974,#58975,#58976,#58977,#58978,#58979,#58980,#58981,#58982,#58983,
#58984,#58985,#58986,#58987,#58988,#58989,#58990,#58991,#58992,#58993,#58994,
#58995,#58996,#58997,#58998,#58999,#59000,#59001,#59002,#59003,#59004,#59005,
#59006,#59007,#59008,#59009,#59010,#59011,#59012,#59013,#59014,#59015,#59016,
#59017,#59018,#59019,#59020,#59021,#59022,#59023,#59024,#59025,#59026,#59027,
#59028,#59029,#59030,#59031,#59032,#59033,#59034,#59035,#59036,#59037,#59038,
#59039,#59040,#59041,#59042,#59043,#59044,#59045,#59046,#59047,#59048,#59049,
#59050,#59051,#59052,#59053,#59054,#59055,#59056,#59057,#59058,#59059,#59060,
#59061,#59062,#59063,#59064,#59065,#59066,#59067,#59068,#59069,#59070,#59071,
#59072,#59073,#59074,#59075,#59076,#59077,#59078)),.UNSPECIFIED.,.F.,.F.,
 .F.,(4,4),(4,1,1,1,1,1,1,1,1,1,1,1,1,1,1,1,1,1,1,1,1,1,1,1,1,1,1,1,1,1,
1,1,1,1,1,1,1,1,1,1,1,1,1,1,1,1,1,1,1,1,1,1,1,1,1,1,1,1,1,1,1,1,1,1,1,1,
1,1,1,1,1,1,1,1,1,1,1,1,1,1,1,1,1,1,1,1,1,1,1,1,1,1,1,1,1,1,1,1,1,1,1,1,
1,1,1,1,1,1,1,1,1,1,1,1,1,1,1,1,1,1,1,1,1,1,1,1,1,1,1,1,1,1,1,1,1,1,1,1,
1,1,1,1,1,1,1,1,1,1,1,1,1,1,1,1,1,1,1,1,1,1,1,1,1,1,1,1,1,1,1,1,1,1,1,1,
1,1,1,1,1,1,1,1,1,1,1,1,1,1,1,1,1,1,1,1,1,1,1,1,1,1,1,1,1,1,1,1,1,1,1,1,
1,1,1,1,1,1,1,1,1,1,1,1,1,1,1,1,1,1,1,1,1,1,1,1,1,1,1,1,1,1,1,1,1,1,1,1,
1,1,1,1,1,1,1,1,1,1,1,1,1,1,1,1,1,1,1,1,1,1,1,1,1,1,1,1,1,1,1,1,1,1,1,1,
1,1,1,1,1,1,1,1,1,1,1,1,1,1,1,1,1,1,1,1,1,1,1,1,1,1,1,1,1,1,1,1,1,1,1,1,
1,1,1,1,1,1,1,1,1,1,1,1,1,1,1,1,1,1,1,1,1,1,1,1,1,1,1,1,1,1,1,1,1,1,1,1,
1,1,1,1,1,1,1,1,1,1,1,1,1,1,1,1,1,1,1,1,1,1,1,1,1,1,1,1,1,1,1,1,1,1,1,1,
1,1,1,1,1,1,1,1,1,1,1,1,1,1,1,1,1,1,1,1,1,1,1,1,1,1,1,1,1,1,1,1,1,1,1,1,
1,1,1,1,1,1,1,1,1,1,1,1,1,1,1,1,1,1,1,1,1,1,1,1,1,1,1,1,1,1,1,1,1,1,1,1,
1,1,4),(0.,0.115296848757168),(11.6154215191109,12.1151087321526,12.6147959451943,
13.114483158236,13.6141703712778,14.1138575843195,14.6135447973612,15.1132320104029,
15.6129192234446,16.1126064364863,16.612293649528,17.1119808625697,17.6116680756114,
18.1113552886532,18.6110425016949,19.1107297147366,19.6104169277783,20.11010414082,
20.6097913538617,21.1094785669034,21.6091657799451,22.1088529929868,22.6085402060286,
23.1082274190703,23.607914632112,24.1076018451537,24.6072890581954,25.1069762712371,
25.6066634842788,26.1063506973205,26.6060379103622,27.1057251234039,27.6054123364457,
28.1050995494874,28.6047867625291,29.1044739755708,29.6041611886125,30.1038484016542,
30.6035356146959,31.1032228277376,31.6029100407793,32.1025972538211,32.6022844668628,
33.1019716799045,33.6016588929462,34.1013461059879,34.6010333190296,35.1007205320713,
35.600407745113,36.1000949581547,36.5997821711965,37.0994693842382,37.5991565972799,
38.0988438103216,38.5985310233633,39.098218236405,39.5979054494467,40.0975926624884,
40.5972798755301,41.0969670885719,41.5966543016136,42.0963415146553,42.596028727697,
43.0957159407387,43.5954031537804,44.0950903668221,44.5947775798638,45.0944647929055,
45.5941520059473,46.093839218989,46.5935264320307,47.0932136450724,47.5929008581141,
48.0925880711558,48.5922752841975,49.0919624972392,49.5916497102809,50.0913369233227,
50.5910241363644,51.0907113494061,51.5903985624478,52.0900857754895,52.5897729885312,
53.0894602015729,53.5891474146146,54.0888346276563,54.588521840698,55.0882090537398,
55.5878962667815,56.0875834798232,56.5872706928649,57.0869579059066,57.5866451189483,
58.08633233199,58.5860195450317,59.0857067580734,59.5853939711152,60.0850811841569,
60.5847683971986,61.0844556102403,61.584142823282,62.0838300363237,62.5835172493654,
63.0832044624071,63.5828916754488,64.0825788884906,64.5822661015323,65.081953314574,
65.5816405276157,66.0813277406574,66.5810149536991,67.0807021667408,67.5803893797825,
68.0800765928242,68.579763805866,69.0794510189077,69.5791382319494,70.0788254449911,
70.5785126580328,71.0781998710745,71.5778870841162,72.0775742971579,72.5772615101996,
73.0769487232413,73.5766359362831,74.0763231493248,74.5760103623665,75.0756975754082,
75.5753847884499,76.0750720014916,76.5747592145333,77.074446427575,77.5741336406168,
78.0738208536585,78.5735080667002,79.0731952797419,79.5728824927836,80.0725697058253,
80.572256918867,81.0719441319087,81.5716313449504,82.0713185579921,82.5710057710339,
83.0706929840756,83.5703801971173,84.070067410159,84.5697546232007,85.0694418362424,
85.5691290492841,86.0688162623258,86.5685034753675,87.0681906884093,87.567877901451,
88.0675651144927,88.5672523275344,89.0669395405761,89.5666267536178,90.0663139666595,
90.5660011797012,91.0656883927429,91.5653756057847,92.0650628188264,92.5647500318681,
93.0644372449098,93.5641244579515,94.0638116709932,94.5634988840349,95.0631860970766,
95.5628733101183,96.06256052316,96.5622477362018,97.0619349492435,97.5616221622852,
98.0613093753269,98.5609965883686,99.0606838014103,99.560371014452,100.060058227494,
100.559745440535,101.059432653577,101.559119866619,102.058807079661,102.558494292702,
103.058181505744,103.557868718786,104.057555931827,104.557243144869,105.056930357911,
105.556617570953,106.056304783994,106.555991997036,107.055679210078,107.555366423119,
108.055053636161,108.554740849203,109.054428062245,109.554115275286,110.053802488328,
110.55348970137,111.053176914411,111.552864127453,112.052551340495,112.552238553537,
113.051925766578,113.55161297962,114.051300192662,114.550987405703,115.050674618745,
115.550361831787,116.050049044828,116.54973625787,117.049423470912,117.549110683954,
118.048797896995,118.548485110037,119.048172323079,119.54785953612,120.047546749162,
120.547233962204,121.046921175246,121.546608388287,122.046295601329,122.545982814371,
123.045670027412,123.545357240454,124.045044453496,124.544731666538,125.044418879579,
125.544106092621,126.043793305663,126.543480518704,127.043167731746,127.542854944788,
128.04254215783,128.542229370871,129.041916583913,129.541603796955,130.041291009996,
130.540978223038,131.04066543608,131.540352649122,132.040039862163,132.539727075205,
133.039414288247,133.539101501288,134.03878871433,134.538475927372,135.038163140414,
135.537850353455,136.037537566497,136.537224779539,137.03691199258,137.536599205622,
138.036286418664,138.535973631705,139.035660844747,139.535348057789,140.035035270831,
140.534722483872,141.034409696914,141.534096909956,142.033784122997,142.533471336039,
143.033158549081,143.532845762123,144.032532975164,144.532220188206,145.031907401248,
145.531594614289,146.031281827331,146.530969040373,147.030656253415,147.530343466456,
148.030030679498,148.52971789254,149.029405105581,149.529092318623,150.028779531665,
150.528466744707,151.028153957748,151.52784117079,152.027528383832,152.527215596873,
153.026902809915,153.526590022957,154.026277235998,154.52596444904,155.025651662082,
155.525338875124,156.025026088165,156.524713301207,157.024400514249,157.52408772729,
158.023774940332,158.523462153374,159.023149366416,159.522836579457,160.022523792499,
160.522211005541,161.021898218582,161.521585431624,162.021272644666,162.520959857708,
163.020647070749,163.520334283791,164.020021496833,164.519708709874,165.019395922916,
165.519083135958,166.018770349,166.518457562041,167.018144775083,167.517831988125,
168.017519201166,168.517206414208,169.01689362725,169.516580840292,170.016268053333,
170.515955266375,171.015642479417,171.515329692458,172.0150169055,172.514704118542,
173.014391331584,173.514078544625,174.013765757667,174.513452970709,175.01314018375,
175.512827396792,176.012514609834,176.512201822876,177.011889035917,177.511576248959,
178.011263462001,178.510950675042,179.010637888084,179.510325101126,180.010012314167,
180.509699527209,181.009386740251,181.509073953293,182.008761166334,182.508448379376,
183.008135592418,183.507822805459,184.007510018501,184.507197231543,185.006884444585,
185.506571657626,186.006258870668,186.50594608371,187.005633296751,187.505320509793,
188.005007722835,188.504694935877,189.004382148918,189.50406936196,190.003756575002,
190.503443788043,191.003131001085,191.502818214127,192.002505427169,192.50219264021,
193.001879853252,193.501567066294,194.001254279335,194.500941492377,195.000628705419,
195.500315918461,196.000003131502,196.499690344544,196.999377557586,197.499064770627,
197.998751983669,198.498439196711,198.998126409752,199.497813622794,199.997500835836,
200.497188048878,200.996875261919,201.496562474961,201.996249688003,202.495936901044,
202.995624114086,203.495311327128,203.99499854017,204.494685753211,204.994372966253,
205.494060179295,205.993747392336,206.493434605378,206.99312181842,207.492809031462,
207.992496244503,208.492183457545,208.991870670587,209.491557883628,209.99124509667,
210.490932309712,210.990619522754,211.490306735795,211.989993948837,212.489681161879,
212.98936837492,213.489055587962,213.988742801004,214.488430014046,214.988117227087,
215.487804440129,215.987491653171,216.487178866212,216.986866079254,217.486553292296,
217.986240505338,218.485927718379,218.985614931421,219.485302144463,219.984989357504,
220.484676570546,220.984363783588,221.484050996629,221.983738209671,222.483425422713,
222.983112635755,223.482799848796,223.982487061838,224.48217427488,224.981861487921,
225.481548700963,225.981235914005,226.480923127047,226.980610340088,227.48029755313,
227.979984766172,228.479671979213,228.979359192255,229.479046405297,229.978733618339,
230.47842083138,230.978108044422,231.477795257464,231.977482470505,232.477169683547,
232.976856896589,233.476544109631,233.976231322672,234.475918535714,234.975605748756,
235.475292961797,235.974980174839,236.474667387881,236.974354600923,237.474041813964,
237.973729027006,238.473416240048,238.973103453089,239.472790666131,239.972477879173,
240.472165092214,240.971852305256,241.471539518298,241.97122673134,242.470913944381,
242.970601157423,243.470288370465),.UNSPECIFIED.);
#351=FACE_BOUND('',#1933,.T.);
#352=FACE_BOUND('',#1935,.T.);
#353=FACE_BOUND('',#1943,.T.);
#354=FACE_BOUND('',#1946,.T.);
#479=PLANE('',#15561);
#480=PLANE('',#15562);
#481=PLANE('',#15563);
#482=PLANE('',#15564);
#483=PLANE('',#15565);
#484=PLANE('',#15566);
#485=PLANE('',#15567);
#486=PLANE('',#15571);
#487=PLANE('',#15572);
#488=PLANE('',#15576);
#489=PLANE('',#15580);
#490=PLANE('',#15584);
#491=PLANE('',#15585);
#1017=FACE_OUTER_BOUND('',#1851,.T.);
#1018=FACE_OUTER_BOUND('',#1852,.T.);
#1019=FACE_OUTER_BOUND('',#1853,.T.);
#1020=FACE_OUTER_BOUND('',#1854,.T.);
#1021=FACE_OUTER_BOUND('',#1855,.T.);
#1022=FACE_OUTER_BOUND('',#1856,.T.);
#1023=FACE_OUTER_BOUND('',#1857,.T.);
#1024=FACE_OUTER_BOUND('',#1858,.T.);
#1025=FACE_OUTER_BOUND('',#1859,.T.);
#1026=FACE_OUTER_BOUND('',#1860,.T.);
#1027=FACE_OUTER_BOUND('',#1861,.T.);
#1028=FACE_OUTER_BOUND('',#1862,.T.);
#1029=FACE_OUTER_BOUND('',#1863,.T.);
#1030=FACE_OUTER_BOUND('',#1864,.T.);
#1031=FACE_OUTER_BOUND('',#1865,.T.);
#1032=FACE_OUTER_BOUND('',#1866,.T.);
#1033=FACE_OUTER_BOUND('',#1867,.T.);
#1034=FACE_OUTER_BOUND('',#1868,.T.);
#1035=FACE_OUTER_BOUND('',#1869,.T.);
#1036=FACE_OUTER_BOUND('',#1870,.T.);
#1037=FACE_OUTER_BOUND('',#1871,.T.);
#1038=FACE_OUTER_BOUND('',#1872,.T.);
#1039=FACE_OUTER_BOUND('',#1873,.T.);
#1040=FACE_OUTER_BOUND('',#1874,.T.);
#1041=FACE_OUTER_BOUND('',#1875,.T.);
#1042=FACE_OUTER_BOUND('',#1876,.T.);
#1043=FACE_OUTER_BOUND('',#1877,.T.);
#1044=FACE_OUTER_BOUND('',#1878,.T.);
#1045=FACE_OUTER_BOUND('',#1879,.T.);
#1046=FACE_OUTER_BOUND('',#1880,.T.);
#1047=FACE_OUTER_BOUND('',#1881,.T.);
#1048=FACE_OUTER_BOUND('',#1882,.T.);
#1049=FACE_OUTER_BOUND('',#1883,.T.);
#1050=FACE_OUTER_BOUND('',#1884,.T.);
#1051=FACE_OUTER_BOUND('',#1885,.T.);
#1052=FACE_OUTER_BOUND('',#1886,.T.);
#1053=FACE_OUTER_BOUND('',#1887,.T.);
#1054=FACE_OUTER_BOUND('',#1888,.T.);
#1055=FACE_OUTER_BOUND('',#1889,.T.);
#1056=FACE_OUTER_BOUND('',#1890,.T.);
#1057=FACE_OUTER_BOUND('',#1891,.T.);
#1058=FACE_OUTER_BOUND('',#1892,.T.);
#1059=FACE_OUTER_BOUND('',#1893,.T.);
#1060=FACE_OUTER_BOUND('',#1894,.T.);
#1061=FACE_OUTER_BOUND('',#1895,.T.);
#1062=FACE_OUTER_BOUND('',#1896,.T.);
#1063=FACE_OUTER_BOUND('',#1897,.T.);
#1064=FACE_OUTER_BOUND('',#1898,.T.);
#1065=FACE_OUTER_BOUND('',#1899,.T.);
#1066=FACE_OUTER_BOUND('',#1900,.T.);
#1067=FACE_OUTER_BOUND('',#1901,.T.);
#1068=FACE_OUTER_BOUND('',#1902,.T.);
#1069=FACE_OUTER_BOUND('',#1903,.T.);
#1070=FACE_OUTER_BOUND('',#1904,.T.);
#1071=FACE_OUTER_BOUND('',#1905,.T.);
#1072=FACE_OUTER_BOUND('',#1906,.T.);
#1073=FACE_OUTER_BOUND('',#1907,.T.);
#1074=FACE_OUTER_BOUND('',#1908,.T.);
#1075=FACE_OUTER_BOUND('',#1909,.T.);
#1076=FACE_OUTER_BOUND('',#1910,.T.);
#1077=FACE_OUTER_BOUND('',#1911,.T.);
#1078=FACE_OUTER_BOUND('',#1912,.T.);
#1079=FACE_OUTER_BOUND('',#1913,.T.);
#1080=FACE_OUTER_BOUND('',#1914,.T.);
#1081=FACE_OUTER_BOUND('',#1915,.T.);
#1082=FACE_OUTER_BOUND('',#1916,.T.);
#1083=FACE_OUTER_BOUND('',#1917,.T.);
#1084=FACE_OUTER_BOUND('',#1918,.T.);
#1085=FACE_OUTER_BOUND('',#1919,.T.);
#1086=FACE_OUTER_BOUND('',#1920,.T.);
#1087=FACE_OUTER_BOUND('',#1921,.T.);
#1088=FACE_OUTER_BOUND('',#1922,.T.);
#1089=FACE_OUTER_BOUND('',#1923,.T.);
#1090=FACE_OUTER_BOUND('',#1924,.T.);
#1091=FACE_OUTER_BOUND('',#1925,.T.);
#1092=FACE_OUTER_BOUND('',#1926,.T.);
#1093=FACE_OUTER_BOUND('',#1927,.T.);
#1094=FACE_OUTER_BOUND('',#1928,.T.);
#1095=FACE_OUTER_BOUND('',#1929,.T.);
#1096=FACE_OUTER_BOUND('',#1930,.T.);
#1097=FACE_OUTER_BOUND('',#1931,.T.);
#1098=FACE_OUTER_BOUND('',#1932,.T.);
#1099=FACE_OUTER_BOUND('',#1934,.T.);
#1100=FACE_OUTER_BOUND('',#1936,.T.);
#1101=FACE_OUTER_BOUND('',#1937,.T.);
#1102=FACE_OUTER_BOUND('',#1938,.T.);
#1103=FACE_OUTER_BOUND('',#1939,.T.);
#1104=FACE_OUTER_BOUND('',#1940,.T.);
#1105=FACE_OUTER_BOUND('',#1941,.T.);
#1106=FACE_OUTER_BOUND('',#1942,.T.);
#1107=FACE_OUTER_BOUND('',#1944,.T.);
#1108=FACE_OUTER_BOUND('',#1945,.T.);
#1109=FACE_OUTER_BOUND('',#1947,.T.);
#1851=EDGE_LOOP('',(#11789,#11790,#11791,#11792));
#1852=EDGE_LOOP('',(#11793,#11794,#11795,#11796));
#1853=EDGE_LOOP('',(#11797,#11798,#11799,#11800));
#1854=EDGE_LOOP('',(#11801,#11802,#11803,#11804));
#1855=EDGE_LOOP('',(#11805,#11806,#11807,#11808));
#1856=EDGE_LOOP('',(#11809,#11810,#11811,#11812));
#1857=EDGE_LOOP('',(#11813,#11814,#11815,#11816));
#1858=EDGE_LOOP('',(#11817,#11818,#11819,#11820));
#1859=EDGE_LOOP('',(#11821,#11822,#11823,#11824));
#1860=EDGE_LOOP('',(#11825,#11826,#11827,#11828));
#1861=EDGE_LOOP('',(#11829,#11830,#11831,#11832));
#1862=EDGE_LOOP('',(#11833,#11834,#11835,#11836));
#1863=EDGE_LOOP('',(#11837,#11838,#11839,#11840));
#1864=EDGE_LOOP('',(#11841,#11842,#11843,#11844));
#1865=EDGE_LOOP('',(#11845,#11846,#11847,#11848));
#1866=EDGE_LOOP('',(#11849,#11850,#11851,#11852));
#1867=EDGE_LOOP('',(#11853,#11854,#11855,#11856));
#1868=EDGE_LOOP('',(#11857,#11858,#11859,#11860));
#1869=EDGE_LOOP('',(#11861,#11862,#11863,#11864));
#1870=EDGE_LOOP('',(#11865,#11866,#11867,#11868));
#1871=EDGE_LOOP('',(#11869,#11870,#11871,#11872));
#1872=EDGE_LOOP('',(#11873,#11874,#11875,#11876));
#1873=EDGE_LOOP('',(#11877,#11878,#11879,#11880));
#1874=EDGE_LOOP('',(#11881,#11882,#11883,#11884));
#1875=EDGE_LOOP('',(#11885,#11886,#11887,#11888));
#1876=EDGE_LOOP('',(#11889,#11890,#11891,#11892));
#1877=EDGE_LOOP('',(#11893,#11894,#11895,#11896));
#1878=EDGE_LOOP('',(#11897,#11898,#11899,#11900));
#1879=EDGE_LOOP('',(#11901,#11902,#11903,#11904));
#1880=EDGE_LOOP('',(#11905,#11906,#11907,#11908));
#1881=EDGE_LOOP('',(#11909,#11910,#11911,#11912));
#1882=EDGE_LOOP('',(#11913,#11914,#11915,#11916));
#1883=EDGE_LOOP('',(#11917,#11918,#11919,#11920));
#1884=EDGE_LOOP('',(#11921,#11922,#11923,#11924));
#1885=EDGE_LOOP('',(#11925,#11926,#11927,#11928));
#1886=EDGE_LOOP('',(#11929,#11930,#11931,#11932));
#1887=EDGE_LOOP('',(#11933,#11934,#11935,#11936,#11937,#11938,#11939,#11940));
#1888=EDGE_LOOP('',(#11941,#11942,#11943,#11944));
#1889=EDGE_LOOP('',(#11945,#11946,#11947,#11948));
#1890=EDGE_LOOP('',(#11949,#11950,#11951,#11952));
#1891=EDGE_LOOP('',(#11953,#11954,#11955,#11956));
#1892=EDGE_LOOP('',(#11957,#11958,#11959,#11960));
#1893=EDGE_LOOP('',(#11961,#11962,#11963,#11964));
#1894=EDGE_LOOP('',(#11965,#11966,#11967,#11968));
#1895=EDGE_LOOP('',(#11969,#11970,#11971,#11972));
#1896=EDGE_LOOP('',(#11973,#11974,#11975,#11976));
#1897=EDGE_LOOP('',(#11977,#11978,#11979,#11980));
#1898=EDGE_LOOP('',(#11981,#11982,#11983,#11984));
#1899=EDGE_LOOP('',(#11985,#11986,#11987,#11988));
#1900=EDGE_LOOP('',(#11989,#11990,#11991,#11992));
#1901=EDGE_LOOP('',(#11993,#11994,#11995,#11996));
#1902=EDGE_LOOP('',(#11997,#11998,#11999,#12000));
#1903=EDGE_LOOP('',(#12001,#12002,#12003,#12004));
#1904=EDGE_LOOP('',(#12005,#12006,#12007,#12008));
#1905=EDGE_LOOP('',(#12009,#12010,#12011,#12012));
#1906=EDGE_LOOP('',(#12013,#12014,#12015,#12016));
#1907=EDGE_LOOP('',(#12017,#12018,#12019,#12020));
#1908=EDGE_LOOP('',(#12021,#12022,#12023,#12024));
#1909=EDGE_LOOP('',(#12025,#12026,#12027,#12028));
#1910=EDGE_LOOP('',(#12029,#12030,#12031,#12032));
#1911=EDGE_LOOP('',(#12033,#12034,#12035,#12036));
#1912=EDGE_LOOP('',(#12037,#12038,#12039,#12040));
#1913=EDGE_LOOP('',(#12041,#12042,#12043,#12044));
#1914=EDGE_LOOP('',(#12045,#12046,#12047,#12048));
#1915=EDGE_LOOP('',(#12049,#12050,#12051,#12052));
#1916=EDGE_LOOP('',(#12053,#12054,#12055,#12056));
#1917=EDGE_LOOP('',(#12057,#12058,#12059,#12060));
#1918=EDGE_LOOP('',(#12061,#12062,#12063,#12064));
#1919=EDGE_LOOP('',(#12065,#12066,#12067,#12068));
#1920=EDGE_LOOP('',(#12069,#12070,#12071,#12072));
#1921=EDGE_LOOP('',(#12073,#12074,#12075,#12076));
#1922=EDGE_LOOP('',(#12077,#12078,#12079,#12080));
#1923=EDGE_LOOP('',(#12081,#12082,#12083,#12084));
#1924=EDGE_LOOP('',(#12085,#12086,#12087,#12088));
#1925=EDGE_LOOP('',(#12089,#12090,#12091,#12092));
#1926=EDGE_LOOP('',(#12093,#12094,#12095,#12096));
#1927=EDGE_LOOP('',(#12097,#12098,#12099,#12100));
#1928=EDGE_LOOP('',(#12101,#12102,#12103,#12104));
#1929=EDGE_LOOP('',(#12105,#12106,#12107,#12108));
#1930=EDGE_LOOP('',(#12109,#12110,#12111,#12112,#12113,#12114));
#1931=EDGE_LOOP('',(#12115,#12116,#12117,#12118));
#1932=EDGE_LOOP('',(#12119));
#1933=EDGE_LOOP('',(#12120));
#1934=EDGE_LOOP('',(#12121));
#1935=EDGE_LOOP('',(#12122));
#1936=EDGE_LOOP('',(#12123,#12124,#12125,#12126));
#1937=EDGE_LOOP('',(#12127,#12128,#12129,#12130,#12131));
#1938=EDGE_LOOP('',(#12132,#12133,#12134,#12135,#12136,#12137,#12138,#12139,
#12140,#12141,#12142,#12143,#12144,#12145,#12146,#12147,#12148,#12149,#12150,
#12151,#12152,#12153,#12154,#12155,#12156,#12157,#12158,#12159,#12160,#12161,
#12162,#12163,#12164,#12165,#12166,#12167,#12168,#12169,#12170,#12171,#12172,
#12173,#12174,#12175,#12176,#12177,#12178,#12179,#12180,#12181,#12182,#12183,
#12184,#12185,#12186,#12187,#12188,#12189,#12190,#12191,#12192,#12193,#12194,
#12195,#12196,#12197,#12198,#12199,#12200,#12201,#12202,#12203,#12204,#12205,
#12206,#12207,#12208));
#1939=EDGE_LOOP('',(#12209,#12210,#12211,#12212));
#1940=EDGE_LOOP('',(#12213,#12214,#12215,#12216,#12217,#12218,#12219,#12220,
#12221,#12222,#12223,#12224,#12225,#12226,#12227,#12228,#12229,#12230,#12231,
#12232,#12233,#12234,#12235,#12236,#12237,#12238,#12239,#12240,#12241,#12242,
#12243,#12244,#12245,#12246,#12247,#12248,#12249,#12250,#12251,#12252,#12253,
#12254,#12255,#12256,#12257,#12258,#12259,#12260,#12261,#12262,#12263,#12264,
#12265,#12266,#12267,#12268,#12269,#12270,#12271,#12272,#12273,#12274,#12275,
#12276,#12277,#12278,#12279,#12280,#12281,#12282,#12283,#12284,#12285,#12286,
#12287,#12288,#12289));
#1941=EDGE_LOOP('',(#12290,#12291,#12292,#12293));
#1942=EDGE_LOOP('',(#12294));
#1943=EDGE_LOOP('',(#12295));
#1944=EDGE_LOOP('',(#12296,#12297,#12298,#12299));
#1945=EDGE_LOOP('',(#12300));
#1946=EDGE_LOOP('',(#12301,#12302,#12303,#12304,#12305,#12306));
#1947=EDGE_LOOP('',(#12307,#12308,#12309,#12310));
#2303=CIRCLE('',#15484,5.91675);
#2304=CIRCLE('',#15521,5.91675);
#2305=CIRCLE('',#15522,5.91675);
#2306=CIRCLE('',#15523,5.91675);
#2307=CIRCLE('',#15525,4.91825);
#2308=CIRCLE('',#15569,5.);
#2309=CIRCLE('',#15570,5.);
#2310=CIRCLE('',#15573,5.91675);
#2311=CIRCLE('',#15575,5.91675);
#2312=CIRCLE('',#15578,4.91825);
#2313=CIRCLE('',#15581,10.);
#2314=CIRCLE('',#15583,10.);
#3073=B_SPLINE_CURVE_WITH_KNOTS('',3,(#50430,#50431,#50432,#50433,#50434,
#50435,#50436,#50437,#50438,#50439,#50440,#50441,#50442,#50443,#50444,#50445),
 .UNSPECIFIED.,.F.,.F.,(4,3,3,3,3,4),(-4.09254174883831,-3.99749770433369,
-3.49781049129198,-2.99812327825027,-2.49843606520856,-2.06980418878614),
 .UNSPECIFIED.);
#3074=B_SPLINE_CURVE_WITH_KNOTS('',3,(#50448,#50449,#50450,#50451,#50452,
#50453,#50454,#50455,#50456,#50457),.UNSPECIFIED.,.F.,.F.,(4,3,3,4),(0.,
0.499687213041709,0.999374426083416,1.11885509353794),.UNSPECIFIED.);
#3075=B_SPLINE_CURVE_WITH_KNOTS('',3,(#50462,#50463,#50464,#50465,#50466,
#50467,#50468,#50469,#50470,#50471,#50472,#50473,#50474,#50475,#50476,#50477,
#50478,#50479,#50480,#50481,#50482,#50483,#50484,#50485,#50486,#50487,#50488,
#50489,#50490,#50491,#50492,#50493,#50494,#50495,#50496,#50497,#50498,#50499,
#50500,#50501),.UNSPECIFIED.,.F.,.F.,(4,3,3,3,3,3,3,3,3,3,3,3,3,4),(-10.3757270560179,
-9.99374426083422,-9.49405704779251,-8.9943698347508,-8.49468262170909,
-7.99499540866738,-7.49530819562566,-6.99562098258395,-6.49593376954224,
-5.99624655650053,-5.49655934345882,-4.99687213041711,-4.4971849173754,
-4.09254174883831),.UNSPECIFIED.);
#3076=B_SPLINE_CURVE_WITH_KNOTS('',3,(#50502,#50503,#50504,#50505,#50506,
#50507,#50508,#50509,#50510,#50511,#50512,#50513,#50514,#50515,#50516,#50517,
#50518,#50519,#50520,#50521,#50522,#50523,#50524,#50525,#50526,#50527,#50528,
#50529,#50530,#50531,#50532,#50533,#50534,#50535,#50536,#50537,#50538,#50539,
#50540,#50541),.UNSPECIFIED.,.F.,.F.,(4,3,3,3,3,3,3,3,3,3,3,3,3,4),(1.11885509353794,
1.49906163912513,1.99874885216684,2.49843606520855,2.99812327825026,3.49781049129198,
3.99749770433369,4.4971849173754,4.99687213041711,5.49655934345882,5.99624655650054,
6.49593376954225,6.99562098258396,7.40204040071752),.UNSPECIFIED.);
#3077=B_SPLINE_CURVE_WITH_KNOTS('',3,(#50546,#50547,#50548,#50549,#50550,
#50551,#50552,#50553,#50554,#50555,#50556,#50557,#50558,#50559,#50560,#50561,
#50562,#50563,#50564,#50565,#50566,#50567,#50568,#50569,#50570,#50571,#50572,
#50573,#50574,#50575,#50576,#50577,#50578,#50579,#50580,#50581,#50582,#50583,
#50584,#50585,#50586,#50587,#50588),.UNSPECIFIED.,.F.,.F.,(4,3,3,3,3,3,
3,3,3,3,3,3,3,3,4),(-16.6589123631975,-16.4896780303765,-15.9899908173347,
-15.490303604293,-14.9906163912513,-14.4909291782096,-13.9912419651679,
-13.4915547521262,-12.9918675390845,-12.4921803260428,-11.9924931130011,
-11.4928058999594,-10.9931186869176,-10.4934314738759,-10.3757270560179),
 .UNSPECIFIED.);
#3078=B_SPLINE_CURVE_WITH_KNOTS('',3,(#50589,#50590,#50591,#50592,#50593,
#50594,#50595,#50596,#50597,#50598,#50599,#50600,#50601,#50602,#50603,#50604,
#50605,#50606,#50607,#50608,#50609,#50610,#50611,#50612,#50613,#50614,#50615,
#50616,#50617,#50618,#50619,#50620,#50621,#50622,#50623,#50624,#50625,#50626,
#50627,#50628,#50629,#50630,#50631),.UNSPECIFIED.,.F.,.F.,(4,3,3,3,3,3,
3,3,3,3,3,3,3,3,4),(7.40204040071752,7.49530819562567,7.99499540866738,
8.49468262170909,8.99436983475081,9.49405704779253,9.99374426083424,10.4934314738759,
10.9931186869177,11.4928058999594,11.9924931130011,12.4921803260428,12.9918675390845,
13.4915547521262,13.6852257078971),.UNSPECIFIED.);
#3079=B_SPLINE_CURVE_WITH_KNOTS('',3,(#50636,#50637,#50638,#50639,#50640,
#50641,#50642,#50643,#50644,#50645,#50646,#50647,#50648,#50649,#50650,#50651,
#50652,#50653,#50654,#50655,#50656,#50657,#50658,#50659,#50660,#50661,#50662,
#50663,#50664,#50665,#50666,#50667,#50668,#50669,#50670,#50671,#50672,#50673,
#50674,#50675),.UNSPECIFIED.,.F.,.F.,(4,3,3,3,3,3,3,3,3,3,3,3,3,4),(-22.9420976703771,
-22.485924586877,-21.9862373738353,-21.4865501607936,-20.9868629477519,
-20.4871757347102,-19.9874885216684,-19.4878013086267,-18.988114095585,
-18.4884268825433,-17.9887396695016,-17.4890524564599,-16.9893652434182,
-16.6589123631975),.UNSPECIFIED.);
#3080=B_SPLINE_CURVE_WITH_KNOTS('',3,(#50676,#50677,#50678,#50679,#50680,
#50681,#50682,#50683,#50684,#50685,#50686,#50687,#50688,#50689,#50690,#50691,
#50692,#50693,#50694,#50695,#50696,#50697,#50698,#50699,#50700,#50701,#50702,
#50703,#50704,#50705,#50706,#50707,#50708,#50709,#50710,#50711,#50712,#50713,
#50714,#50715),.UNSPECIFIED.,.F.,.F.,(4,3,3,3,3,3,3,3,3,3,3,3,3,4),(13.6852257078971,
13.9912419651679,14.4909291782096,14.9906163912513,15.4903036042931,15.9899908173348,
16.4896780303765,16.9893652434182,17.4890524564599,17.9887396695016,18.4884268825433,
18.988114095585,19.4878013086267,19.9684110150767),.UNSPECIFIED.);
#3081=B_SPLINE_CURVE_WITH_KNOTS('',3,(#50720,#50721,#50722,#50723,#50724,
#50725,#50726,#50727,#50728,#50729,#50730,#50731,#50732,#50733,#50734,#50735,
#50736,#50737,#50738,#50739,#50740,#50741,#50742,#50743,#50744,#50745,#50746,
#50747,#50748,#50749,#50750,#50751,#50752,#50753,#50754,#50755,#50756,#50757,
#50758,#50759,#50760,#50761,#50762),.UNSPECIFIED.,.F.,.F.,(4,3,3,3,3,3,
3,3,3,3,3,3,3,3,4),(-29.2252829775567,-28.9818583564192,-28.4821711433775,
-27.9824839303358,-27.4827967172941,-26.9831095042524,-26.4834222912107,
-25.983735078169,-25.4840478651273,-24.9843606520855,-24.4846734390438,
-23.9849862260021,-23.4852990129604,-22.9856117999187,-22.9420976703771),
 .UNSPECIFIED.);
#3082=B_SPLINE_CURVE_WITH_KNOTS('',3,(#50763,#50764,#50765,#50766,#50767,
#50768,#50769,#50770,#50771,#50772,#50773,#50774,#50775,#50776,#50777,#50778,
#50779,#50780,#50781,#50782,#50783,#50784,#50785,#50786,#50787,#50788,#50789,
#50790,#50791,#50792,#50793,#50794,#50795,#50796,#50797,#50798,#50799,#50800,
#50801,#50802,#50803,#50804,#50805),.UNSPECIFIED.,.F.,.F.,(4,3,3,3,3,3,
3,3,3,3,3,3,3,3,4),(19.9684110150767,19.9874885216684,20.4871757347102,
20.9868629477519,21.4865501607936,21.9862373738353,22.485924586877,22.9856117999187,
23.4852990129604,23.9849862260021,24.4846734390438,24.9843606520855,25.4840478651272,
25.983735078169,26.2515963222563),.UNSPECIFIED.);
#3083=B_SPLINE_CURVE_WITH_KNOTS('',3,(#50810,#50811,#50812,#50813,#50814,
#50815,#50816,#50817,#50818,#50819,#50820,#50821,#50822,#50823,#50824,#50825,
#50826,#50827,#50828,#50829,#50830,#50831,#50832,#50833,#50834,#50835,#50836,
#50837,#50838,#50839,#50840,#50841,#50842,#50843,#50844,#50845,#50846,#50847,
#50848,#50849,#50850,#50851,#50852),.UNSPECIFIED.,.F.,.F.,(4,3,3,3,3,3,
3,3,3,3,3,3,3,3,4),(-35.5084682847362,-35.4777921259615,-34.9781049129198,
-34.4784176998781,-33.9787304868363,-33.4790432737946,-32.9793560607529,
-32.4796688477112,-31.9799816346695,-31.4802944216278,-30.9806072085861,
-30.4809199955444,-29.9812327825027,-29.4815455694609,-29.2252829775567),
 .UNSPECIFIED.);
#3084=B_SPLINE_CURVE_WITH_KNOTS('',3,(#50853,#50854,#50855,#50856,#50857,
#50858,#50859,#50860,#50861,#50862,#50863,#50864,#50865,#50866,#50867,#50868,
#50869,#50870,#50871,#50872,#50873,#50874,#50875,#50876,#50877,#50878,#50879,
#50880,#50881,#50882,#50883,#50884,#50885,#50886,#50887,#50888,#50889,#50890,
#50891,#50892,#50893,#50894,#50895),.UNSPECIFIED.,.F.,.F.,(4,3,3,3,3,3,
3,3,3,3,3,3,3,3,4),(26.2515963222563,26.4834222912107,26.9831095042524,
27.4827967172941,27.9824839303358,28.4821711433775,28.9818583564192,29.481545569461,
29.9812327825027,30.4809199955444,30.9806072085861,31.4802944216278,31.9799816346695,
32.4796688477112,32.5347816294359),.UNSPECIFIED.);
#3085=B_SPLINE_CURVE_WITH_KNOTS('',3,(#50900,#50901,#50902,#50903,#50904,
#50905,#50906,#50907,#50908,#50909,#50910,#50911,#50912,#50913,#50914,#50915,
#50916,#50917,#50918,#50919,#50920,#50921,#50922,#50923,#50924,#50925,#50926,
#50927,#50928,#50929,#50930,#50931,#50932,#50933,#50934,#50935,#50936,#50937,
#50938,#50939),.UNSPECIFIED.,.F.,.F.,(4,3,3,3,3,3,3,3,3,3,3,3,3,4),(-41.7916535919158,
-41.474038682462,-40.9743514694203,-40.4746642563786,-39.9749770433369,
-39.4752898302952,-38.9756026172535,-38.4759154042117,-37.97622819117,-37.4765409781283,
-36.9768537650866,-36.4771665520449,-35.9774793390032,-35.5084682847362),
 .UNSPECIFIED.);
#3086=B_SPLINE_CURVE_WITH_KNOTS('',3,(#50940,#50941,#50942,#50943,#50944,
#50945,#50946,#50947,#50948,#50949,#50950,#50951,#50952,#50953,#50954,#50955,
#50956,#50957,#50958,#50959,#50960,#50961,#50962,#50963,#50964,#50965,#50966,
#50967,#50968,#50969,#50970,#50971,#50972,#50973,#50974,#50975,#50976,#50977,
#50978,#50979),.UNSPECIFIED.,.F.,.F.,(4,3,3,3,3,3,3,3,3,3,3,3,3,4),(32.5347816294359,
32.9793560607529,33.4790432737947,33.9787304868364,34.4784176998781,34.9781049129198,
35.4777921259615,35.9774793390032,36.4771665520449,36.9768537650866,37.4765409781283,
37.97622819117,38.4759154042117,38.8179669366154),.UNSPECIFIED.);
#3087=B_SPLINE_CURVE_WITH_KNOTS('',3,(#50984,#50985,#50986,#50987,#50988,
#50989,#50990,#50991,#50992,#50993,#50994,#50995,#50996,#50997,#50998,#50999,
#51000,#51001,#51002,#51003,#51004,#51005,#51006,#51007,#51008,#51009,#51010,
#51011,#51012,#51013,#51014,#51015,#51016,#51017,#51018,#51019,#51020,#51021,
#51022,#51023,#51024,#51025,#51026),.UNSPECIFIED.,.F.,.F.,(4,3,3,3,3,3,
3,3,3,3,3,3,3,3,4),(-48.0748388990954,-47.9699724520042,-47.4702852389625,
-46.9705980259208,-46.4709108128791,-45.9712235998374,-45.4715363867957,
-44.971849173754,-44.4721619607123,-43.9724747476706,-43.4727875346288,
-42.9731003215871,-42.4734131085454,-41.9737258955037,-41.7916535919158),
 .UNSPECIFIED.);
#3088=B_SPLINE_CURVE_WITH_KNOTS('',3,(#51027,#51028,#51029,#51030,#51031,
#51032,#51033,#51034,#51035,#51036,#51037,#51038,#51039,#51040,#51041,#51042,
#51043,#51044,#51045,#51046,#51047,#51048,#51049,#51050,#51051,#51052,#51053,
#51054,#51055,#51056,#51057,#51058,#51059,#51060,#51061,#51062,#51063,#51064,
#51065,#51066,#51067,#51068,#51069),.UNSPECIFIED.,.F.,.F.,(4,3,3,3,3,3,
3,3,3,3,3,3,3,3,4),(38.8179669366154,38.9756026172534,39.4752898302952,
39.9749770433369,40.4746642563786,40.9743514694203,41.474038682462,41.9737258955037,
42.4734131085454,42.9731003215871,43.4727875346289,43.9724747476706,44.4721619607123,
44.971849173754,45.101152243795),.UNSPECIFIED.);
#3089=B_SPLINE_CURVE_WITH_KNOTS('',3,(#51074,#51075,#51076,#51077,#51078,
#51079,#51080,#51081,#51082,#51083,#51084,#51085,#51086,#51087,#51088,#51089,
#51090,#51091,#51092,#51093,#51094,#51095,#51096,#51097,#51098,#51099,#51100,
#51101,#51102,#51103,#51104,#51105,#51106,#51107,#51108,#51109,#51110,#51111,
#51112,#51113),.UNSPECIFIED.,.F.,.F.,(4,3,3,3,3,3,3,3,3,3,3,3,3,4),(-54.358024206275,
-53.9662190085048,-53.4665317954631,-52.9668445824214,-52.4671573693797,
-51.9674701563379,-51.4677829432962,-50.9680957302545,-50.4684085172128,
-49.9687213041711,-49.4690340911294,-48.9693468780877,-48.469659665046,
-48.0748388990954),.UNSPECIFIED.);
#3090=B_SPLINE_CURVE_WITH_KNOTS('',3,(#51114,#51115,#51116,#51117,#51118,
#51119,#51120,#51121,#51122,#51123,#51124,#51125,#51126,#51127,#51128,#51129,
#51130,#51131,#51132,#51133,#51134,#51135,#51136,#51137,#51138,#51139,#51140,
#51141,#51142,#51143,#51144,#51145,#51146,#51147,#51148,#51149,#51150,#51151,
#51152,#51153),.UNSPECIFIED.,.F.,.F.,(4,3,3,3,3,3,3,3,3,3,3,3,3,4),(45.101152243795,
45.4715363867957,45.9712235998374,46.4709108128791,46.9705980259208,47.4702852389625,
47.9699724520043,48.469659665046,48.9693468780877,49.4690340911294,49.9687213041711,
50.4684085172128,50.9680957302545,51.3843375509746),.UNSPECIFIED.);
#3091=B_SPLINE_CURVE_WITH_KNOTS('',3,(#51158,#51159,#51160,#51161,#51162,
#51163,#51164,#51165,#51166,#51167,#51168,#51169,#51170,#51171,#51172,#51173,
#51174,#51175,#51176,#51177,#51178,#51179,#51180,#51181,#51182,#51183,#51184,
#51185,#51186,#51187,#51188,#51189,#51190,#51191,#51192,#51193,#51194,#51195,
#51196,#51197,#51198,#51199,#51200),.UNSPECIFIED.,.F.,.F.,(4,3,3,3,3,3,
3,3,3,3,3,3,3,3,4),(-60.6412095134546,-60.462152778047,-59.9624655650053,
-59.4627783519636,-58.9630911389219,-58.4634039258802,-57.9637167128385,
-57.4640294997968,-56.964342286755,-56.4646550737133,-55.9649678606716,
-55.4652806476299,-54.9655934345882,-54.4659062215465,-54.358024206275),
 .UNSPECIFIED.);
#3092=B_SPLINE_CURVE_WITH_KNOTS('',3,(#51201,#51202,#51203,#51204,#51205,
#51206,#51207,#51208,#51209,#51210,#51211,#51212,#51213,#51214,#51215,#51216,
#51217,#51218,#51219,#51220,#51221,#51222,#51223,#51224,#51225,#51226,#51227,
#51228,#51229,#51230,#51231,#51232,#51233,#51234,#51235,#51236,#51237,#51238,
#51239,#51240,#51241,#51242,#51243),.UNSPECIFIED.,.F.,.F.,(4,3,3,3,3,3,
3,3,3,3,3,3,3,3,4),(51.3843375509746,51.4677829432962,51.967470156338,52.4671573693797,
52.9668445824214,53.4665317954631,53.9662190085048,54.4659062215465,54.9655934345882,
55.4652806476299,55.9649678606716,56.4646550737133,56.964342286755,57.4640294997968,
57.6675228581542),.UNSPECIFIED.);
#3093=B_SPLINE_CURVE_WITH_KNOTS('',3,(#51248,#51249,#51250,#51251,#51252,
#51253,#51254,#51255,#51256,#51257,#51258,#51259,#51260,#51261,#51262,#51263,
#51264,#51265,#51266,#51267,#51268,#51269,#51270,#51271,#51272,#51273,#51274,
#51275,#51276,#51277,#51278,#51279,#51280,#51281,#51282,#51283,#51284,#51285,
#51286,#51287),.UNSPECIFIED.,.F.,.F.,(4,3,3,3,3,3,3,3,3,3,3,3,3,4),(-66.9243948206342,
-66.4583993345476,-65.9587121215058,-65.4590249084641,-64.9593376954224,
-64.4596504823807,-63.959963269339,-63.4602760562973,-62.9605888432556,
-62.4609016302139,-61.9612144171722,-61.4615272041304,-60.9618399910887,
-60.6412095134546),.UNSPECIFIED.);
#3094=B_SPLINE_CURVE_WITH_KNOTS('',3,(#51288,#51289,#51290,#51291,#51292,
#51293,#51294,#51295,#51296,#51297,#51298,#51299,#51300,#51301,#51302,#51303,
#51304,#51305,#51306,#51307,#51308,#51309,#51310,#51311,#51312,#51313,#51314,
#51315,#51316,#51317,#51318,#51319,#51320,#51321,#51322,#51323,#51324,#51325,
#51326,#51327),.UNSPECIFIED.,.F.,.F.,(4,3,3,3,3,3,3,3,3,3,3,3,3,4),(57.6675228581542,
57.9637167128385,58.4634039258802,58.9630911389219,59.4627783519636,59.9624655650053,
60.462152778047,60.9618399910887,61.4615272041304,61.9612144171722,62.4609016302139,
62.9605888432556,63.4602760562973,63.9507081653338),.UNSPECIFIED.);
#3095=B_SPLINE_CURVE_WITH_KNOTS('',3,(#51332,#51333,#51334,#51335,#51336,
#51337,#51338,#51339,#51340,#51341,#51342,#51343,#51344,#51345,#51346,#51347,
#51348,#51349,#51350,#51351,#51352,#51353,#51354,#51355,#51356,#51357,#51358,
#51359,#51360,#51361,#51362,#51363,#51364,#51365,#51366,#51367,#51368,#51369,
#51370,#51371,#51372,#51373,#51374),.UNSPECIFIED.,.F.,.F.,(4,3,3,3,3,3,
3,3,3,3,3,3,3,3,4),(-73.2075801278138,-72.9543331040898,-72.4546458910481,
-71.9549586780064,-71.4552714649647,-70.9555842519229,-70.4558970388812,
-69.9562098258395,-69.4565226127978,-68.9568353997561,-68.4571481867144,
-67.9574609736727,-67.457773760631,-66.9580865475893,-66.9243948206342),
 .UNSPECIFIED.);
#3096=B_SPLINE_CURVE_WITH_KNOTS('',3,(#51375,#51376,#51377,#51378,#51379,
#51380,#51381,#51382,#51383,#51384,#51385,#51386,#51387,#51388,#51389,#51390,
#51391,#51392,#51393,#51394,#51395,#51396,#51397,#51398,#51399,#51400,#51401,
#51402,#51403,#51404,#51405,#51406,#51407,#51408,#51409,#51410,#51411,#51412,
#51413,#51414,#51415,#51416,#51417),.UNSPECIFIED.,.F.,.F.,(4,3,3,3,3,3,
3,3,3,3,3,3,3,3,4),(63.9507081653338,63.959963269339,64.4596504823807,64.9593376954224,
65.4590249084641,65.9587121215058,66.4583993345476,66.9580865475893,67.457773760631,
67.9574609736727,68.4571481867144,68.9568353997561,69.4565226127979,69.9562098258396,
70.2338934725134),.UNSPECIFIED.);
#3097=B_SPLINE_CURVE_WITH_KNOTS('',3,(#51422,#51423,#51424,#51425,#51426,
#51427,#51428,#51429,#51430,#51431,#51432,#51433,#51434,#51435,#51436,#51437,
#51438,#51439,#51440,#51441,#51442,#51443,#51444,#51445,#51446,#51447,#51448,
#51449,#51450,#51451,#51452,#51453,#51454,#51455,#51456,#51457,#51458,#51459,
#51460,#51461,#51462,#51463,#51464),.UNSPECIFIED.,.F.,.F.,(4,3,3,3,3,3,
3,3,3,3,3,3,3,3,4),(-79.4907654349934,-79.450266873632,-78.9505796605903,
-78.4508924475486,-77.9512052345069,-77.4515180214652,-76.9518308084235,
-76.4521435953818,-75.9524563823401,-75.4527691692983,-74.9530819562566,
-74.4533947432149,-73.9537075301732,-73.4540203171315,-73.2075801278138),
 .UNSPECIFIED.);
#3098=B_SPLINE_CURVE_WITH_KNOTS('',3,(#51465,#51466,#51467,#51468,#51469,
#51470,#51471,#51472,#51473,#51474,#51475,#51476,#51477,#51478,#51479,#51480,
#51481,#51482,#51483,#51484,#51485,#51486,#51487,#51488,#51489,#51490,#51491,
#51492,#51493,#51494,#51495,#51496,#51497,#51498,#51499,#51500,#51501,#51502,
#51503,#51504,#51505,#51506,#51507),.UNSPECIFIED.,.F.,.F.,(4,3,3,3,3,3,
3,3,3,3,3,3,3,3,4),(70.2338934725134,70.4558970388813,70.955584251923,71.4552714649647,
71.9549586780064,72.4546458910481,72.9543331040898,73.4540203171315,73.9537075301732,
74.4533947432149,74.9530819562566,75.4527691692983,75.95245638234,76.4521435953817,
76.517078779693),.UNSPECIFIED.);
#3099=B_SPLINE_CURVE_WITH_KNOTS('',3,(#51512,#51513,#51514,#51515,#51516,
#51517,#51518,#51519,#51520,#51521,#51522,#51523,#51524,#51525,#51526,#51527,
#51528,#51529,#51530,#51531,#51532,#51533,#51534,#51535,#51536,#51537,#51538,
#51539,#51540,#51541,#51542,#51543,#51544,#51545,#51546,#51547,#51548,#51549,
#51550,#51551),.UNSPECIFIED.,.F.,.F.,(4,3,3,3,3,3,3,3,3,3,3,3,3,4),(-85.773950742173,
-85.4465134301326,-84.9468262170908,-84.4471390040491,-83.9474517910074,
-83.4477645779657,-82.948077364924,-82.4483901518823,-81.9487029388406,
-81.4490157257989,-80.9493285127572,-80.4496412997155,-79.9499540866738,
-79.4907654349934),.UNSPECIFIED.);
#3100=B_SPLINE_CURVE_WITH_KNOTS('',3,(#51552,#51553,#51554,#51555,#51556,
#51557,#51558,#51559,#51560,#51561,#51562,#51563,#51564,#51565,#51566,#51567,
#51568,#51569,#51570,#51571,#51572,#51573,#51574,#51575,#51576,#51577,#51578,
#51579,#51580,#51581,#51582,#51583,#51584,#51585,#51586,#51587,#51588,#51589,
#51590,#51591),.UNSPECIFIED.,.F.,.F.,(4,3,3,3,3,3,3,3,3,3,3,3,3,4),(76.517078779693,
76.9518308084235,77.4515180214652,77.9512052345069,78.4508924475486,78.9505796605903,
79.450266873632,79.9499540866737,80.4496412997155,80.9493285127572,81.4490157257989,
81.9487029388406,82.4483901518823,82.8002640868726),.UNSPECIFIED.);
#3101=B_SPLINE_CURVE_WITH_KNOTS('',3,(#51596,#51597,#51598,#51599,#51600,
#51601,#51602,#51603,#51604,#51605,#51606,#51607,#51608,#51609,#51610,#51611,
#51612,#51613,#51614,#51615,#51616,#51617,#51618,#51619,#51620,#51621,#51622,
#51623,#51624,#51625,#51626,#51627,#51628,#51629,#51630,#51631,#51632,#51633,
#51634,#51635,#51636,#51637,#51638),.UNSPECIFIED.,.F.,.F.,(4,3,3,3,3,3,
3,3,3,3,3,3,3,3,4),(-92.0571360493526,-91.9424471996748,-91.4427599866331,
-90.9430727735914,-90.4433855605497,-89.943698347508,-89.4440111344663,
-88.9443239214246,-88.4446367083828,-87.9449494953411,-87.4452622822994,
-86.9455750692577,-86.445887856216,-85.9462006431743,-85.773950742173),
 .UNSPECIFIED.);
#3102=B_SPLINE_CURVE_WITH_KNOTS('',3,(#51639,#51640,#51641,#51642,#51643,
#51644,#51645,#51646,#51647,#51648,#51649,#51650,#51651,#51652,#51653,#51654,
#51655,#51656,#51657,#51658,#51659,#51660,#51661,#51662,#51663,#51664,#51665,
#51666,#51667,#51668,#51669,#51670,#51671,#51672,#51673,#51674,#51675,#51676,
#51677,#51678,#51679,#51680,#51681),.UNSPECIFIED.,.F.,.F.,(4,3,3,3,3,3,
3,3,3,3,3,3,3,3,4),(82.8002640868726,82.948077364924,83.4477645779658,83.9474517910075,
84.4471390040491,84.9468262170909,85.4465134301326,85.9462006431743,86.445887856216,
86.9455750692577,87.4452622822994,87.9449494953411,88.4446367083828,88.9443239214245,
89.0834493940522),.UNSPECIFIED.);
#3103=B_SPLINE_CURVE_WITH_KNOTS('',3,(#51686,#51687,#51688,#51689,#51690,
#51691,#51692,#51693,#51694,#51695,#51696,#51697,#51698,#51699,#51700,#51701,
#51702,#51703,#51704,#51705,#51706,#51707,#51708,#51709,#51710,#51711,#51712,
#51713,#51714,#51715,#51716,#51717,#51718,#51719,#51720,#51721,#51722,#51723,
#51724,#51725),.UNSPECIFIED.,.F.,.F.,(4,3,3,3,3,3,3,3,3,3,3,3,3,4),(-98.3403213565322,
-97.9386937561753,-97.4390065431336,-96.9393193300919,-96.4396321170502,
-95.9399449040085,-95.4402576909668,-94.940570477925,-94.4408832648834,
-93.9411960518416,-93.4415088387999,-92.9418216257582,-92.4421344127165,
-92.0571360493526),.UNSPECIFIED.);
#3104=B_SPLINE_CURVE_WITH_KNOTS('',3,(#51726,#51727,#51728,#51729,#51730,
#51731,#51732,#51733,#51734,#51735,#51736,#51737,#51738,#51739,#51740,#51741,
#51742,#51743,#51744,#51745,#51746,#51747,#51748,#51749,#51750,#51751,#51752,
#51753,#51754,#51755,#51756,#51757,#51758,#51759,#51760,#51761,#51762,#51763,
#51764,#51765),.UNSPECIFIED.,.F.,.F.,(4,3,3,3,3,3,3,3,3,3,3,3,3,4),(89.0834493940522,
89.4440111344662,89.943698347508,90.4433855605497,90.9430727735914,91.4427599866331,
91.9424471996748,92.4421344127165,92.9418216257583,93.4415088388,93.9411960518417,
94.4408832648834,94.9405704779251,95.3666347012318),.UNSPECIFIED.);
#3105=B_SPLINE_CURVE_WITH_KNOTS('',3,(#51770,#51771,#51772,#51773,#51774,
#51775,#51776,#51777,#51778,#51779,#51780,#51781,#51782,#51783,#51784,#51785,
#51786,#51787,#51788,#51789,#51790,#51791,#51792,#51793,#51794,#51795,#51796,
#51797,#51798,#51799,#51800,#51801,#51802,#51803,#51804,#51805,#51806,#51807,
#51808,#51809,#51810,#51811,#51812),.UNSPECIFIED.,.F.,.F.,(4,3,3,3,3,3,
3,3,3,3,3,3,3,3,4),(-104.623506663712,-104.434627525718,-103.934940312676,
-103.435253099634,-102.935565886592,-102.435878673551,-101.936191460509,
-101.436504247467,-100.936817034426,-100.437129821384,-99.9374426083422,
-99.4377553953005,-98.9380681822588,-98.4383809692171,-98.3403213565322),
 .UNSPECIFIED.);
#3106=B_SPLINE_CURVE_WITH_KNOTS('',3,(#51813,#51814,#51815,#51816,#51817,
#51818,#51819,#51820,#51821,#51822,#51823,#51824,#51825,#51826,#51827,#51828,
#51829,#51830,#51831,#51832,#51833,#51834,#51835,#51836,#51837,#51838,#51839,
#51840,#51841,#51842,#51843,#51844,#51845,#51846,#51847,#51848,#51849,#51850,
#51851,#51852,#51853,#51854,#51855),.UNSPECIFIED.,.F.,.F.,(4,3,3,3,3,3,
3,3,3,3,3,3,3,3,4),(95.3666347012318,95.4402576909668,95.9399449040085,
96.4396321170502,96.9393193300919,97.4390065431336,97.9386937561753,98.438380969217,
98.9380681822587,99.4377553953005,99.9374426083422,100.437129821384,100.936817034426,
101.436504247467,101.649820008411),.UNSPECIFIED.);
#3107=B_SPLINE_CURVE_WITH_KNOTS('',3,(#51860,#51861,#51862,#51863,#51864,
#51865,#51866,#51867,#51868,#51869,#51870,#51871,#51872,#51873,#51874,#51875,
#51876,#51877,#51878,#51879,#51880,#51881,#51882,#51883,#51884,#51885,#51886,
#51887,#51888,#51889,#51890,#51891,#51892,#51893,#51894,#51895,#51896,#51897,
#51898,#51899),.UNSPECIFIED.,.F.,.F.,(4,3,3,3,3,3,3,3,3,3,3,3,3,4),(-110.906691970891,
-110.430874082218,-109.931186869176,-109.431499656135,-108.931812443093,
-108.432125230051,-107.93243801701,-107.432750803968,-106.933063590926,
-106.433376377884,-105.933689164843,-105.434001951801,-104.934314738759,
-104.623506663712),.UNSPECIFIED.);
#3108=B_SPLINE_CURVE_WITH_KNOTS('',3,(#51900,#51901,#51902,#51903,#51904,
#51905,#51906,#51907,#51908,#51909,#51910,#51911,#51912,#51913,#51914,#51915,
#51916,#51917,#51918,#51919,#51920,#51921,#51922,#51923,#51924,#51925,#51926,
#51927,#51928,#51929,#51930,#51931,#51932,#51933,#51934,#51935,#51936,#51937,
#51938,#51939),.UNSPECIFIED.,.F.,.F.,(4,3,3,3,3,3,3,3,3,3,3,3,3,4),(101.649820008411,
101.936191460509,102.435878673551,102.935565886592,103.435253099634,103.934940312676,
104.434627525718,104.934314738759,105.434001951801,105.933689164843,106.433376377884,
106.933063590926,107.432750803968,107.933005315591),.UNSPECIFIED.);
#3109=B_SPLINE_CURVE_WITH_KNOTS('',3,(#51944,#51945,#51946,#51947,#51948,
#51949,#51950,#51951,#51952,#51953,#51954,#51955,#51956,#51957,#51958,#51959,
#51960,#51961,#51962,#51963,#51964,#51965,#51966,#51967,#51968,#51969,#51970,
#51971,#51972,#51973,#51974,#51975,#51976,#51977,#51978,#51979,#51980,#51981,
#51982,#51983,#51984,#51985,#51986),.UNSPECIFIED.,.F.,.F.,(4,3,3,3,3,3,
3,3,3,3,3,3,3,3,4),(-117.189877278071,-116.92680785176,-116.427120638719,
-115.927433425677,-115.427746212635,-114.928058999594,-114.428371786552,
-113.92868457351,-113.428997360468,-112.929310147427,-112.429622934385,
-111.929935721343,-111.430248508302,-110.93056129526,-110.906691970891),
 .UNSPECIFIED.);
#3110=B_SPLINE_CURVE_WITH_KNOTS('',3,(#51987,#51988,#51989,#51990,#51991,
#51992,#51993,#51994,#51995,#51996,#51997,#51998,#51999,#52000,#52001,#52002,
#52003,#52004,#52005,#52006,#52007,#52008,#52009,#52010,#52011,#52012,#52013,
#52014,#52015,#52016,#52017,#52018,#52019,#52020,#52021,#52022,#52023,#52024,
#52025,#52026),.UNSPECIFIED.,.F.,.F.,(4,3,3,3,3,3,3,3,3,3,3,3,3,4),(107.933005315591,
108.432125230051,108.931812443093,109.431499656135,109.931186869176,110.430874082218,
110.93056129526,111.430248508302,111.929935721343,112.429622934385,112.929310147427,
113.428997360468,113.92868457351,114.216190622771),.UNSPECIFIED.);
#3111=B_SPLINE_CURVE_WITH_KNOTS('',3,(#52031,#52032,#52033,#52034,#52035,
#52036,#52037,#52038,#52039,#52040,#52041,#52042,#52043,#52044,#52045,#52046,
#52047,#52048,#52049,#52050,#52051,#52052,#52053,#52054,#52055,#52056,#52057,
#52058,#52059,#52060,#52061,#52062,#52063,#52064,#52065,#52066,#52067,#52068,
#52069,#52070,#52071,#52072,#52073),.UNSPECIFIED.,.F.,.F.,(4,3,3,3,3,3,
3,3,3,3,3,3,3,3,4),(-123.473062585251,-123.422741621303,-122.923054408261,
-122.423367195219,-121.923679982177,-121.423992769136,-120.924305556094,
-120.424618343052,-119.924931130011,-119.425243916969,-118.925556703927,
-118.425869490885,-117.926182277844,-117.426495064802,-117.189877278071),
 .UNSPECIFIED.);
#3112=B_SPLINE_CURVE_WITH_KNOTS('',3,(#52074,#52075,#52076,#52077,#52078,
#52079,#52080,#52081,#52082,#52083,#52084,#52085,#52086,#52087,#52088,#52089,
#52090,#52091,#52092,#52093,#52094,#52095,#52096,#52097,#52098,#52099,#52100,
#52101,#52102,#52103,#52104,#52105,#52106,#52107,#52108,#52109,#52110,#52111,
#52112,#52113,#52114,#52115,#52116),.UNSPECIFIED.,.F.,.F.,(4,3,3,3,3,3,
3,3,3,3,3,3,3,3,4),(114.216190622771,114.428371786552,114.928058999594,
115.427746212635,115.927433425677,116.427120638719,116.92680785176,117.426495064802,
117.926182277844,118.425869490886,118.925556703927,119.425243916969,119.924931130011,
120.424618343052,120.49937592995),.UNSPECIFIED.);
#3113=B_SPLINE_CURVE_WITH_KNOTS('',3,(#52121,#52122,#52123,#52124,#52125,
#52126,#52127,#52128,#52129,#52130,#52131,#52132,#52133,#52134,#52135,#52136,
#52137,#52138,#52139,#52140,#52141,#52142,#52143,#52144,#52145,#52146,#52147,
#52148,#52149,#52150,#52151,#52152,#52153,#52154,#52155,#52156,#52157,#52158,
#52159,#52160),.UNSPECIFIED.,.F.,.F.,(4,3,3,3,3,3,3,3,3,3,3,3,3,4),(-129.75624789243,
-129.418988177803,-128.919300964761,-128.41961375172,-127.919926538678,
-127.420239325636,-126.920552112595,-126.420864899553,-125.921177686511,
-125.421490473469,-124.921803260428,-124.422116047386,-123.922428834344,
-123.473062585251),.UNSPECIFIED.);
#3114=B_SPLINE_CURVE_WITH_KNOTS('',3,(#52161,#52162,#52163,#52164,#52165,
#52166,#52167,#52168,#52169,#52170,#52171,#52172,#52173,#52174,#52175,#52176,
#52177,#52178,#52179,#52180,#52181,#52182,#52183,#52184,#52185,#52186,#52187,
#52188,#52189,#52190,#52191,#52192,#52193,#52194,#52195,#52196,#52197,#52198,
#52199,#52200),.UNSPECIFIED.,.F.,.F.,(4,3,3,3,3,3,3,3,3,3,3,3,3,4),(120.49937592995,
120.924305556094,121.423992769136,121.923679982177,122.423367195219,122.923054408261,
123.422741621303,123.922428834344,124.422116047386,124.921803260428,125.421490473469,
125.921177686511,126.420864899553,126.78256123713),.UNSPECIFIED.);
#3115=B_SPLINE_CURVE_WITH_KNOTS('',3,(#52205,#52206,#52207,#52208,#52209,
#52210,#52211,#52212,#52213,#52214,#52215,#52216,#52217,#52218,#52219,#52220,
#52221,#52222,#52223,#52224,#52225,#52226,#52227,#52228,#52229,#52230,#52231,
#52232,#52233,#52234,#52235,#52236,#52237,#52238,#52239,#52240,#52241,#52242,
#52243,#52244,#52245,#52246,#52247),.UNSPECIFIED.,.F.,.F.,(4,3,3,3,3,3,
3,3,3,3,3,3,3,3,4),(-136.03943319961,-135.914921947345,-135.415234734304,
-134.915547521262,-134.41586030822,-133.916173095179,-133.416485882137,
-132.916798669095,-132.417111456053,-131.917424243012,-131.41773702997,
-130.918049816928,-130.418362603887,-129.918675390845,-129.75624789243),
 .UNSPECIFIED.);
#3116=B_SPLINE_CURVE_WITH_KNOTS('',3,(#52248,#52249,#52250,#52251,#52252,
#52253,#52254,#52255,#52256,#52257,#52258,#52259,#52260,#52261,#52262,#52263,
#52264,#52265,#52266,#52267,#52268,#52269,#52270,#52271,#52272,#52273,#52274,
#52275,#52276,#52277,#52278,#52279,#52280,#52281,#52282,#52283,#52284,#52285,
#52286,#52287,#52288,#52289,#52290),.UNSPECIFIED.,.F.,.F.,(4,3,3,3,3,3,
3,3,3,3,3,3,3,3,4),(126.78256123713,126.920552112595,127.420239325636,127.919926538678,
128.41961375172,128.919300964761,129.418988177803,129.918675390845,130.418362603887,
130.918049816928,131.41773702997,131.917424243012,132.417111456053,132.916798669095,
133.065746544309),.UNSPECIFIED.);
#3117=B_SPLINE_CURVE_WITH_KNOTS('',3,(#52295,#52296,#52297,#52298,#52299,
#52300,#52301,#52302,#52303,#52304,#52305,#52306,#52307,#52308,#52309,#52310,
#52311,#52312,#52313,#52314,#52315,#52316,#52317,#52318,#52319,#52320,#52321,
#52322,#52323,#52324,#52325,#52326,#52327,#52328,#52329,#52330,#52331,#52332,
#52333,#52334),.UNSPECIFIED.,.F.,.F.,(4,3,3,3,3,3,3,3,3,3,3,3,3,4),(-142.322618506789,
-141.911168503846,-141.411481290804,-140.911794077762,-140.412106864721,
-139.912419651679,-139.412732438637,-138.913045225596,-138.413358012554,
-137.913670799512,-137.41398358647,-136.914296373429,-136.414609160387,
-136.03943319961),.UNSPECIFIED.);
#3118=B_SPLINE_CURVE_WITH_KNOTS('',3,(#52335,#52336,#52337,#52338,#52339,
#52340,#52341,#52342,#52343,#52344,#52345,#52346,#52347,#52348,#52349,#52350,
#52351,#52352,#52353,#52354,#52355,#52356,#52357,#52358,#52359,#52360,#52361,
#52362,#52363,#52364,#52365,#52366,#52367,#52368,#52369,#52370,#52371,#52372,
#52373,#52374),.UNSPECIFIED.,.F.,.F.,(4,3,3,3,3,3,3,3,3,3,3,3,3,4),(133.065746544309,
133.416485882137,133.916173095178,134.41586030822,134.915547521262,135.415234734304,
135.914921947345,136.414609160387,136.914296373429,137.41398358647,137.913670799512,
138.413358012554,138.913045225596,139.348931851489),.UNSPECIFIED.);
#3119=B_SPLINE_CURVE_WITH_KNOTS('',3,(#52379,#52380,#52381,#52382,#52383,
#52384,#52385,#52386,#52387,#52388,#52389,#52390,#52391,#52392,#52393,#52394,
#52395,#52396,#52397,#52398,#52399,#52400,#52401,#52402,#52403,#52404,#52405,
#52406,#52407,#52408,#52409,#52410,#52411,#52412,#52413,#52414,#52415,#52416,
#52417,#52418,#52419,#52420,#52421),.UNSPECIFIED.,.F.,.F.,(4,3,3,3,3,3,
3,3,3,3,3,3,3,3,4),(-148.605803813969,-148.407102273388,-147.907415060346,
-147.407727847305,-146.908040634263,-146.408353421221,-145.90866620818,
-145.408978995138,-144.909291782096,-144.409604569054,-143.909917356013,
-143.410230142971,-142.910542929929,-142.410855716888,-142.322618506789),
 .UNSPECIFIED.);
#3120=B_SPLINE_CURVE_WITH_KNOTS('',3,(#52422,#52423,#52424,#52425,#52426,
#52427,#52428,#52429,#52430,#52431,#52432,#52433,#52434,#52435,#52436,#52437,
#52438,#52439,#52440,#52441,#52442,#52443,#52444,#52445,#52446,#52447,#52448,
#52449,#52450,#52451,#52452,#52453,#52454,#52455,#52456,#52457,#52458,#52459,
#52460,#52461,#52462,#52463,#52464),.UNSPECIFIED.,.F.,.F.,(4,3,3,3,3,3,
3,3,3,3,3,3,3,3,4),(139.348931851489,139.412732438637,139.912419651679,
140.412106864721,140.911794077762,141.411481290804,141.911168503846,142.410855716888,
142.910542929929,143.410230142971,143.909917356013,144.409604569054,144.909291782096,
145.408978995138,145.632117158668),.UNSPECIFIED.);
#3121=B_SPLINE_CURVE_WITH_KNOTS('',3,(#52469,#52470,#52471,#52472,#52473,
#52474,#52475,#52476,#52477,#52478,#52479,#52480,#52481,#52482,#52483,#52484,
#52485,#52486,#52487,#52488,#52489,#52490,#52491,#52492,#52493,#52494,#52495,
#52496,#52497,#52498,#52499,#52500,#52501,#52502,#52503,#52504,#52505,#52506,
#52507,#52508),.UNSPECIFIED.,.F.,.F.,(4,3,3,3,3,3,3,3,3,3,3,3,3,4),(-154.888989121148,
-154.403348829889,-153.903661616847,-153.403974403805,-152.904287190764,
-152.404599977722,-151.90491276468,-151.405225551638,-150.905538338597,
-150.405851125555,-149.906163912513,-149.406476699472,-148.90678948643,
-148.605803813969),.UNSPECIFIED.);
#3122=B_SPLINE_CURVE_WITH_KNOTS('',3,(#52509,#52510,#52511,#52512,#52513,
#52514,#52515,#52516,#52517,#52518,#52519,#52520,#52521,#52522,#52523,#52524,
#52525,#52526,#52527,#52528,#52529,#52530,#52531,#52532,#52533,#52534,#52535,
#52536,#52537,#52538,#52539,#52540,#52541,#52542,#52543,#52544,#52545,#52546,
#52547,#52548,#52549,#52550,#52551),.UNSPECIFIED.,.F.,.F.,(4,3,3,3,3,3,
3,3,3,3,3,3,3,3,4),(145.632117158668,145.90866620818,146.408353421221,146.908040634263,
147.407727847305,147.907415060346,148.407102273388,148.90678948643,149.406476699472,
149.906163912513,150.405851125555,150.905538338597,151.405225551638,151.90491276468,
151.915302465848),.UNSPECIFIED.);
#3123=B_SPLINE_CURVE_WITH_KNOTS('',3,(#52556,#52557,#52558,#52559,#52560,
#52561,#52562,#52563,#52564,#52565,#52566,#52567,#52568,#52569,#52570,#52571,
#52572,#52573,#52574,#52575,#52576,#52577,#52578,#52579,#52580,#52581,#52582,
#52583,#52584,#52585,#52586,#52587,#52588,#52589,#52590,#52591,#52592,#52593,
#52594,#52595,#52596,#52597,#52598),.UNSPECIFIED.,.F.,.F.,(4,3,3,3,3,3,
3,3,3,3,3,3,3,3,4),(-161.172174428328,-160.899282599431,-160.399595386389,
-159.899908173348,-159.400220960306,-158.900533747264,-158.400846534222,
-157.901159321181,-157.401472108139,-156.901784895097,-156.402097682056,
-155.902410469014,-155.402723255972,-154.90303604293,-154.888989121148),
 .UNSPECIFIED.);
#3124=B_SPLINE_CURVE_WITH_KNOTS('',3,(#52599,#52600,#52601,#52602,#52603,
#52604,#52605,#52606,#52607,#52608,#52609,#52610,#52611,#52612,#52613,#52614,
#52615,#52616,#52617,#52618,#52619,#52620,#52621,#52622,#52623,#52624,#52625,
#52626,#52627,#52628,#52629,#52630,#52631,#52632,#52633,#52634,#52635,#52636,
#52637,#52638),.UNSPECIFIED.,.F.,.F.,(4,3,3,3,3,3,3,3,3,3,3,3,3,4),(151.915302465848,
152.404599977722,152.904287190763,153.403974403805,153.903661616847,154.403348829889,
154.90303604293,155.402723255972,155.902410469014,156.402097682055,156.901784895097,
157.401472108139,157.901159321181,158.198487773028),.UNSPECIFIED.);
#3125=B_SPLINE_CURVE_WITH_KNOTS('',3,(#52643,#52644,#52645,#52646,#52647,
#52648,#52649,#52650,#52651,#52652,#52653,#52654,#52655,#52656,#52657,#52658,
#52659,#52660,#52661,#52662,#52663,#52664,#52665,#52666,#52667,#52668,#52669,
#52670,#52671,#52672,#52673,#52674,#52675,#52676,#52677,#52678,#52679,#52680,
#52681,#52682,#52683,#52684,#52685),.UNSPECIFIED.,.F.,.F.,(4,3,3,3,3,3,
3,3,3,3,3,3,3,3,4),(-167.455359735508,-167.395216368973,-166.895529155931,
-166.39584194289,-165.896154729848,-165.396467516806,-164.896780303765,
-164.397093090723,-163.897405877681,-163.397718664639,-162.898031451598,
-162.398344238556,-161.898657025514,-161.398969812473,-161.172174428328),
 .UNSPECIFIED.);
#3126=B_SPLINE_CURVE_WITH_KNOTS('',3,(#52686,#52687,#52688,#52689,#52690,
#52691,#52692,#52693,#52694,#52695,#52696,#52697,#52698,#52699,#52700,#52701,
#52702,#52703,#52704,#52705,#52706,#52707,#52708,#52709,#52710,#52711,#52712,
#52713,#52714,#52715,#52716,#52717,#52718,#52719,#52720,#52721,#52722,#52723,
#52724,#52725,#52726,#52727,#52728),.UNSPECIFIED.,.F.,.F.,(4,3,3,3,3,3,
3,3,3,3,3,3,3,3,4),(158.198487773028,158.400846534222,158.900533747264,
159.400220960306,159.899908173347,160.399595386389,160.899282599431,161.398969812473,
161.898657025514,162.398344238556,162.898031451598,163.397718664639,163.897405877681,
164.397093090723,164.481673080207),.UNSPECIFIED.);
#3127=B_SPLINE_CURVE_WITH_KNOTS('',3,(#52733,#52734,#52735,#52736,#52737,
#52738,#52739,#52740,#52741,#52742,#52743,#52744,#52745,#52746,#52747,#52748,
#52749,#52750,#52751,#52752,#52753,#52754,#52755,#52756,#52757,#52758,#52759,
#52760,#52761,#52762,#52763,#52764,#52765,#52766,#52767,#52768,#52769,#52770,
#52771,#52772),.UNSPECIFIED.,.F.,.F.,(4,3,3,3,3,3,3,3,3,3,3,3,3,4),(-173.738545042687,
-173.391462925474,-172.891775712432,-172.39208849939,-171.892401286349,
-171.392714073307,-170.893026860265,-170.393339647223,-169.893652434182,
-169.39396522114,-168.894278008098,-168.394590795057,-167.894903582015,
-167.455359735508),.UNSPECIFIED.);
#3128=B_SPLINE_CURVE_WITH_KNOTS('',3,(#52773,#52774,#52775,#52776,#52777,
#52778,#52779,#52780,#52781,#52782,#52783,#52784,#52785,#52786,#52787,#52788,
#52789,#52790,#52791,#52792,#52793,#52794,#52795,#52796,#52797,#52798,#52799,
#52800,#52801,#52802,#52803,#52804,#52805,#52806,#52807,#52808,#52809,#52810,
#52811,#52812),.UNSPECIFIED.,.F.,.F.,(4,3,3,3,3,3,3,3,3,3,3,3,3,4),(164.481673080207,
164.896780303765,165.396467516806,165.896154729848,166.39584194289,166.895529155931,
167.395216368973,167.894903582015,168.394590795057,168.894278008098,169.39396522114,
169.893652434182,170.393339647223,170.764858387387),.UNSPECIFIED.);
#3129=B_SPLINE_CURVE_WITH_KNOTS('',3,(#52817,#52818,#52819,#52820,#52821,
#52822,#52823,#52824,#52825,#52826,#52827,#52828,#52829,#52830,#52831,#52832,
#52833,#52834,#52835,#52836,#52837,#52838,#52839,#52840,#52841,#52842,#52843,
#52844,#52845,#52846,#52847,#52848,#52849,#52850,#52851,#52852,#52853,#52854,
#52855,#52856,#52857,#52858,#52859),.UNSPECIFIED.,.F.,.F.,(4,3,3,3,3,3,
3,3,3,3,3,3,3,3,4),(-180.021730349867,-179.887396695016,-179.387709481974,
-178.888022268933,-178.388335055891,-177.888647842849,-177.388960629807,
-176.889273416766,-176.389586203724,-175.889898990682,-175.390211777641,
-174.890524564599,-174.390837351557,-173.891150138515,-173.738545042687),
 .UNSPECIFIED.);
#3130=B_SPLINE_CURVE_WITH_KNOTS('',3,(#52860,#52861,#52862,#52863,#52864,
#52865,#52866,#52867,#52868,#52869,#52870,#52871,#52872,#52873,#52874,#52875,
#52876,#52877,#52878,#52879,#52880,#52881,#52882,#52883,#52884,#52885,#52886,
#52887,#52888,#52889,#52890,#52891,#52892,#52893,#52894,#52895,#52896,#52897,
#52898,#52899,#52900,#52901,#52902),.UNSPECIFIED.,.F.,.F.,(4,3,3,3,3,3,
3,3,3,3,3,3,3,3,4),(170.764858387387,170.893026860265,171.392714073307,
171.892401286349,172.39208849939,172.891775712432,173.391462925474,173.891150138515,
174.390837351557,174.890524564599,175.390211777641,175.889898990682,176.389586203724,
176.889273416766,177.048043694566),.UNSPECIFIED.);
#3131=B_SPLINE_CURVE_WITH_KNOTS('',3,(#52907,#52908,#52909,#52910,#52911,
#52912,#52913,#52914,#52915,#52916,#52917,#52918,#52919,#52920,#52921,#52922,
#52923,#52924,#52925,#52926,#52927,#52928,#52929,#52930,#52931,#52932,#52933,
#52934,#52935,#52936,#52937,#52938,#52939,#52940,#52941,#52942,#52943,#52944,
#52945,#52946),.UNSPECIFIED.,.F.,.F.,(4,3,3,3,3,3,3,3,3,3,3,3,3,4),(-186.304915657046,
-185.883643251516,-185.383956038475,-184.884268825433,-184.384581612391,
-183.88489439935,-183.385207186308,-182.885519973266,-182.385832760224,
-181.886145547183,-181.386458334141,-180.886771121099,-180.387083908058,
-180.021730349867),.UNSPECIFIED.);
#3132=B_SPLINE_CURVE_WITH_KNOTS('',3,(#52947,#52948,#52949,#52950,#52951,
#52952,#52953,#52954,#52955,#52956,#52957,#52958,#52959,#52960,#52961,#52962,
#52963,#52964,#52965,#52966,#52967,#52968,#52969,#52970,#52971,#52972,#52973,
#52974,#52975,#52976,#52977,#52978,#52979,#52980,#52981,#52982,#52983,#52984,
#52985,#52986),.UNSPECIFIED.,.F.,.F.,(4,3,3,3,3,3,3,3,3,3,3,3,3,4),(177.048043694566,
177.388960629807,177.888647842849,178.388335055891,178.888022268932,179.387709481974,
179.887396695016,180.387083908058,180.886771121099,181.386458334141,181.886145547183,
182.385832760225,182.885519973266,183.331229001746),.UNSPECIFIED.);
#3133=B_SPLINE_CURVE_WITH_KNOTS('',3,(#52991,#52992,#52993,#52994,#52995,
#52996,#52997,#52998,#52999,#53000,#53001,#53002,#53003,#53004,#53005,#53006,
#53007,#53008,#53009,#53010,#53011,#53012,#53013,#53014,#53015,#53016,#53017,
#53018,#53019,#53020,#53021,#53022,#53023,#53024,#53025,#53026,#53027,#53028,
#53029,#53030,#53031,#53032,#53033),.UNSPECIFIED.,.F.,.F.,(4,3,3,3,3,3,
3,3,3,3,3,3,3,3,4),(-192.588100964226,-192.379577021059,-191.879889808017,
-191.380202594975,-190.880515381934,-190.380828168892,-189.88114095585,
-189.381453742808,-188.881766529767,-188.382079316725,-187.882392103683,
-187.382704890642,-186.8830176776,-186.383330464558,-186.304915657046),
 .UNSPECIFIED.);
#3134=B_SPLINE_CURVE_WITH_KNOTS('',3,(#53034,#53035,#53036,#53037,#53038,
#53039,#53040,#53041,#53042,#53043,#53044,#53045,#53046,#53047,#53048,#53049,
#53050,#53051,#53052,#53053,#53054,#53055,#53056,#53057,#53058,#53059,#53060,
#53061,#53062,#53063,#53064,#53065,#53066,#53067,#53068,#53069,#53070,#53071,
#53072,#53073,#53074,#53075,#53076),.UNSPECIFIED.,.F.,.F.,(4,3,3,3,3,3,
3,3,3,3,3,3,3,3,4),(183.331229001746,183.385207186308,183.88489439935,184.384581612391,
184.884268825433,185.383956038475,185.883643251516,186.383330464558,186.8830176776,
187.382704890642,187.882392103683,188.382079316725,188.881766529767,189.381453742808,
189.614414308925),.UNSPECIFIED.);
#3135=B_SPLINE_CURVE_WITH_KNOTS('',3,(#53081,#53082,#53083,#53084,#53085,
#53086,#53087,#53088,#53089,#53090,#53091,#53092,#53093,#53094,#53095,#53096,
#53097,#53098,#53099,#53100,#53101,#53102,#53103,#53104,#53105,#53106,#53107,
#53108,#53109,#53110,#53111,#53112,#53113,#53114,#53115,#53116,#53117,#53118,
#53119,#53120),.UNSPECIFIED.,.F.,.F.,(4,3,3,3,3,3,3,3,3,3,3,3,3,4),(-198.871286271405,
-198.375823577559,-197.876136364518,-197.376449151476,-196.876761938434,
-196.377074725392,-195.877387512351,-195.377700299309,-194.878013086267,
-194.378325873226,-193.878638660184,-193.378951447142,-192.8792642341,-192.588100964226),
 .UNSPECIFIED.);
#3136=B_SPLINE_CURVE_WITH_KNOTS('',3,(#53121,#53122,#53123,#53124,#53125,
#53126,#53127,#53128,#53129,#53130,#53131,#53132,#53133,#53134,#53135,#53136,
#53137,#53138,#53139,#53140,#53141,#53142,#53143,#53144,#53145,#53146,#53147,
#53148,#53149,#53150,#53151,#53152,#53153,#53154,#53155,#53156,#53157,#53158,
#53159,#53160,#53161,#53162,#53163),.UNSPECIFIED.,.F.,.F.,(4,3,3,3,3,3,
3,3,3,3,3,3,3,3,4),(189.614414308925,189.88114095585,190.380828168892,190.880515381934,
191.380202594975,191.879889808017,192.379577021059,192.8792642341,193.378951447142,
193.878638660184,194.378325873226,194.878013086267,195.377700299309,195.877387512351,
195.897599616105),.UNSPECIFIED.);
#3137=B_SPLINE_CURVE_WITH_KNOTS('',3,(#53168,#53169,#53170,#53171,#53172,
#53173,#53174,#53175,#53176,#53177,#53178,#53179,#53180,#53181,#53182,#53183,
#53184,#53185,#53186,#53187,#53188,#53189,#53190,#53191,#53192,#53193,#53194,
#53195,#53196,#53197,#53198,#53199,#53200,#53201,#53202,#53203,#53204,#53205,
#53206,#53207,#53208,#53209,#53210),.UNSPECIFIED.,.F.,.F.,(4,3,3,3,3,3,
3,3,3,3,3,3,3,3,4),(-205.154471578585,-204.871757347102,-204.37207013406,
-203.872382921018,-203.372695707976,-202.873008494935,-202.373321281893,
-201.873634068851,-201.373946855809,-200.874259642768,-200.374572429726,
-199.874885216684,-199.375198003643,-198.875510790601,-198.871286271405),
 .UNSPECIFIED.);
#3138=B_SPLINE_CURVE_WITH_KNOTS('',3,(#53211,#53212,#53213,#53214,#53215,
#53216,#53217,#53218,#53219,#53220,#53221,#53222,#53223,#53224,#53225,#53226,
#53227,#53228,#53229,#53230,#53231,#53232,#53233,#53234,#53235,#53236,#53237,
#53238,#53239,#53240,#53241,#53242,#53243,#53244,#53245,#53246,#53247,#53248,
#53249,#53250),.UNSPECIFIED.,.F.,.F.,(4,3,3,3,3,3,3,3,3,3,3,3,3,4),(195.897599616105,
196.377074725392,196.876761938434,197.376449151476,197.876136364518,198.375823577559,
198.875510790601,199.375198003643,199.874885216684,200.374572429726,200.874259642768,
201.373946855809,201.873634068851,202.180784923285),.UNSPECIFIED.);
#3139=B_SPLINE_CURVE_WITH_KNOTS('',3,(#53255,#53256,#53257,#53258,#53259,
#53260,#53261,#53262,#53263,#53264,#53265,#53266,#53267,#53268,#53269,#53270,
#53271,#53272,#53273,#53274,#53275,#53276,#53277,#53278,#53279,#53280,#53281,
#53282,#53283,#53284,#53285,#53286,#53287,#53288,#53289,#53290,#53291,#53292,
#53293,#53294,#53295,#53296,#53297),.UNSPECIFIED.,.F.,.F.,(4,3,3,3,3,3,
3,3,3,3,3,3,3,3,4),(-211.437656885764,-211.367691116644,-210.868003903602,
-210.36831669056,-209.868629477519,-209.368942264477,-208.869255051435,
-208.369567838393,-207.869880625352,-207.37019341231,-206.870506199268,
-206.370818986227,-205.871131773185,-205.371444560143,-205.154471578585),
 .UNSPECIFIED.);
#3140=B_SPLINE_CURVE_WITH_KNOTS('',3,(#53298,#53299,#53300,#53301,#53302,
#53303,#53304,#53305,#53306,#53307,#53308,#53309,#53310,#53311,#53312,#53313,
#53314,#53315,#53316,#53317,#53318,#53319,#53320,#53321,#53322,#53323,#53324,
#53325,#53326,#53327,#53328,#53329,#53330,#53331,#53332,#53333,#53334,#53335,
#53336,#53337,#53338,#53339,#53340),.UNSPECIFIED.,.F.,.F.,(4,3,3,3,3,3,
3,3,3,3,3,3,3,3,4),(202.180784923285,202.373321281893,202.873008494935,
203.372695707976,203.872382921018,204.37207013406,204.871757347101,205.371444560143,
205.871131773185,206.370818986227,206.870506199268,207.37019341231,207.869880625352,
208.369567838393,208.463970230464),.UNSPECIFIED.);
#3141=B_SPLINE_CURVE_WITH_KNOTS('',3,(#53345,#53346,#53347,#53348,#53349,
#53350,#53351,#53352,#53353,#53354,#53355,#53356,#53357,#53358,#53359,#53360,
#53361,#53362,#53363,#53364,#53365,#53366,#53367,#53368,#53369,#53370,#53371,
#53372,#53373,#53374,#53375,#53376,#53377,#53378,#53379,#53380,#53381,#53382,
#53383,#53384),.UNSPECIFIED.,.F.,.F.,(4,3,3,3,3,3,3,3,3,3,3,3,3,4),(-217.720842192944,
-217.363937673144,-216.864250460103,-216.364563247061,-215.864876034019,
-215.365188820977,-214.865501607936,-214.365814394894,-213.866127181852,
-213.366439968811,-212.866752755769,-212.367065542727,-211.867378329685,
-211.437656885764),.UNSPECIFIED.);
#3142=B_SPLINE_CURVE_WITH_KNOTS('',3,(#53385,#53386,#53387,#53388,#53389,
#53390,#53391,#53392,#53393,#53394,#53395,#53396,#53397,#53398,#53399,#53400,
#53401,#53402,#53403,#53404,#53405,#53406,#53407,#53408,#53409,#53410,#53411,
#53412,#53413,#53414,#53415,#53416,#53417,#53418,#53419,#53420,#53421,#53422,
#53423,#53424),.UNSPECIFIED.,.F.,.F.,(4,3,3,3,3,3,3,3,3,3,3,3,3,4),(208.463970230464,
208.869255051435,209.368942264477,209.868629477519,210.36831669056,210.868003903602,
211.367691116644,211.867378329685,212.367065542727,212.866752755769,213.366439968811,
213.866127181852,214.365814394894,214.747155537644),.UNSPECIFIED.);
#3143=B_SPLINE_CURVE_WITH_KNOTS('',3,(#53429,#53430,#53431,#53432,#53433,
#53434,#53435,#53436,#53437,#53438,#53439,#53440,#53441,#53442,#53443,#53444,
#53445,#53446,#53447,#53448,#53449,#53450,#53451,#53452,#53453,#53454,#53455,
#53456,#53457,#53458,#53459,#53460,#53461,#53462,#53463,#53464,#53465,#53466,
#53467,#53468,#53469,#53470,#53471),.UNSPECIFIED.,.F.,.F.,(4,3,3,3,3,3,
3,3,3,3,3,3,3,3,4),(-224.004027500124,-223.859871442686,-223.360184229645,
-222.860497016603,-222.360809803561,-221.86112259052,-221.361435377478,
-220.861748164436,-220.362060951395,-219.862373738353,-219.362686525311,
-218.862999312269,-218.363312099228,-217.863624886186,-217.720842192944),
 .UNSPECIFIED.);
#3144=B_SPLINE_CURVE_WITH_KNOTS('',3,(#53472,#53473,#53474,#53475,#53476,
#53477,#53478,#53479,#53480,#53481,#53482,#53483,#53484,#53485,#53486,#53487,
#53488,#53489,#53490,#53491,#53492,#53493,#53494,#53495,#53496,#53497,#53498,
#53499,#53500,#53501,#53502,#53503,#53504,#53505,#53506,#53507,#53508,#53509,
#53510,#53511,#53512,#53513,#53514),.UNSPECIFIED.,.F.,.F.,(4,3,3,3,3,3,
3,3,3,3,3,3,3,3,4),(214.747155537644,214.865501607936,215.365188820977,
215.864876034019,216.364563247061,216.864250460103,217.363937673144,217.863624886186,
218.363312099228,218.862999312269,219.362686525311,219.862373738353,220.362060951395,
220.861748164436,221.030340844823),.UNSPECIFIED.);
#3145=B_SPLINE_CURVE_WITH_KNOTS('',3,(#53523,#53524,#53525,#53526,#53527,
#53528,#53529,#53530,#53531,#53532,#53533,#53534,#53535),.UNSPECIFIED.,
 .F.,.F.,(4,3,3,3,4),(-231.854866851354,-231.355179638312,-230.85549242527,
-230.355805212229,-230.287212807303),.UNSPECIFIED.);
#3146=B_SPLINE_CURVE_WITH_KNOTS('',3,(#53539,#53540,#53541,#53542,#53543,
#53544,#53545,#53546,#53547,#53548,#53549,#53550,#53551,#53552,#53553,#53554,
#53555,#53556,#53557),.UNSPECIFIED.,.F.,.F.,(4,3,3,3,3,3,4),(227.313526152003,
227.357681933978,227.85736914702,228.357056360062,228.856743573104,229.356430786145,
229.785062662568),.UNSPECIFIED.);
#3147=B_SPLINE_CURVE_WITH_KNOTS('',3,(#53564,#53565,#53566,#53567,#53568,
#53569,#53570,#53571,#53572,#53573,#53574,#53575,#53576,#53577,#53578),
 .UNSPECIFIED.,.F.,.F.,(4,1,1,1,1,1,1,1,1,1,1,1,4),(235.619449019234,235.974980174839,
236.474667387881,236.974354600923,237.474041813964,237.973729027006,238.473416240048,
238.973103453089,239.472790666131,239.972477879173,240.472165092214,240.971852305256,
241.400484181679),.UNSPECIFIED.);
#3148=B_SPLINE_CURVE_WITH_KNOTS('',3,(#53581,#53582,#53583,#53584,#53585,
#53586,#53587,#53588,#53589,#53590,#53591,#53592,#53593),.UNSPECIFIED.,
 .F.,.F.,(4,1,1,1,1,1,1,1,1,1,4),(235.619449019234,235.66360480121,236.163292014252,
236.662979227294,237.162666440336,237.662353653377,238.162040866419,238.661728079461,
239.161415292502,239.661102505544,240.160789718586),.UNSPECIFIED.);
#3149=B_SPLINE_CURVE_WITH_KNOTS('',3,(#53598,#53599,#53600,#53601,#53602,
#53603,#53604,#53605,#53606,#53607,#53608,#53609,#53610,#53611,#53612,#53613,
#53614),.UNSPECIFIED.,.F.,.F.,(4,1,1,1,1,1,1,1,1,1,1,1,1,1,4),(229.336263712055,
229.479046405297,229.978733618339,230.47842083138,230.978108044422,231.477795257464,
231.977482470505,232.477169683547,232.976856896589,233.476544109631,233.976231322672,
234.475918535714,234.975605748756,235.475292961797,235.619449019234),
 .UNSPECIFIED.);
#3150=B_SPLINE_CURVE_WITH_KNOTS('',3,(#53615,#53616,#53617,#53618,#53619,
#53620,#53621,#53622,#53623,#53624,#53625,#53626,#53627,#53628,#53629,#53630),
 .UNSPECIFIED.,.F.,.F.,(4,1,1,1,1,1,1,1,1,1,1,1,1,4),(229.336263712055,
229.66735824471,230.167045457752,230.666732670793,231.166419883835,231.666107096877,
232.165794309918,232.66548152296,233.165168736002,233.664855949044,234.164543162085,
234.664230375127,235.163917588169,235.619449019234),.UNSPECIFIED.);
#3151=B_SPLINE_CURVE_WITH_KNOTS('',3,(#53635,#53636,#53637,#53638,#53639,
#53640,#53641,#53642,#53643,#53644,#53645,#53646,#53647,#53648,#53649,#53650),
 .UNSPECIFIED.,.F.,.F.,(4,1,1,1,1,1,1,1,1,1,1,1,1,4),(223.053078404875,
223.482799848796,223.982487061838,224.48217427488,224.981861487921,225.481548700963,
225.981235914005,226.480923127047,226.980610340088,227.48029755313,227.979984766172,
228.479671979213,228.979359192255,229.336263712055),.UNSPECIFIED.);
#3152=B_SPLINE_CURVE_WITH_KNOTS('',3,(#53651,#53652,#53653,#53654,#53655,
#53656,#53657,#53658,#53659,#53660,#53661,#53662,#53663,#53664,#53665,#53666,
#53667),.UNSPECIFIED.,.F.,.F.,(4,1,1,1,1,1,1,1,1,1,1,1,1,1,4),(223.053078404875,
223.171424475168,223.671111688209,224.170798901251,224.670486114293,225.170173327334,
225.669860540376,226.169547753418,226.66923496646,227.168922179501,227.668609392543,
228.168296605585,228.667983818626,229.167671031668,229.336263712055),
 .UNSPECIFIED.);
#3153=B_SPLINE_CURVE_WITH_KNOTS('',3,(#53672,#53673,#53674,#53675,#53676,
#53677,#53678,#53679,#53680,#53681,#53682,#53683,#53684,#53685,#53686,#53687,
#53688),.UNSPECIFIED.,.F.,.F.,(4,1,1,1,1,1,1,1,1,1,1,1,1,1,4),(216.769893097696,
216.986866079254,217.486553292296,217.986240505338,218.485927718379,218.985614931421,
219.485302144463,219.984989357504,220.484676570546,220.984363783588,221.484050996629,
221.983738209671,222.483425422713,222.983112635755,223.053078404875),
 .UNSPECIFIED.);
#3154=B_SPLINE_CURVE_WITH_KNOTS('',3,(#53689,#53690,#53691,#53692,#53693,
#53694,#53695,#53696,#53697,#53698,#53699,#53700,#53701,#53702,#53703,#53704),
 .UNSPECIFIED.,.F.,.F.,(4,1,1,1,1,1,1,1,1,1,1,1,1,4),(216.769893097696,
217.175177918667,217.674865131709,218.174552344751,218.674239557792,219.173926770834,
219.673613983876,220.173301196917,220.672988409959,221.172675623001,221.672362836043,
222.172050049084,222.671737262126,223.053078404875),.UNSPECIFIED.);
#3155=B_SPLINE_CURVE_WITH_KNOTS('',3,(#53709,#53710,#53711,#53712,#53713,
#53714,#53715,#53716,#53717,#53718,#53719,#53720,#53721,#53722,#53723,#53724,
#53725),.UNSPECIFIED.,.F.,.F.,(4,1,1,1,1,1,1,1,1,1,1,1,1,1,4),(210.486707790516,
210.490932309712,210.990619522754,211.490306735795,211.989993948837,212.489681161879,
212.98936837492,213.489055587962,213.988742801004,214.488430014046,214.988117227087,
215.487804440129,215.987491653171,216.487178866212,216.769893097696),
 .UNSPECIFIED.);
#3156=B_SPLINE_CURVE_WITH_KNOTS('',3,(#53726,#53727,#53728,#53729,#53730,
#53731,#53732,#53733,#53734,#53735,#53736,#53737,#53738,#53739,#53740,#53741,
#53742),.UNSPECIFIED.,.F.,.F.,(4,1,1,1,1,1,1,1,1,1,1,1,1,1,4),(210.486707790516,
210.679244149125,211.178931362167,211.678618575208,212.17830578825,212.677993001292,
213.177680214333,213.677367427375,214.177054640417,214.676741853459,215.1764290665,
215.676116279542,216.175803492584,216.675490705625,216.769893097696),
 .UNSPECIFIED.);
#3157=B_SPLINE_CURVE_WITH_KNOTS('',3,(#53747,#53748,#53749,#53750,#53751,
#53752,#53753,#53754,#53755,#53756,#53757,#53758,#53759,#53760,#53761,#53762),
 .UNSPECIFIED.,.F.,.F.,(4,1,1,1,1,1,1,1,1,1,1,1,1,4),(204.203522483337,
204.494685753211,204.994372966253,205.494060179295,205.993747392336,206.493434605378,
206.99312181842,207.492809031462,207.992496244503,208.492183457545,208.991870670587,
209.491557883628,209.99124509667,210.486707790516),.UNSPECIFIED.);
#3158=B_SPLINE_CURVE_WITH_KNOTS('',3,(#53763,#53764,#53765,#53766,#53767,
#53768,#53769,#53770,#53771,#53772,#53773,#53774,#53775,#53776,#53777,#53778),
 .UNSPECIFIED.,.F.,.F.,(4,1,1,1,1,1,1,1,1,1,1,1,1,4),(204.203522483337,
204.682997592624,205.182684805666,205.682372018708,206.182059231749,206.681746444791,
207.181433657833,207.681120870875,208.180808083916,208.680495296958,209.18018251,
209.679869723041,210.179556936083,210.486707790516),.UNSPECIFIED.);
#3159=B_SPLINE_CURVE_WITH_KNOTS('',3,(#53783,#53784,#53785,#53786,#53787,
#53788,#53789,#53790,#53791,#53792,#53793,#53794,#53795,#53796,#53797,#53798,
#53799),.UNSPECIFIED.,.F.,.F.,(4,1,1,1,1,1,1,1,1,1,1,1,1,1,4),(197.920337176157,
197.998751983669,198.498439196711,198.998126409752,199.497813622794,199.997500835836,
200.497188048878,200.996875261919,201.496562474961,201.996249688003,202.495936901044,
202.995624114086,203.495311327128,203.99499854017,204.203522483337),
 .UNSPECIFIED.);
#3160=B_SPLINE_CURVE_WITH_KNOTS('',3,(#53800,#53801,#53802,#53803,#53804,
#53805,#53806,#53807,#53808,#53809,#53810,#53811,#53812,#53813,#53814,#53815,
#53816),.UNSPECIFIED.,.F.,.F.,(4,1,1,1,1,1,1,1,1,1,1,1,1,1,4),(197.920337176157,
198.187063823082,198.686751036124,199.186438249166,199.686125462207,200.185812675249,
200.685499888291,201.185187101332,201.684874314374,202.184561527416,202.684248740457,
203.183935953499,203.683623166541,204.183310379583,204.203522483337),
 .UNSPECIFIED.);
#3161=B_SPLINE_CURVE_WITH_KNOTS('',3,(#53821,#53822,#53823,#53824,#53825,
#53826,#53827,#53828,#53829,#53830,#53831,#53832,#53833,#53834,#53835,#53836),
 .UNSPECIFIED.,.F.,.F.,(4,1,1,1,1,1,1,1,1,1,1,1,1,4),(191.637151868977,
192.002505427169,192.50219264021,193.001879853252,193.501567066294,194.001254279335,
194.500941492377,195.000628705419,195.500315918461,196.000003131502,196.499690344544,
196.999377557586,197.499064770627,197.920337176157),.UNSPECIFIED.);
#3162=B_SPLINE_CURVE_WITH_KNOTS('',3,(#53837,#53838,#53839,#53840,#53841,
#53842,#53843,#53844,#53845,#53846,#53847,#53848,#53849,#53850,#53851,#53852,
#53853),.UNSPECIFIED.,.F.,.F.,(4,1,1,1,1,1,1,1,1,1,1,1,1,1,4),(191.637151868977,
191.69113005354,192.190817266582,192.690504479623,193.190191692665,193.689878905707,
194.189566118748,194.68925333179,195.188940544832,195.688627757874,196.188314970915,
196.688002183957,197.187689396999,197.68737661004,197.920337176157),
 .UNSPECIFIED.);
#3163=B_SPLINE_CURVE_WITH_KNOTS('',3,(#53858,#53859,#53860,#53861,#53862,
#53863,#53864,#53865,#53866,#53867,#53868,#53869,#53870,#53871,#53872,#53873,
#53874),.UNSPECIFIED.,.F.,.F.,(4,1,1,1,1,1,1,1,1,1,1,1,1,1,4),(185.353966561798,
185.506571657626,186.006258870668,186.50594608371,187.005633296751,187.505320509793,
188.005007722835,188.504694935877,189.004382148918,189.50406936196,190.003756575002,
190.503443788043,191.003131001085,191.502818214127,191.637151868977),
 .UNSPECIFIED.);
#3164=B_SPLINE_CURVE_WITH_KNOTS('',3,(#53875,#53876,#53877,#53878,#53879,
#53880,#53881,#53882,#53883,#53884,#53885,#53886,#53887,#53888,#53889,#53890),
 .UNSPECIFIED.,.F.,.F.,(4,1,1,1,1,1,1,1,1,1,1,1,1,4),(185.353966561798,
185.694883497039,186.194570710081,186.694257923123,187.193945136164,187.693632349206,
188.193319562248,188.69300677529,189.192693988331,189.692381201373,190.192068414415,
190.691755627456,191.191442840498,191.637151868977),.UNSPECIFIED.);
#3165=B_SPLINE_CURVE_WITH_KNOTS('',3,(#53895,#53896,#53897,#53898,#53899,
#53900,#53901,#53902,#53903,#53904,#53905,#53906,#53907,#53908,#53909,#53910),
 .UNSPECIFIED.,.F.,.F.,(4,1,1,1,1,1,1,1,1,1,1,1,1,4),(179.070781254618,
179.510325101126,180.010012314167,180.509699527209,181.009386740251,181.509073953293,
182.008761166334,182.508448379376,183.008135592418,183.507822805459,184.007510018501,
184.507197231543,185.006884444585,185.353966561798),.UNSPECIFIED.);
#3166=B_SPLINE_CURVE_WITH_KNOTS('',3,(#53911,#53912,#53913,#53914,#53915,
#53916,#53917,#53918,#53919,#53920,#53921,#53922,#53923,#53924,#53925,#53926,
#53927),.UNSPECIFIED.,.F.,.F.,(4,1,1,1,1,1,1,1,1,1,1,1,1,1,4),(179.070781254618,
179.198949727497,179.698636940539,180.198324153581,180.698011366622,181.197698579664,
181.697385792706,182.197073005747,182.696760218789,183.196447431831,183.696134644872,
184.195821857914,184.695509070956,185.195196283998,185.353966561798),
 .UNSPECIFIED.);
#3167=B_SPLINE_CURVE_WITH_KNOTS('',3,(#53932,#53933,#53934,#53935,#53936,
#53937,#53938,#53939,#53940,#53941,#53942,#53943,#53944,#53945,#53946,#53947,
#53948),.UNSPECIFIED.,.F.,.F.,(4,1,1,1,1,1,1,1,1,1,1,1,1,1,4),(172.787595947439,
173.014391331584,173.514078544625,174.013765757667,174.513452970709,175.01314018375,
175.512827396792,176.012514609834,176.512201822876,177.011889035917,177.511576248959,
178.011263462001,178.510950675042,179.010637888084,179.070781254618),
 .UNSPECIFIED.);
#3168=B_SPLINE_CURVE_WITH_KNOTS('',3,(#53949,#53950,#53951,#53952,#53953,
#53954,#53955,#53956,#53957,#53958,#53959,#53960,#53961,#53962,#53963,#53964),
 .UNSPECIFIED.,.F.,.F.,(4,1,1,1,1,1,1,1,1,1,1,1,1,4),(172.787595947439,
173.202703170997,173.702390384038,174.20207759708,174.701764810122,175.201452023163,
175.701139236205,176.200826449247,176.700513662289,177.20020087533,177.699888088372,
178.199575301414,178.699262514455,179.070781254618),.UNSPECIFIED.);
#3169=B_SPLINE_CURVE_WITH_KNOTS('',3,(#53969,#53970,#53971,#53972,#53973,
#53974,#53975,#53976,#53977,#53978,#53979,#53980,#53981,#53982,#53983,#53984,
#53985),.UNSPECIFIED.,.F.,.F.,(4,1,1,1,1,1,1,1,1,1,1,1,1,1,4),(166.504410640259,
166.518457562041,167.018144775083,167.517831988125,168.017519201166,168.517206414208,
169.01689362725,169.516580840292,170.016268053333,170.515955266375,171.015642479417,
171.515329692458,172.0150169055,172.514704118542,172.787595947439),
 .UNSPECIFIED.);
#3170=B_SPLINE_CURVE_WITH_KNOTS('',3,(#53986,#53987,#53988,#53989,#53990,
#53991,#53992,#53993,#53994,#53995,#53996,#53997,#53998,#53999,#54000,#54001,
#54002),.UNSPECIFIED.,.F.,.F.,(4,1,1,1,1,1,1,1,1,1,1,1,1,1,4),(166.504410640259,
166.706769401454,167.206456614496,167.706143827538,168.205831040579,168.705518253621,
169.205205466663,169.704892679705,170.204579892746,170.704267105788,171.20395431883,
171.703641531871,172.203328744913,172.703015957955,172.787595947439),
 .UNSPECIFIED.);
#3171=B_SPLINE_CURVE_WITH_KNOTS('',3,(#54007,#54008,#54009,#54010,#54011,
#54012,#54013,#54014,#54015,#54016,#54017,#54018,#54019,#54020,#54021,#54022),
 .UNSPECIFIED.,.F.,.F.,(4,1,1,1,1,1,1,1,1,1,1,1,1,4),(160.22122533308,160.522211005541,
161.021898218582,161.521585431624,162.021272644666,162.520959857708,163.020647070749,
163.520334283791,164.020021496833,164.519708709874,165.019395922916,165.519083135958,
166.018770349,166.504410640259),.UNSPECIFIED.);
#3172=B_SPLINE_CURVE_WITH_KNOTS('',3,(#54023,#54024,#54025,#54026,#54027,
#54028,#54029,#54030,#54031,#54032,#54033,#54034,#54035,#54036,#54037,#54038),
 .UNSPECIFIED.,.F.,.F.,(4,1,1,1,1,1,1,1,1,1,1,1,1,4),(160.22122533308,160.710522844954,
161.210210057995,161.709897271037,162.209584484079,162.709271697121,163.208958910162,
163.708646123204,164.208333336246,164.708020549287,165.207707762329,165.707394975371,
166.207082188413,166.504410640259),.UNSPECIFIED.);
#3173=B_SPLINE_CURVE_WITH_KNOTS('',3,(#54043,#54044,#54045,#54046,#54047,
#54048,#54049,#54050,#54051,#54052,#54053,#54054,#54055,#54056,#54057,#54058,
#54059),.UNSPECIFIED.,.F.,.F.,(4,1,1,1,1,1,1,1,1,1,1,1,1,1,4),(153.9380400259,
154.026277235998,154.52596444904,155.025651662082,155.525338875124,156.025026088165,
156.524713301207,157.024400514249,157.52408772729,158.023774940332,158.523462153374,
159.023149366416,159.522836579457,160.022523792499,160.22122533308),
 .UNSPECIFIED.);
#3174=B_SPLINE_CURVE_WITH_KNOTS('',3,(#54060,#54061,#54062,#54063,#54064,
#54065,#54066,#54067,#54068,#54069,#54070,#54071,#54072,#54073,#54074,#54075,
#54076),.UNSPECIFIED.,.F.,.F.,(4,1,1,1,1,1,1,1,1,1,1,1,1,1,4),(153.9380400259,
154.214589075412,154.714276288453,155.213963501495,155.713650714537,156.213337927578,
156.71302514062,157.212712353662,157.712399566704,158.212086779745,158.711773992787,
159.211461205829,159.71114841887,160.210835631912,160.22122533308),
 .UNSPECIFIED.);
#3175=B_SPLINE_CURVE_WITH_KNOTS('',3,(#54081,#54082,#54083,#54084,#54085,
#54086,#54087,#54088,#54089,#54090,#54091,#54092,#54093,#54094,#54095,#54096),
 .UNSPECIFIED.,.F.,.F.,(4,1,1,1,1,1,1,1,1,1,1,1,1,4),(147.654854718721,
148.030030679498,148.52971789254,149.029405105581,149.529092318623,150.028779531665,
150.528466744707,151.028153957748,151.52784117079,152.027528383832,152.527215596873,
153.026902809915,153.526590022957,153.9380400259),.UNSPECIFIED.);
#3176=B_SPLINE_CURVE_WITH_KNOTS('',3,(#54097,#54098,#54099,#54100,#54101,
#54102,#54103,#54104,#54105,#54106,#54107,#54108,#54109,#54110,#54111,#54112,
#54113),.UNSPECIFIED.,.F.,.F.,(4,1,1,1,1,1,1,1,1,1,1,1,1,1,4),(147.654854718721,
147.718655305869,148.218342518911,148.718029731953,149.217716944994,149.717404158036,
150.217091371078,150.71677858412,151.216465797161,151.716153010203,152.215840223245,
152.715527436286,153.215214649328,153.71490186237,153.9380400259),
 .UNSPECIFIED.);
#3177=B_SPLINE_CURVE_WITH_KNOTS('',3,(#54118,#54119,#54120,#54121,#54122,
#54123,#54124,#54125,#54126,#54127,#54128,#54129,#54130,#54131,#54132,#54133,
#54134),.UNSPECIFIED.,.F.,.F.,(4,1,1,1,1,1,1,1,1,1,1,1,1,1,4),(141.371669411541,
141.534096909956,142.033784122997,142.533471336039,143.033158549081,143.532845762123,
144.032532975164,144.532220188206,145.031907401248,145.531594614289,146.031281827331,
146.530969040373,147.030656253415,147.530343466456,147.654854718721),
 .UNSPECIFIED.);
#3178=B_SPLINE_CURVE_WITH_KNOTS('',3,(#54135,#54136,#54137,#54138,#54139,
#54140,#54141,#54142,#54143,#54144,#54145,#54146,#54147,#54148,#54149,#54150),
 .UNSPECIFIED.,.F.,.F.,(4,1,1,1,1,1,1,1,1,1,1,1,1,4),(141.371669411541,
141.722408749369,142.22209596241,142.721783175452,143.221470388494,143.721157601536,
144.220844814577,144.720532027619,145.220219240661,145.719906453702,146.219593666744,
146.719280879786,147.218968092828,147.654854718721),.UNSPECIFIED.);
#3179=B_SPLINE_CURVE_WITH_KNOTS('',3,(#54155,#54156,#54157,#54158,#54159,
#54160,#54161,#54162,#54163,#54164,#54165,#54166,#54167,#54168,#54169,#54170),
 .UNSPECIFIED.,.F.,.F.,(4,1,1,1,1,1,1,1,1,1,1,1,1,4),(135.088484104361,
135.537850353455,136.037537566497,136.537224779539,137.03691199258,137.536599205622,
138.036286418664,138.535973631705,139.035660844747,139.535348057789,140.035035270831,
140.534722483872,141.034409696914,141.371669411541),.UNSPECIFIED.);
#3180=B_SPLINE_CURVE_WITH_KNOTS('',3,(#54171,#54172,#54173,#54174,#54175,
#54176,#54177,#54178,#54179,#54180,#54181,#54182,#54183,#54184,#54185,#54186,
#54187),.UNSPECIFIED.,.F.,.F.,(4,1,1,1,1,1,1,1,1,1,1,1,1,1,4),(135.088484104361,
135.226474979827,135.726162192868,136.22584940591,136.725536618952,137.225223831993,
137.724911045035,138.224598258077,138.724285471118,139.22397268416,139.723659897202,
140.223347110244,140.723034323285,141.222721536327,141.371669411541),
 .UNSPECIFIED.);
#3181=B_SPLINE_CURVE_WITH_KNOTS('',3,(#54192,#54193,#54194,#54195,#54196,
#54197,#54198,#54199,#54200,#54201,#54202,#54203,#54204,#54205,#54206,#54207,
#54208),.UNSPECIFIED.,.F.,.F.,(4,1,1,1,1,1,1,1,1,1,1,1,1,1,4),(128.805298797182,
129.041916583913,129.541603796955,130.041291009996,130.540978223038,131.04066543608,
131.540352649122,132.040039862163,132.539727075205,133.039414288247,133.539101501288,
134.03878871433,134.538475927372,135.038163140414,135.088484104361),
 .UNSPECIFIED.);
#3182=B_SPLINE_CURVE_WITH_KNOTS('',3,(#54209,#54210,#54211,#54212,#54213,
#54214,#54215,#54216,#54217,#54218,#54219,#54220,#54221,#54222,#54223,#54224),
 .UNSPECIFIED.,.F.,.F.,(4,1,1,1,1,1,1,1,1,1,1,1,1,4),(128.805298797182,
129.230228423326,129.729915636368,130.229602849409,130.729290062451,131.228977275493,
131.728664488535,132.228351701576,132.728038914618,133.22772612766,133.727413340701,
134.227100553743,134.726787766785,135.088484104361),.UNSPECIFIED.);
#3183=B_SPLINE_CURVE_WITH_KNOTS('',3,(#54229,#54230,#54231,#54232,#54233,
#54234,#54235,#54236,#54237,#54238,#54239,#54240,#54241,#54242,#54243,#54244,
#54245),.UNSPECIFIED.,.F.,.F.,(4,1,1,1,1,1,1,1,1,1,1,1,1,1,4),(122.522113490002,
122.545982814371,123.045670027412,123.545357240454,124.045044453496,124.544731666538,
125.044418879579,125.544106092621,126.043793305663,126.543480518704,127.043167731746,
127.542854944788,128.04254215783,128.542229370871,128.805298797182),
 .UNSPECIFIED.);
#3184=B_SPLINE_CURVE_WITH_KNOTS('',3,(#54246,#54247,#54248,#54249,#54250,
#54251,#54252,#54253,#54254,#54255,#54256,#54257,#54258,#54259,#54260,#54261,
#54262),.UNSPECIFIED.,.F.,.F.,(4,1,1,1,1,1,1,1,1,1,1,1,1,1,4),(122.522113490002,
122.734294653784,123.233981866825,123.733669079867,124.233356292909,124.733043505951,
125.232730718992,125.732417932034,126.232105145076,126.731792358117,127.231479571159,
127.731166784201,128.230853997243,128.730541210284,128.805298797182),
 .UNSPECIFIED.);
#3185=B_SPLINE_CURVE_WITH_KNOTS('',3,(#54267,#54268,#54269,#54270,#54271,
#54272,#54273,#54274,#54275,#54276,#54277,#54278,#54279,#54280,#54281,#54282),
 .UNSPECIFIED.,.F.,.F.,(4,1,1,1,1,1,1,1,1,1,1,1,1,4),(116.238928182823,
116.54973625787,117.049423470912,117.549110683954,118.048797896995,118.548485110037,
119.048172323079,119.54785953612,120.047546749162,120.547233962204,121.046921175246,
121.546608388287,122.046295601329,122.522113490002),.UNSPECIFIED.);
#3186=B_SPLINE_CURVE_WITH_KNOTS('',3,(#54283,#54284,#54285,#54286,#54287,
#54288,#54289,#54290,#54291,#54292,#54293,#54294,#54295,#54296,#54297,#54298),
 .UNSPECIFIED.,.F.,.F.,(4,1,1,1,1,1,1,1,1,1,1,1,1,4),(116.238928182823,
116.738048097283,117.237735310325,117.737422523367,118.237109736408,118.73679694945,
119.236484162492,119.736171375533,120.235858588575,120.735545801617,121.235233014659,
121.7349202277,122.234607440742,122.522113490002),.UNSPECIFIED.);
#3187=B_SPLINE_CURVE_WITH_KNOTS('',3,(#54303,#54304,#54305,#54306,#54307,
#54308,#54309,#54310,#54311,#54312,#54313,#54314,#54315,#54316,#54317,#54318,
#54319),.UNSPECIFIED.,.F.,.F.,(4,1,1,1,1,1,1,1,1,1,1,1,1,1,4),(109.955742875643,
110.053802488328,110.55348970137,111.053176914411,111.552864127453,112.052551340495,
112.552238553537,113.051925766578,113.55161297962,114.051300192662,114.550987405703,
115.050674618745,115.550361831787,116.050049044828,116.238928182823),
 .UNSPECIFIED.);
#3188=B_SPLINE_CURVE_WITH_KNOTS('',3,(#54320,#54321,#54322,#54323,#54324,
#54325,#54326,#54327,#54328,#54329,#54330,#54331,#54332,#54333,#54334,#54335,
#54336),.UNSPECIFIED.,.F.,.F.,(4,1,1,1,1,1,1,1,1,1,1,1,1,1,4),(109.955742875643,
110.242114327741,110.741801540783,111.241488753824,111.741175966866,112.240863179908,
112.74055039295,113.240237605991,113.739924819033,114.239612032075,114.739299245116,
115.238986458158,115.7386736712,116.238360884242,116.238928182823),
 .UNSPECIFIED.);
#3189=B_SPLINE_CURVE_WITH_KNOTS('',3,(#54341,#54342,#54343,#54344,#54345,
#54346,#54347,#54348,#54349,#54350,#54351,#54352,#54353,#54354,#54355,#54356),
 .UNSPECIFIED.,.F.,.F.,(4,1,1,1,1,1,1,1,1,1,1,1,1,4),(103.672557568463,
104.057555931827,104.557243144869,105.056930357911,105.556617570953,106.056304783994,
106.555991997036,107.055679210078,107.555366423119,108.055053636161,108.554740849203,
109.054428062245,109.554115275286,109.955742875643),.UNSPECIFIED.);
#3190=B_SPLINE_CURVE_WITH_KNOTS('',3,(#54357,#54358,#54359,#54360,#54361,
#54362,#54363,#54364,#54365,#54366,#54367,#54368,#54369,#54370,#54371,#54372,
#54373),.UNSPECIFIED.,.F.,.F.,(4,1,1,1,1,1,1,1,1,1,1,1,1,1,4),(103.672557568464,
103.746180558199,104.24586777124,104.745554984282,105.245242197324,105.744929410366,
106.244616623407,106.744303836449,107.243991049491,107.743678262532,108.243365475574,
108.743052688616,109.242739901658,109.742427114699,109.955742875643),
 .UNSPECIFIED.);
#3191=B_SPLINE_CURVE_WITH_KNOTS('',3,(#54378,#54379,#54380,#54381,#54382,
#54383,#54384,#54385,#54386,#54387,#54388,#54389,#54390,#54391,#54392,#54393,
#54394),.UNSPECIFIED.,.F.,.F.,(4,1,1,1,1,1,1,1,1,1,1,1,1,1,4),(97.3893722612838,
97.5616221622852,98.0613093753269,98.5609965883686,99.0606838014103,99.560371014452,
100.060058227494,100.559745440535,101.059432653577,101.559119866619,102.058807079661,
102.558494292702,103.058181505744,103.557868718786,103.672557568463),
 .UNSPECIFIED.);
#3192=B_SPLINE_CURVE_WITH_KNOTS('',3,(#54395,#54396,#54397,#54398,#54399,
#54400,#54401,#54402,#54403,#54404,#54405,#54406,#54407,#54408,#54409,#54410),
 .UNSPECIFIED.,.F.,.F.,(4,1,1,1,1,1,1,1,1,1,1,1,1,4),(97.3893722612839,
97.7499340016982,98.2496212147399,98.7493084277816,99.2489956408234,99.7486828538651,
100.248370066907,100.748057279948,101.24774449299,101.747431706032,102.247118919074,
102.746806132115,103.246493345157,103.672557568464),.UNSPECIFIED.);
#3193=B_SPLINE_CURVE_WITH_KNOTS('',3,(#54415,#54416,#54417,#54418,#54419,
#54420,#54421,#54422,#54423,#54424,#54425,#54426,#54427,#54428,#54429,#54430),
 .UNSPECIFIED.,.F.,.F.,(4,1,1,1,1,1,1,1,1,1,1,1,1,4),(91.1061869541043,
91.5653756057847,92.0650628188264,92.5647500318681,93.0644372449098,93.5641244579515,
94.0638116709932,94.5634988840349,95.0631860970766,95.5628733101183,96.06256052316,
96.5622477362018,97.0619349492435,97.3893722612838),.UNSPECIFIED.);
#3194=B_SPLINE_CURVE_WITH_KNOTS('',3,(#54431,#54432,#54433,#54434,#54435,
#54436,#54437,#54438,#54439,#54440,#54441,#54442,#54443,#54444,#54445,#54446,
#54447),.UNSPECIFIED.,.F.,.F.,(4,1,1,1,1,1,1,1,1,1,1,1,1,1,4),(91.1061869541043,
91.254000232156,91.7536874451977,92.2533746582394,92.7530618712811,93.2527490843228,
93.7524362973645,94.2521235104062,94.7518107234479,95.2514979364897,95.7511851495314,
96.2508723625731,96.7505595756148,97.2502467886565,97.3893722612839),
 .UNSPECIFIED.);
#3195=B_SPLINE_CURVE_WITH_KNOTS('',3,(#54452,#54453,#54454,#54455,#54456,
#54457,#54458,#54459,#54460,#54461,#54462,#54463,#54464,#54465,#54466,#54467,
#54468),.UNSPECIFIED.,.F.,.F.,(4,1,1,1,1,1,1,1,1,1,1,1,1,1,4),(84.8230016469247,
85.0694418362424,85.5691290492841,86.0688162623258,86.5685034753675,87.0681906884093,
87.567877901451,88.0675651144927,88.5672523275344,89.0669395405761,89.5666267536178,
90.0663139666595,90.5660011797012,91.0656883927429,91.1061869541043),
 .UNSPECIFIED.);
#3196=B_SPLINE_CURVE_WITH_KNOTS('',3,(#54469,#54470,#54471,#54472,#54473,
#54474,#54475,#54476,#54477,#54478,#54479,#54480,#54481,#54482,#54483,#54484),
 .UNSPECIFIED.,.F.,.F.,(4,1,1,1,1,1,1,1,1,1,1,1,1,4),(84.8230016469247,
85.2577536756554,85.7574408886971,86.2571281017389,86.7568153147806,87.2565025278223,
87.756189740864,88.2558769539057,88.7555641669474,89.2552513799891,89.7549385930308,
90.2546258060726,90.7543130191143,91.1061869541043),.UNSPECIFIED.);
#3197=B_SPLINE_CURVE_WITH_KNOTS('',3,(#54489,#54490,#54491,#54492,#54493,
#54494,#54495,#54496,#54497,#54498,#54499,#54500,#54501,#54502,#54503,#54504,
#54505),.UNSPECIFIED.,.F.,.F.,(4,1,1,1,1,1,1,1,1,1,1,1,1,1,4),(78.5398163397451,
78.5735080667002,79.0731952797419,79.5728824927836,80.0725697058253,80.572256918867,
81.0719441319087,81.5716313449504,82.0713185579921,82.5710057710339,83.0706929840756,
83.5703801971173,84.070067410159,84.5697546232007,84.8230016469247),
 .UNSPECIFIED.);
#3198=B_SPLINE_CURVE_WITH_KNOTS('',3,(#54506,#54507,#54508,#54509,#54510,
#54511,#54512,#54513,#54514,#54515,#54516,#54517,#54518,#54519,#54520,#54521,
#54522),.UNSPECIFIED.,.F.,.F.,(4,1,1,1,1,1,1,1,1,1,1,1,1,1,4),(78.5398163397451,
78.7618199061132,79.2615071191549,79.7611943321966,80.2608815452383,80.76056875828,
81.2602559713218,81.7599431843635,82.2596303974052,82.7593176104469,83.2590048234886,
83.7586920365303,84.258379249572,84.7580664626137,84.8230016469247),
 .UNSPECIFIED.);
#3199=B_SPLINE_CURVE_WITH_KNOTS('',3,(#54527,#54528,#54529,#54530,#54531,
#54532,#54533,#54534,#54535,#54536,#54537,#54538,#54539,#54540,#54541,#54542),
 .UNSPECIFIED.,.F.,.F.,(4,1,1,1,1,1,1,1,1,1,1,1,1,4),(72.2566310325655,
72.5772615101996,73.0769487232413,73.5766359362831,74.0763231493248,74.5760103623665,
75.0756975754082,75.5753847884499,76.0750720014916,76.5747592145333,77.074446427575,
77.5741336406168,78.0738208536585,78.5398163397451),.UNSPECIFIED.);
#3200=B_SPLINE_CURVE_WITH_KNOTS('',3,(#54543,#54544,#54545,#54546,#54547,
#54548,#54549,#54550,#54551,#54552,#54553,#54554,#54555,#54556,#54557,#54558,
#54559),.UNSPECIFIED.,.F.,.F.,(4,1,1,1,1,1,1,1,1,1,1,1,1,1,4),(72.2566310325655,
72.265886136571,72.7655733496127,73.2652605626544,73.7649477756961,74.2646349887378,
74.7643222017795,75.2640094148212,75.7636966278629,76.2633838409046,76.7630710539463,
77.2627582669881,77.7624454800298,78.2621326930715,78.5398163397451),
 .UNSPECIFIED.);
#3201=B_SPLINE_CURVE_WITH_KNOTS('',3,(#54564,#54565,#54566,#54567,#54568,
#54569,#54570,#54571,#54572,#54573,#54574,#54575,#54576,#54577,#54578,#54579,
#54580),.UNSPECIFIED.,.F.,.F.,(4,1,1,1,1,1,1,1,1,1,1,1,1,1,4),(65.9734457253859,
66.0813277406574,66.5810149536991,67.0807021667408,67.5803893797825,68.0800765928242,
68.579763805866,69.0794510189077,69.5791382319494,70.0788254449911,70.5785126580328,
71.0781998710745,71.5778870841162,72.0775742971579,72.2566310325655),
 .UNSPECIFIED.);
#3202=B_SPLINE_CURVE_WITH_KNOTS('',3,(#54581,#54582,#54583,#54584,#54585,
#54586,#54587,#54588,#54589,#54590,#54591,#54592,#54593,#54594,#54595,#54596),
 .UNSPECIFIED.,.F.,.F.,(4,1,1,1,1,1,1,1,1,1,1,1,1,4),(65.9734457253859,
66.2696395800704,66.7693267931121,67.2690140061538,67.7687012191955,68.2683884322373,
68.768075645279,69.2677628583207,69.7674500713624,70.2671372844041,70.7668244974458,
71.2665117104875,71.7661989235292,72.2566310325655),.UNSPECIFIED.);
#3203=B_SPLINE_CURVE_WITH_KNOTS('',3,(#54601,#54602,#54603,#54604,#54605,
#54606,#54607,#54608,#54609,#54610,#54611,#54612,#54613,#54614,#54615,#54616),
 .UNSPECIFIED.,.F.,.F.,(4,1,1,1,1,1,1,1,1,1,1,1,1,4),(59.6902604182063,
60.0850811841569,60.5847683971986,61.0844556102403,61.584142823282,62.0838300363237,
62.5835172493654,63.0832044624071,63.5828916754488,64.0825788884906,64.5822661015323,
65.081953314574,65.5816405276157,65.9734457253859),.UNSPECIFIED.);
#3204=B_SPLINE_CURVE_WITH_KNOTS('',3,(#54617,#54618,#54619,#54620,#54621,
#54622,#54623,#54624,#54625,#54626,#54627,#54628,#54629,#54630,#54631,#54632,
#54633),.UNSPECIFIED.,.F.,.F.,(4,1,1,1,1,1,1,1,1,1,1,1,1,1,4),(59.6902604182063,
59.7737058105282,60.2733930235699,60.7730802366116,61.2727674496533,61.772454662695,
62.2721418757367,62.7718290887784,63.2715163018202,63.7712035148619,64.2708907279036,
64.7705779409453,65.270265153987,65.7699523670287,65.9734457253859),
 .UNSPECIFIED.);
#3205=B_SPLINE_CURVE_WITH_KNOTS('',3,(#54638,#54639,#54640,#54641,#54642,
#54643,#54644,#54645,#54646,#54647,#54648,#54649,#54650,#54651,#54652,#54653,
#54654),.UNSPECIFIED.,.F.,.F.,(4,1,1,1,1,1,1,1,1,1,1,1,1,1,4),(53.4070751110267,
53.5891474146146,54.0888346276563,54.588521840698,55.0882090537398,55.5878962667815,
56.0875834798232,56.5872706928649,57.0869579059066,57.5866451189483,58.08633233199,
58.5860195450317,59.0857067580734,59.5853939711152,59.6902604182063),
 .UNSPECIFIED.);
#3206=B_SPLINE_CURVE_WITH_KNOTS('',3,(#54655,#54656,#54657,#54658,#54659,
#54660,#54661,#54662,#54663,#54664,#54665,#54666,#54667,#54668,#54669,#54670),
 .UNSPECIFIED.,.F.,.F.,(4,1,1,1,1,1,1,1,1,1,1,1,1,4),(53.4070751110268,
53.7774592540276,54.2771464670694,54.7768336801111,55.2765208931528,55.7762081061945,
56.2758953192362,56.7755825322779,57.2752697453196,57.7749569583613,58.274644171403,
58.7743313844448,59.2740185974865,59.6902604182063),.UNSPECIFIED.);
#3207=B_SPLINE_CURVE_WITH_KNOTS('',3,(#54675,#54676,#54677,#54678,#54679,
#54680,#54681,#54682,#54683,#54684,#54685,#54686,#54687,#54688,#54689,#54690),
 .UNSPECIFIED.,.F.,.F.,(4,1,1,1,1,1,1,1,1,1,1,1,1,4),(47.1238898038471,
47.5929008581141,48.0925880711558,48.5922752841975,49.0919624972392,49.5916497102809,
50.0913369233227,50.5910241363644,51.0907113494061,51.5903985624478,52.0900857754895,
52.5897729885312,53.0894602015729,53.4070751110267),.UNSPECIFIED.);
#3208=B_SPLINE_CURVE_WITH_KNOTS('',3,(#54691,#54692,#54693,#54694,#54695,
#54696,#54697,#54698,#54699,#54700,#54701,#54702,#54703,#54704,#54705,#54706,
#54707),.UNSPECIFIED.,.F.,.F.,(4,1,1,1,1,1,1,1,1,1,1,1,1,1,4),(47.1238898038472,
47.2815254844854,47.7812126975271,48.2808999105688,48.7805871236105,49.2802743366523,
49.779961549694,50.2796487627357,50.7793359757774,51.2790231888191,51.7787104018608,
52.2783976149025,52.7780848279442,53.2777720409859,53.4070751110268),
 .UNSPECIFIED.);
#3209=B_SPLINE_CURVE_WITH_KNOTS('',3,(#54712,#54713,#54714,#54715,#54716,
#54717,#54718,#54719,#54720,#54721,#54722,#54723,#54724,#54725,#54726,#54727,
#54728),.UNSPECIFIED.,.F.,.F.,(4,1,1,1,1,1,1,1,1,1,1,1,1,1,4),(40.8407044966675,
41.0969670885719,41.5966543016136,42.0963415146553,42.596028727697,43.0957159407387,
43.5954031537804,44.0950903668221,44.5947775798638,45.0944647929055,45.5941520059473,
46.093839218989,46.5935264320307,47.0932136450724,47.1238898038471),
 .UNSPECIFIED.);
#3210=B_SPLINE_CURVE_WITH_KNOTS('',3,(#54729,#54730,#54731,#54732,#54733,
#54734,#54735,#54736,#54737,#54738,#54739,#54740,#54741,#54742,#54743,#54744),
 .UNSPECIFIED.,.F.,.F.,(4,1,1,1,1,1,1,1,1,1,1,1,1,4),(40.8407044966676,
41.2852789279849,41.7849661410266,42.2846533540683,42.78434056711,43.2840277801517,
43.7837149931934,44.2834022062351,44.7830894192769,45.2827766323186,45.7824638453603,
46.282151058402,46.7818382714437,47.1238898038472),.UNSPECIFIED.);
#3211=B_SPLINE_CURVE_WITH_KNOTS('',3,(#54749,#54750,#54751,#54752,#54753,
#54754,#54755,#54756,#54757,#54758,#54759,#54760,#54761,#54762,#54763,#54764,
#54765),.UNSPECIFIED.,.F.,.F.,(4,1,1,1,1,1,1,1,1,1,1,1,1,1,4),(34.5575191894879,
34.6010333190296,35.1007205320713,35.600407745113,36.1000949581547,36.5997821711965,
37.0994693842382,37.5991565972799,38.0988438103216,38.5985310233633,39.098218236405,
39.5979054494467,40.0975926624884,40.5972798755301,40.8407044966675),
 .UNSPECIFIED.);
#3212=B_SPLINE_CURVE_WITH_KNOTS('',3,(#54766,#54767,#54768,#54769,#54770,
#54771,#54772,#54773,#54774,#54775,#54776,#54777,#54778,#54779,#54780,#54781,
#54782),.UNSPECIFIED.,.F.,.F.,(4,1,1,1,1,1,1,1,1,1,1,1,1,1,4),(34.557519189488,
34.7893451584426,35.2890323714843,35.7887195845261,36.2884067975678,36.7880940106095,
37.2877812236512,37.7874684366929,38.2871556497346,38.7868428627763,39.286530075818,
39.7862172888597,40.2859045019015,40.7855917149432,40.8407044966676),
 .UNSPECIFIED.);
#3213=B_SPLINE_CURVE_WITH_KNOTS('',3,(#54787,#54788,#54789,#54790,#54791,
#54792,#54793,#54794,#54795,#54796,#54797,#54798,#54799,#54800,#54801,#54802),
 .UNSPECIFIED.,.F.,.F.,(4,1,1,1,1,1,1,1,1,1,1,1,1,4),(28.2743338823083,
28.6047867625291,29.1044739755708,29.6041611886125,30.1038484016542,30.6035356146959,
31.1032228277376,31.6029100407793,32.1025972538211,32.6022844668628,33.1019716799045,
33.6016588929462,34.1013461059879,34.5575191894879),.UNSPECIFIED.);
#3214=B_SPLINE_CURVE_WITH_KNOTS('',3,(#54803,#54804,#54805,#54806,#54807,
#54808,#54809,#54810,#54811,#54812,#54813,#54814,#54815,#54816,#54817,#54818,
#54819),.UNSPECIFIED.,.F.,.F.,(4,1,1,1,1,1,1,1,1,1,1,1,1,1,4),(28.2743338823084,
28.2934113889004,28.7930986019421,29.2927858149838,29.7924730280255,30.2921602410672,
30.7918474541089,31.2915346671507,31.7912218801924,32.2909090932341,32.7905963062758,
33.2902835193175,33.7899707323592,34.2896579454009,34.557519189488),
 .UNSPECIFIED.);
#3215=B_SPLINE_CURVE_WITH_KNOTS('',3,(#54824,#54825,#54826,#54827,#54828,
#54829,#54830,#54831,#54832,#54833,#54834,#54835,#54836,#54837,#54838,#54839,
#54840),.UNSPECIFIED.,.F.,.F.,(4,1,1,1,1,1,1,1,1,1,1,1,1,1,4),(21.9911485751287,
22.1088529929868,22.6085402060286,23.1082274190703,23.607914632112,24.1076018451537,
24.6072890581954,25.1069762712371,25.6066634842788,26.1063506973205,26.6060379103622,
27.1057251234039,27.6054123364457,28.1050995494874,28.2743338823083),
 .UNSPECIFIED.);
#3216=B_SPLINE_CURVE_WITH_KNOTS('',3,(#54841,#54842,#54843,#54844,#54845,
#54846,#54847,#54848,#54849,#54850,#54851,#54852,#54853,#54854,#54855,#54856),
 .UNSPECIFIED.,.F.,.F.,(4,1,1,1,1,1,1,1,1,1,1,1,1,4),(21.9911485751288,
22.2971648323999,22.7968520454416,23.2965392584833,23.796226471525,24.2959136845667,
24.7956008976084,25.2952881106501,25.7949753236918,26.2946625367335,26.7943497497753,
27.294036962817,27.7937241758587,28.2743338823084),.UNSPECIFIED.);
#3217=B_SPLINE_CURVE_WITH_KNOTS('',3,(#54861,#54862,#54863,#54864,#54865,
#54866,#54867,#54868,#54869,#54870,#54871,#54872,#54873,#54874,#54875,#54876),
 .UNSPECIFIED.,.F.,.F.,(4,1,1,1,1,1,1,1,1,1,1,1,1,4),(15.7079632679492,
16.1126064364863,16.612293649528,17.1119808625697,17.6116680756114,18.1113552886532,
18.6110425016949,19.1107297147366,19.6104169277783,20.11010414082,20.6097913538617,
21.1094785669034,21.6091657799451,21.9911485751287),.UNSPECIFIED.);
#3218=B_SPLINE_CURVE_WITH_KNOTS('',3,(#54877,#54878,#54879,#54880,#54881,
#54882,#54883,#54884,#54885,#54886,#54887,#54888,#54889,#54890,#54891,#54892,
#54893),.UNSPECIFIED.,.F.,.F.,(4,1,1,1,1,1,1,1,1,1,1,1,1,1,4),(15.7079632679492,
15.8012310628576,16.3009182758993,16.800605488941,17.3002927019828,17.7999799150245,
18.2996671280662,18.7993543411079,19.2990415541496,19.7987287671913,20.298415980233,
20.7981031932747,21.2977904063164,21.7974776193581,21.9911485751288),
 .UNSPECIFIED.);
#3219=B_SPLINE_CURVE_WITH_KNOTS('',3,(#54946,#54947,#54948,#54949,#54950,
#54951,#54952,#54953,#54954,#54955,#54956,#54957,#54958,#54959,#54960,#54961,
#54962,#54963,#54964,#54965,#54966,#54967,#54968,#54969,#54970,#54971,#54972,
#54973,#54974,#54975,#54976,#54977,#54978,#54979,#54980,#54981,#54982,#54983,
#54984,#54985,#54986,#54987,#54988,#54989,#54990,#54991,#54992,#54993,#54994,
#54995,#54996,#54997,#54998,#54999,#55000,#55001,#55002,#55003,#55004,#55005,
#55006,#55007,#55008,#55009,#55010,#55011,#55012,#55013,#55014,#55015,#55016,
#55017,#55018,#55019,#55020,#55021,#55022,#55023,#55024,#55025,#55026,#55027,
#55028,#55029,#55030,#55031,#55032,#55033,#55034,#55035,#55036,#55037,#55038,
#55039,#55040,#55041,#55042,#55043,#55044,#55045,#55046,#55047,#55048,#55049,
#55050,#55051,#55052,#55053,#55054,#55055,#55056,#55057),.UNSPECIFIED.,
 .F.,.F.,(4,3,3,3,3,3,3,3,3,3,3,3,3,3,3,3,3,3,3,3,3,3,3,3,3,3,3,3,3,3,3,
3,3,3,3,3,3,4),(-1.13094109509802,-1.09555301847653,-1.05191077246943,-1.02403062395787,
-1.00813854529478,-1.00052830557018,-0.993876160984945,-0.949033314345626,
-0.903913416286832,-0.871831333015361,-0.865263807587487,-0.858234145025541,
-0.839749249743891,-0.794775856894288,-0.749099847114423,-0.702998994975979,
-0.67015530307118,-0.65938726757389,-0.653338187751441,-0.606207711122551,
-0.571624227356783,-0.52477896769309,-0.4775450680471,-0.45430610006491,
-0.447310014249259,-0.440818772196958,-0.392835159315427,-0.342234241752502,
-0.291633324189578,-0.255179158665881,-0.239230461249263,-0.229162927859656,
-0.222808275366792,-0.174282107380972,-0.12474438340666,-0.0750152592867178,
-0.0256716031603919,0.),.UNSPECIFIED.);
#3220=B_SPLINE_CURVE_WITH_KNOTS('',3,(#55058,#55059,#55060,#55061,#55062,
#55063,#55064,#55065,#55066,#55067,#55068,#55069,#55070,#55071,#55072,#55073,
#55074,#55075,#55076,#55077,#55078,#55079,#55080,#55081,#55082,#55083,#55084,
#55085,#55086,#55087,#55088,#55089,#55090,#55091,#55092,#55093,#55094,#55095,
#55096,#55097,#55098,#55099,#55100,#55101,#55102,#55103,#55104,#55105,#55106,
#55107,#55108,#55109,#55110,#55111,#55112,#55113,#55114,#55115,#55116,#55117,
#55118,#55119,#55120,#55121,#55122,#55123,#55124,#55125,#55126,#55127,#55128,
#55129,#55130,#55131,#55132,#55133,#55134,#55135,#55136,#55137,#55138,#55139,
#55140,#55141,#55142,#55143,#55144,#55145,#55146,#55147,#55148,#55149,#55150,
#55151,#55152,#55153,#55154,#55155,#55156,#55157,#55158,#55159,#55160,#55161,
#55162,#55163,#55164,#55165,#55166),.UNSPECIFIED.,.F.,.F.,(4,3,3,3,3,3,
3,3,3,3,3,3,3,3,3,3,3,3,3,3,3,3,3,3,3,3,3,3,3,3,3,3,3,3,3,3,4),(-1.12653966532771,
-1.08458299748631,-1.03483149315989,-0.985279599381992,-0.975815498433229,
-0.967599728292632,-0.918737646949452,-0.870231088088996,-0.833191367947055,
-0.824932489274649,-0.81718932838954,-0.796151647805113,-0.748401850681541,
-0.700478100468338,-0.653200435706217,-0.619650854833934,-0.606444877375552,
-0.599947690904268,-0.553426660564813,-0.519002112217086,-0.472281839936397,
-0.425888913622091,-0.404346747613177,-0.397440927235775,-0.39106097225247,
-0.345595566799898,-0.299573576175339,-0.253551585550779,-0.221857637356932,
-0.205368177310387,-0.194980811358931,-0.189035396833246,-0.144860126169755,
-0.100702737474855,-0.0569688291873824,-0.0141848851110983,0.),
 .UNSPECIFIED.);
#3221=B_SPLINE_CURVE_WITH_KNOTS('',3,(#57035,#57036,#57037,#57038,#57039,
#57040,#57041,#57042,#57043,#57044,#57045,#57046,#57047,#57048,#57049,#57050,
#57051,#57052,#57053,#57054,#57055,#57056,#57057,#57058,#57059,#57060,#57061,
#57062,#57063,#57064,#57065,#57066,#57067,#57068,#57069,#57070,#57071,#57072,
#57073,#57074),.UNSPECIFIED.,.F.,.F.,(4,3,3,3,3,3,3,3,3,3,3,3,3,4),(221.030340844823,
221.361435377478,221.86112259052,222.360809803561,222.860497016603,223.360184229645,
223.859871442686,224.359558655728,224.85924586877,225.358933081812,225.858620294853,
226.358307507895,226.857994720937,227.313526152003),.UNSPECIFIED.);
#3222=B_SPLINE_CURVE_WITH_KNOTS('',3,(#57076,#57077,#57078,#57079,#57080,
#57081,#57082,#57083,#57084,#57085,#57086,#57087,#57088,#57089,#57090,#57091,
#57092,#57093,#57094,#57095,#57096,#57097,#57098,#57099,#57100,#57101,#57102,
#57103,#57104,#57105,#57106,#57107,#57108,#57109,#57110,#57111,#57112,#57113,
#57114,#57115,#57116,#57117,#57118,#57119,#57120,#57121,#57122,#57123,#57124,
#57125,#57126,#57127,#57128,#57129,#57130,#57131,#57132,#57133,#57134,#57135,
#57136,#57137,#57138,#57139,#57140,#57141,#57142,#57143,#57144,#57145,#57146,
#57147,#57148,#57149,#57150,#57151,#57152,#57153,#57154,#57155,#57156,#57157,
#57158,#57159,#57160,#57161,#57162,#57163,#57164,#57165,#57166,#57167,#57168,
#57169,#57170,#57171,#57172,#57173,#57174,#57175,#57176,#57177,#57178,#57179,
#57180,#57181),.UNSPECIFIED.,.F.,.F.,(4,3,3,3,3,3,3,3,3,3,3,3,3,3,3,3,3,
3,3,3,3,3,3,3,3,3,3,3,3,3,3,3,3,3,3,4),(0.,0.0352857241728138,0.0785968005211441,
0.122543680878482,0.164561866032942,0.181925963986356,0.191292943908678,
0.198769809597266,0.244693115546795,0.290616421496325,0.335746406070846,
0.381175755521027,0.394700494941097,0.400587470417484,0.446722411686962,
0.493312170072264,0.539988246407058,0.557729506053438,0.592565372786847,
0.602152221655606,0.609811280274756,0.656489736582357,0.704212096377392,
0.7521337137357,0.794275076828207,0.81534575837446,0.822329730595576,0.836416439920714,
0.88442476768464,0.933058731823078,0.957243848511161,0.968294021888866,
0.977747896967412,1.02724813744154,1.07696146625084,1.12653966532774),
 .UNSPECIFIED.);
#3223=B_SPLINE_CURVE_WITH_KNOTS('',3,(#57182,#57183,#57184,#57185,#57186,
#57187,#57188,#57189,#57190,#57191,#57192,#57193,#57194,#57195),
 .UNSPECIFIED.,.F.,.F.,(4,1,1,1,1,1,1,1,1,1,1,4),(10.3757270560181,10.8043589324405,
11.3040461454822,11.8037333585239,12.3034205715656,12.8031077846074,13.3027949976491,
13.8024822106908,14.3021694237325,14.8018566367742,15.3015438498159,15.7079632679492),
 .UNSPECIFIED.);
#3224=B_SPLINE_CURVE_WITH_KNOTS('',3,(#57199,#57200,#57201,#57202,#57203,
#57204,#57205,#57206,#57207,#57208,#57209,#57210),.UNSPECIFIED.,.F.,.F.,
(4,1,1,1,1,1,1,1,1,4),(11.6154215191109,12.1151087321526,12.6147959451943,
13.114483158236,13.6141703712778,14.1138575843195,14.6135447973612,15.1132320104029,
15.6129192234446,15.7079632679492),.UNSPECIFIED.);
#3225=B_SPLINE_CURVE_WITH_KNOTS('',3,(#59079,#59080,#59081,#59082,#59083,
#59084,#59085,#59086,#59087,#59088,#59089,#59090,#59091,#59092,#59093,#59094,
#59095,#59096,#59097,#59098,#59099,#59100,#59101,#59102,#59103,#59104,#59105,
#59106,#59107,#59108,#59109,#59110,#59111,#59112,#59113,#59114,#59115,#59116,
#59117,#59118,#59119,#59120,#59121,#59122,#59123,#59124,#59125,#59126,#59127,
#59128,#59129,#59130,#59131,#59132,#59133,#59134,#59135,#59136,#59137,#59138,
#59139,#59140,#59141,#59142,#59143,#59144,#59145,#59146,#59147,#59148,#59149,
#59150,#59151,#59152,#59153,#59154,#59155,#59156,#59157,#59158,#59159,#59160,
#59161,#59162,#59163,#59164,#59165,#59166,#59167,#59168,#59169,#59170,#59171,
#59172,#59173,#59174,#59175,#59176,#59177,#59178,#59179,#59180,#59181,#59182,
#59183,#59184),.UNSPECIFIED.,.F.,.F.,(4,3,3,3,3,3,3,3,3,3,3,3,3,3,3,3,3,
3,3,3,3,3,3,3,3,3,3,3,3,3,3,3,3,3,3,4),(0.,0.0421292382714313,0.091750200305321,
0.141456976711247,0.189144780929015,0.226472585797489,0.232898121965279,
0.282553157773798,0.332208193582317,0.380717833282778,0.4288180329463,0.441643201872779,
0.447579677179949,0.494878310127159,0.542047678686319,0.58849366827198,
0.610502777243903,0.643793248697581,0.654127499556154,0.660011487124506,
0.705941659246836,0.75196767154723,0.797593194966215,0.83720987191977,0.857018210396548,
0.863932831637979,0.870762041059155,0.876826548873325,0.921927000756489,
0.966986484162723,0.987480810529615,0.996684100011213,1.00397890643578,
1.04815620422644,1.09160411182441,1.13094109509786),.UNSPECIFIED.);
#3226=B_SPLINE_CURVE_WITH_KNOTS('',3,(#59185,#59186,#59187,#59188,#59189,
#59190,#59191,#59192,#59193,#59194,#59195,#59196,#59197,#59198,#59199,#59200,
#59201,#59202,#59203,#59204,#59205,#59206,#59207,#59208,#59209,#59210,#59211,
#59212,#59213,#59214,#59215,#59216,#59217,#59218,#59219,#59220,#59221,#59222,
#59223,#59224),.UNSPECIFIED.,.F.,.F.,(4,3,3,3,3,3,3,3,3,3,3,3,3,4),(-230.287212807303,
-229.856117999187,-229.356430786145,-228.856743573104,-228.357056360062,
-227.85736914702,-227.357681933978,-226.857994720937,-226.358307507895,
-225.858620294853,-225.358933081812,-224.85924586877,-224.359558655728,
-224.004027500124),.UNSPECIFIED.);
#4083=LINE('',#50428,#4931);
#4084=LINE('',#50461,#4932);
#4085=LINE('',#50545,#4933);
#4086=LINE('',#50635,#4934);
#4087=LINE('',#50719,#4935);
#4088=LINE('',#50809,#4936);
#4089=LINE('',#50899,#4937);
#4090=LINE('',#50983,#4938);
#4091=LINE('',#51073,#4939);
#4092=LINE('',#51157,#4940);
#4093=LINE('',#51247,#4941);
#4094=LINE('',#51331,#4942);
#4095=LINE('',#51421,#4943);
#4096=LINE('',#51511,#4944);
#4097=LINE('',#51595,#4945);
#4098=LINE('',#51685,#4946);
#4099=LINE('',#51769,#4947);
#4100=LINE('',#51859,#4948);
#4101=LINE('',#51943,#4949);
#4102=LINE('',#52030,#4950);
#4103=LINE('',#52120,#4951);
#4104=LINE('',#52204,#4952);
#4105=LINE('',#52294,#4953);
#4106=LINE('',#52378,#4954);
#4107=LINE('',#52468,#4955);
#4108=LINE('',#52555,#4956);
#4109=LINE('',#52642,#4957);
#4110=LINE('',#52732,#4958);
#4111=LINE('',#52816,#4959);
#4112=LINE('',#52906,#4960);
#4113=LINE('',#52990,#4961);
#4114=LINE('',#53080,#4962);
#4115=LINE('',#53167,#4963);
#4116=LINE('',#53254,#4964);
#4117=LINE('',#53344,#4965);
#4118=LINE('',#53428,#4966);
#4119=LINE('',#53519,#4967);
#4120=LINE('',#53537,#4968);
#4121=LINE('',#53562,#4969);
#4122=LINE('',#53597,#4970);
#4123=LINE('',#53634,#4971);
#4124=LINE('',#53671,#4972);
#4125=LINE('',#53708,#4973);
#4126=LINE('',#53746,#4974);
#4127=LINE('',#53782,#4975);
#4128=LINE('',#53820,#4976);
#4129=LINE('',#53857,#4977);
#4130=LINE('',#53894,#4978);
#4131=LINE('',#53931,#4979);
#4132=LINE('',#53968,#4980);
#4133=LINE('',#54006,#4981);
#4134=LINE('',#54042,#4982);
#4135=LINE('',#54080,#4983);
#4136=LINE('',#54117,#4984);
#4137=LINE('',#54154,#4985);
#4138=LINE('',#54191,#4986);
#4139=LINE('',#54228,#4987);
#4140=LINE('',#54266,#4988);
#4141=LINE('',#54302,#4989);
#4142=LINE('',#54340,#4990);
#4143=LINE('',#54377,#4991);
#4144=LINE('',#54414,#4992);
#4145=LINE('',#54451,#4993);
#4146=LINE('',#54488,#4994);
#4147=LINE('',#54526,#4995);
#4148=LINE('',#54563,#4996);
#4149=LINE('',#54600,#4997);
#4150=LINE('',#54637,#4998);
#4151=LINE('',#54674,#4999);
#4152=LINE('',#54711,#5000);
#4153=LINE('',#54748,#5001);
#4154=LINE('',#54786,#5002);
#4155=LINE('',#54823,#5003);
#4156=LINE('',#54860,#5004);
#4157=LINE('',#54897,#5005);
#4158=LINE('',#54899,#5006);
#4159=LINE('',#54901,#5007);
#4160=LINE('',#54902,#5008);
#4161=LINE('',#54905,#5009);
#4162=LINE('',#54907,#5010);
#4163=LINE('',#54908,#5011);
#4164=LINE('',#54911,#5012);
#4165=LINE('',#54913,#5013);
#4166=LINE('',#54914,#5014);
#4167=LINE('',#54917,#5015);
#4168=LINE('',#54919,#5016);
#4169=LINE('',#54920,#5017);
#4170=LINE('',#54923,#5018);
#4171=LINE('',#54925,#5019);
#4172=LINE('',#54926,#5020);
#4173=LINE('',#54928,#5021);
#4174=LINE('',#54929,#5022);
#4175=LINE('',#54935,#5023);
#4176=LINE('',#54944,#5024);
#4177=LINE('',#59232,#5025);
#4931=VECTOR('',#17659,6.);
#4932=VECTOR('',#17664,6.);
#4933=VECTOR('',#17667,6.);
#4934=VECTOR('',#17670,6.);
#4935=VECTOR('',#17673,6.);
#4936=VECTOR('',#17676,6.);
#4937=VECTOR('',#17679,6.);
#4938=VECTOR('',#17682,6.);
#4939=VECTOR('',#17685,6.);
#4940=VECTOR('',#17688,6.);
#4941=VECTOR('',#17691,6.);
#4942=VECTOR('',#17694,6.);
#4943=VECTOR('',#17697,6.);
#4944=VECTOR('',#17700,6.);
#4945=VECTOR('',#17703,6.);
#4946=VECTOR('',#17706,6.);
#4947=VECTOR('',#17709,6.);
#4948=VECTOR('',#17712,6.);
#4949=VECTOR('',#17715,6.);
#4950=VECTOR('',#17718,6.);
#4951=VECTOR('',#17721,6.);
#4952=VECTOR('',#17724,6.);
#4953=VECTOR('',#17727,6.);
#4954=VECTOR('',#17730,6.);
#4955=VECTOR('',#17733,6.);
#4956=VECTOR('',#17736,6.);
#4957=VECTOR('',#17739,6.);
#4958=VECTOR('',#17742,6.);
#4959=VECTOR('',#17745,6.);
#4960=VECTOR('',#17748,6.);
#4961=VECTOR('',#17751,6.);
#4962=VECTOR('',#17754,6.);
#4963=VECTOR('',#17757,6.);
#4964=VECTOR('',#17760,6.);
#4965=VECTOR('',#17763,6.);
#4966=VECTOR('',#17766,6.);
#4967=VECTOR('',#17771,6.);
#4968=VECTOR('',#17774,6.);
#4969=VECTOR('',#17779,4.91825);
#4970=VECTOR('',#17784,4.91825);
#4971=VECTOR('',#17787,4.91825);
#4972=VECTOR('',#17790,4.91825);
#4973=VECTOR('',#17793,4.91825);
#4974=VECTOR('',#17796,4.91825);
#4975=VECTOR('',#17799,4.91825);
#4976=VECTOR('',#17802,4.91825);
#4977=VECTOR('',#17805,4.91825);
#4978=VECTOR('',#17808,4.91825);
#4979=VECTOR('',#17811,4.91825);
#4980=VECTOR('',#17814,4.91825);
#4981=VECTOR('',#17817,4.91825);
#4982=VECTOR('',#17820,4.91825);
#4983=VECTOR('',#17823,4.91825);
#4984=VECTOR('',#17826,4.91825);
#4985=VECTOR('',#17829,4.91825);
#4986=VECTOR('',#17832,4.91825);
#4987=VECTOR('',#17835,4.91825);
#4988=VECTOR('',#17838,4.91825);
#4989=VECTOR('',#17841,4.91825);
#4990=VECTOR('',#17844,4.91825);
#4991=VECTOR('',#17847,4.91825);
#4992=VECTOR('',#17850,4.91825);
#4993=VECTOR('',#17853,4.91825);
#4994=VECTOR('',#17856,4.91825);
#4995=VECTOR('',#17859,4.91825);
#4996=VECTOR('',#17862,4.91825);
#4997=VECTOR('',#17865,4.91825);
#4998=VECTOR('',#17868,4.91825);
#4999=VECTOR('',#17871,4.91825);
#5000=VECTOR('',#17874,4.91825);
#5001=VECTOR('',#17877,4.91825);
#5002=VECTOR('',#17880,4.91825);
#5003=VECTOR('',#17883,4.91825);
#5004=VECTOR('',#17886,4.91825);
#5005=VECTOR('',#17889,10.);
#5006=VECTOR('',#17890,10.);
#5007=VECTOR('',#17891,10.);
#5008=VECTOR('',#17892,10.);
#5009=VECTOR('',#17895,10.);
#5010=VECTOR('',#17896,10.);
#5011=VECTOR('',#17897,10.);
#5012=VECTOR('',#17900,10.);
#5013=VECTOR('',#17901,10.);
#5014=VECTOR('',#17902,10.);
#5015=VECTOR('',#17905,10.);
#5016=VECTOR('',#17906,10.);
#5017=VECTOR('',#17907,10.);
#5018=VECTOR('',#17910,10.);
#5019=VECTOR('',#17911,10.);
#5020=VECTOR('',#17912,10.);
#5021=VECTOR('',#17915,10.);
#5022=VECTOR('',#17916,10.);
#5023=VECTOR('',#17923,5.);
#5024=VECTOR('',#17936,6.);
#5025=VECTOR('',#17953,10.);
#6171=VERTEX_POINT('',#50426);
#6172=VERTEX_POINT('',#50427);
#6173=VERTEX_POINT('',#50429);
#6174=VERTEX_POINT('',#50446);
#6175=VERTEX_POINT('',#50459);
#6176=VERTEX_POINT('',#50460);
#6177=VERTEX_POINT('',#50543);
#6178=VERTEX_POINT('',#50544);
#6179=VERTEX_POINT('',#50633);
#6180=VERTEX_POINT('',#50634);
#6181=VERTEX_POINT('',#50717);
#6182=VERTEX_POINT('',#50718);
#6183=VERTEX_POINT('',#50807);
#6184=VERTEX_POINT('',#50808);
#6185=VERTEX_POINT('',#50897);
#6186=VERTEX_POINT('',#50898);
#6187=VERTEX_POINT('',#50981);
#6188=VERTEX_POINT('',#50982);
#6189=VERTEX_POINT('',#51071);
#6190=VERTEX_POINT('',#51072);
#6191=VERTEX_POINT('',#51155);
#6192=VERTEX_POINT('',#51156);
#6193=VERTEX_POINT('',#51245);
#6194=VERTEX_POINT('',#51246);
#6195=VERTEX_POINT('',#51329);
#6196=VERTEX_POINT('',#51330);
#6197=VERTEX_POINT('',#51419);
#6198=VERTEX_POINT('',#51420);
#6199=VERTEX_POINT('',#51509);
#6200=VERTEX_POINT('',#51510);
#6201=VERTEX_POINT('',#51593);
#6202=VERTEX_POINT('',#51594);
#6203=VERTEX_POINT('',#51683);
#6204=VERTEX_POINT('',#51684);
#6205=VERTEX_POINT('',#51767);
#6206=VERTEX_POINT('',#51768);
#6207=VERTEX_POINT('',#51857);
#6208=VERTEX_POINT('',#51858);
#6209=VERTEX_POINT('',#51941);
#6210=VERTEX_POINT('',#51942);
#6211=VERTEX_POINT('',#52028);
#6212=VERTEX_POINT('',#52029);
#6213=VERTEX_POINT('',#52118);
#6214=VERTEX_POINT('',#52119);
#6215=VERTEX_POINT('',#52202);
#6216=VERTEX_POINT('',#52203);
#6217=VERTEX_POINT('',#52292);
#6218=VERTEX_POINT('',#52293);
#6219=VERTEX_POINT('',#52376);
#6220=VERTEX_POINT('',#52377);
#6221=VERTEX_POINT('',#52466);
#6222=VERTEX_POINT('',#52467);
#6223=VERTEX_POINT('',#52553);
#6224=VERTEX_POINT('',#52554);
#6225=VERTEX_POINT('',#52640);
#6226=VERTEX_POINT('',#52641);
#6227=VERTEX_POINT('',#52730);
#6228=VERTEX_POINT('',#52731);
#6229=VERTEX_POINT('',#52814);
#6230=VERTEX_POINT('',#52815);
#6231=VERTEX_POINT('',#52904);
#6232=VERTEX_POINT('',#52905);
#6233=VERTEX_POINT('',#52988);
#6234=VERTEX_POINT('',#52989);
#6235=VERTEX_POINT('',#53078);
#6236=VERTEX_POINT('',#53079);
#6237=VERTEX_POINT('',#53165);
#6238=VERTEX_POINT('',#53166);
#6239=VERTEX_POINT('',#53252);
#6240=VERTEX_POINT('',#53253);
#6241=VERTEX_POINT('',#53342);
#6242=VERTEX_POINT('',#53343);
#6243=VERTEX_POINT('',#53426);
#6244=VERTEX_POINT('',#53427);
#6245=VERTEX_POINT('',#53516);
#6246=VERTEX_POINT('',#53518);
#6247=VERTEX_POINT('',#53520);
#6248=VERTEX_POINT('',#53522);
#6249=VERTEX_POINT('',#53536);
#6250=VERTEX_POINT('',#53538);
#6251=VERTEX_POINT('',#53560);
#6252=VERTEX_POINT('',#53561);
#6253=VERTEX_POINT('',#53563);
#6254=VERTEX_POINT('',#53579);
#6255=VERTEX_POINT('',#53595);
#6256=VERTEX_POINT('',#53596);
#6257=VERTEX_POINT('',#53632);
#6258=VERTEX_POINT('',#53633);
#6259=VERTEX_POINT('',#53669);
#6260=VERTEX_POINT('',#53670);
#6261=VERTEX_POINT('',#53706);
#6262=VERTEX_POINT('',#53707);
#6263=VERTEX_POINT('',#53744);
#6264=VERTEX_POINT('',#53745);
#6265=VERTEX_POINT('',#53780);
#6266=VERTEX_POINT('',#53781);
#6267=VERTEX_POINT('',#53818);
#6268=VERTEX_POINT('',#53819);
#6269=VERTEX_POINT('',#53855);
#6270=VERTEX_POINT('',#53856);
#6271=VERTEX_POINT('',#53892);
#6272=VERTEX_POINT('',#53893);
#6273=VERTEX_POINT('',#53929);
#6274=VERTEX_POINT('',#53930);
#6275=VERTEX_POINT('',#53966);
#6276=VERTEX_POINT('',#53967);
#6277=VERTEX_POINT('',#54004);
#6278=VERTEX_POINT('',#54005);
#6279=VERTEX_POINT('',#54040);
#6280=VERTEX_POINT('',#54041);
#6281=VERTEX_POINT('',#54078);
#6282=VERTEX_POINT('',#54079);
#6283=VERTEX_POINT('',#54115);
#6284=VERTEX_POINT('',#54116);
#6285=VERTEX_POINT('',#54152);
#6286=VERTEX_POINT('',#54153);
#6287=VERTEX_POINT('',#54189);
#6288=VERTEX_POINT('',#54190);
#6289=VERTEX_POINT('',#54226);
#6290=VERTEX_POINT('',#54227);
#6291=VERTEX_POINT('',#54264);
#6292=VERTEX_POINT('',#54265);
#6293=VERTEX_POINT('',#54300);
#6294=VERTEX_POINT('',#54301);
#6295=VERTEX_POINT('',#54338);
#6296=VERTEX_POINT('',#54339);
#6297=VERTEX_POINT('',#54375);
#6298=VERTEX_POINT('',#54376);
#6299=VERTEX_POINT('',#54412);
#6300=VERTEX_POINT('',#54413);
#6301=VERTEX_POINT('',#54449);
#6302=VERTEX_POINT('',#54450);
#6303=VERTEX_POINT('',#54486);
#6304=VERTEX_POINT('',#54487);
#6305=VERTEX_POINT('',#54524);
#6306=VERTEX_POINT('',#54525);
#6307=VERTEX_POINT('',#54561);
#6308=VERTEX_POINT('',#54562);
#6309=VERTEX_POINT('',#54598);
#6310=VERTEX_POINT('',#54599);
#6311=VERTEX_POINT('',#54635);
#6312=VERTEX_POINT('',#54636);
#6313=VERTEX_POINT('',#54672);
#6314=VERTEX_POINT('',#54673);
#6315=VERTEX_POINT('',#54709);
#6316=VERTEX_POINT('',#54710);
#6317=VERTEX_POINT('',#54746);
#6318=VERTEX_POINT('',#54747);
#6319=VERTEX_POINT('',#54784);
#6320=VERTEX_POINT('',#54785);
#6321=VERTEX_POINT('',#54821);
#6322=VERTEX_POINT('',#54822);
#6323=VERTEX_POINT('',#54858);
#6324=VERTEX_POINT('',#54859);
#6325=VERTEX_POINT('',#54895);
#6326=VERTEX_POINT('',#54896);
#6327=VERTEX_POINT('',#54898);
#6328=VERTEX_POINT('',#54900);
#6329=VERTEX_POINT('',#54904);
#6330=VERTEX_POINT('',#54906);
#6331=VERTEX_POINT('',#54910);
#6332=VERTEX_POINT('',#54912);
#6333=VERTEX_POINT('',#54916);
#6334=VERTEX_POINT('',#54918);
#6335=VERTEX_POINT('',#54922);
#6336=VERTEX_POINT('',#54924);
#6337=VERTEX_POINT('',#54932);
#6338=VERTEX_POINT('',#54934);
#6339=VERTEX_POINT('',#54939);
#6340=VERTEX_POINT('',#54942);
#6341=VERTEX_POINT('',#57075);
#6342=VERTEX_POINT('',#57197);
#6343=VERTEX_POINT('',#59227);
#6344=VERTEX_POINT('',#59230);
#8131=EDGE_CURVE('',#6171,#6172,#4083,.T.);
#8132=EDGE_CURVE('',#6171,#6173,#3073,.T.);
#8133=EDGE_CURVE('',#6173,#6174,#2303,.F.);
#8134=EDGE_CURVE('',#6174,#6172,#3074,.T.);
#8135=EDGE_CURVE('',#6175,#6176,#4084,.T.);
#8136=EDGE_CURVE('',#6175,#6171,#3075,.T.);
#8137=EDGE_CURVE('',#6172,#6176,#3076,.T.);
#8138=EDGE_CURVE('',#6177,#6178,#4085,.T.);
#8139=EDGE_CURVE('',#6177,#6175,#3077,.T.);
#8140=EDGE_CURVE('',#6176,#6178,#3078,.T.);
#8141=EDGE_CURVE('',#6179,#6180,#4086,.T.);
#8142=EDGE_CURVE('',#6179,#6177,#3079,.T.);
#8143=EDGE_CURVE('',#6178,#6180,#3080,.T.);
#8144=EDGE_CURVE('',#6181,#6182,#4087,.T.);
#8145=EDGE_CURVE('',#6181,#6179,#3081,.T.);
#8146=EDGE_CURVE('',#6180,#6182,#3082,.T.);
#8147=EDGE_CURVE('',#6183,#6184,#4088,.T.);
#8148=EDGE_CURVE('',#6183,#6181,#3083,.T.);
#8149=EDGE_CURVE('',#6182,#6184,#3084,.T.);
#8150=EDGE_CURVE('',#6185,#6186,#4089,.T.);
#8151=EDGE_CURVE('',#6185,#6183,#3085,.T.);
#8152=EDGE_CURVE('',#6184,#6186,#3086,.T.);
#8153=EDGE_CURVE('',#6187,#6188,#4090,.T.);
#8154=EDGE_CURVE('',#6187,#6185,#3087,.T.);
#8155=EDGE_CURVE('',#6186,#6188,#3088,.T.);
#8156=EDGE_CURVE('',#6189,#6190,#4091,.T.);
#8157=EDGE_CURVE('',#6189,#6187,#3089,.T.);
#8158=EDGE_CURVE('',#6188,#6190,#3090,.T.);
#8159=EDGE_CURVE('',#6191,#6192,#4092,.T.);
#8160=EDGE_CURVE('',#6191,#6189,#3091,.T.);
#8161=EDGE_CURVE('',#6190,#6192,#3092,.T.);
#8162=EDGE_CURVE('',#6193,#6194,#4093,.T.);
#8163=EDGE_CURVE('',#6193,#6191,#3093,.T.);
#8164=EDGE_CURVE('',#6192,#6194,#3094,.T.);
#8165=EDGE_CURVE('',#6195,#6196,#4094,.T.);
#8166=EDGE_CURVE('',#6195,#6193,#3095,.T.);
#8167=EDGE_CURVE('',#6194,#6196,#3096,.T.);
#8168=EDGE_CURVE('',#6197,#6198,#4095,.T.);
#8169=EDGE_CURVE('',#6197,#6195,#3097,.T.);
#8170=EDGE_CURVE('',#6196,#6198,#3098,.T.);
#8171=EDGE_CURVE('',#6199,#6200,#4096,.T.);
#8172=EDGE_CURVE('',#6199,#6197,#3099,.T.);
#8173=EDGE_CURVE('',#6198,#6200,#3100,.T.);
#8174=EDGE_CURVE('',#6201,#6202,#4097,.T.);
#8175=EDGE_CURVE('',#6201,#6199,#3101,.T.);
#8176=EDGE_CURVE('',#6200,#6202,#3102,.T.);
#8177=EDGE_CURVE('',#6203,#6204,#4098,.T.);
#8178=EDGE_CURVE('',#6203,#6201,#3103,.T.);
#8179=EDGE_CURVE('',#6202,#6204,#3104,.T.);
#8180=EDGE_CURVE('',#6205,#6206,#4099,.T.);
#8181=EDGE_CURVE('',#6205,#6203,#3105,.T.);
#8182=EDGE_CURVE('',#6204,#6206,#3106,.T.);
#8183=EDGE_CURVE('',#6207,#6208,#4100,.T.);
#8184=EDGE_CURVE('',#6207,#6205,#3107,.T.);
#8185=EDGE_CURVE('',#6206,#6208,#3108,.T.);
#8186=EDGE_CURVE('',#6209,#6210,#4101,.T.);
#8187=EDGE_CURVE('',#6209,#6207,#3109,.T.);
#8188=EDGE_CURVE('',#6208,#6210,#3110,.T.);
#8189=EDGE_CURVE('',#6211,#6212,#4102,.T.);
#8190=EDGE_CURVE('',#6211,#6209,#3111,.T.);
#8191=EDGE_CURVE('',#6210,#6212,#3112,.T.);
#8192=EDGE_CURVE('',#6213,#6214,#4103,.T.);
#8193=EDGE_CURVE('',#6213,#6211,#3113,.T.);
#8194=EDGE_CURVE('',#6212,#6214,#3114,.T.);
#8195=EDGE_CURVE('',#6215,#6216,#4104,.T.);
#8196=EDGE_CURVE('',#6215,#6213,#3115,.T.);
#8197=EDGE_CURVE('',#6214,#6216,#3116,.T.);
#8198=EDGE_CURVE('',#6217,#6218,#4105,.T.);
#8199=EDGE_CURVE('',#6217,#6215,#3117,.T.);
#8200=EDGE_CURVE('',#6216,#6218,#3118,.T.);
#8201=EDGE_CURVE('',#6219,#6220,#4106,.T.);
#8202=EDGE_CURVE('',#6219,#6217,#3119,.T.);
#8203=EDGE_CURVE('',#6218,#6220,#3120,.T.);
#8204=EDGE_CURVE('',#6221,#6222,#4107,.T.);
#8205=EDGE_CURVE('',#6221,#6219,#3121,.T.);
#8206=EDGE_CURVE('',#6220,#6222,#3122,.T.);
#8207=EDGE_CURVE('',#6223,#6224,#4108,.T.);
#8208=EDGE_CURVE('',#6223,#6221,#3123,.T.);
#8209=EDGE_CURVE('',#6222,#6224,#3124,.T.);
#8210=EDGE_CURVE('',#6225,#6226,#4109,.T.);
#8211=EDGE_CURVE('',#6225,#6223,#3125,.T.);
#8212=EDGE_CURVE('',#6224,#6226,#3126,.T.);
#8213=EDGE_CURVE('',#6227,#6228,#4110,.T.);
#8214=EDGE_CURVE('',#6227,#6225,#3127,.T.);
#8215=EDGE_CURVE('',#6226,#6228,#3128,.T.);
#8216=EDGE_CURVE('',#6229,#6230,#4111,.T.);
#8217=EDGE_CURVE('',#6229,#6227,#3129,.T.);
#8218=EDGE_CURVE('',#6228,#6230,#3130,.T.);
#8219=EDGE_CURVE('',#6231,#6232,#4112,.T.);
#8220=EDGE_CURVE('',#6231,#6229,#3131,.T.);
#8221=EDGE_CURVE('',#6230,#6232,#3132,.T.);
#8222=EDGE_CURVE('',#6233,#6234,#4113,.T.);
#8223=EDGE_CURVE('',#6233,#6231,#3133,.T.);
#8224=EDGE_CURVE('',#6232,#6234,#3134,.T.);
#8225=EDGE_CURVE('',#6235,#6236,#4114,.T.);
#8226=EDGE_CURVE('',#6235,#6233,#3135,.T.);
#8227=EDGE_CURVE('',#6234,#6236,#3136,.T.);
#8228=EDGE_CURVE('',#6237,#6238,#4115,.T.);
#8229=EDGE_CURVE('',#6237,#6235,#3137,.T.);
#8230=EDGE_CURVE('',#6236,#6238,#3138,.T.);
#8231=EDGE_CURVE('',#6239,#6240,#4116,.T.);
#8232=EDGE_CURVE('',#6239,#6237,#3139,.T.);
#8233=EDGE_CURVE('',#6238,#6240,#3140,.T.);
#8234=EDGE_CURVE('',#6241,#6242,#4117,.T.);
#8235=EDGE_CURVE('',#6241,#6239,#3141,.T.);
#8236=EDGE_CURVE('',#6240,#6242,#3142,.T.);
#8237=EDGE_CURVE('',#6243,#6244,#4118,.T.);
#8238=EDGE_CURVE('',#6243,#6241,#3143,.T.);
#8239=EDGE_CURVE('',#6242,#6244,#3144,.T.);
#8240=EDGE_CURVE('',#6245,#6245,#2304,.T.);
#8241=EDGE_CURVE('',#6245,#6246,#4119,.T.);
#8242=EDGE_CURVE('',#6246,#6247,#2305,.T.);
#8243=EDGE_CURVE('',#6247,#6248,#3145,.T.);
#8244=EDGE_CURVE('',#6248,#6249,#4120,.T.);
#8245=EDGE_CURVE('',#6249,#6250,#3146,.T.);
#8246=EDGE_CURVE('',#6250,#6246,#2306,.T.);
#8247=EDGE_CURVE('',#6251,#6252,#4121,.T.);
#8248=EDGE_CURVE('',#6251,#6253,#3147,.T.);
#8249=EDGE_CURVE('',#6254,#6253,#2307,.T.);
#8250=EDGE_CURVE('',#6252,#6254,#3148,.T.);
#8251=EDGE_CURVE('',#6255,#6256,#4122,.T.);
#8252=EDGE_CURVE('',#6255,#6251,#3149,.T.);
#8253=EDGE_CURVE('',#6256,#6252,#3150,.T.);
#8254=EDGE_CURVE('',#6257,#6258,#4123,.T.);
#8255=EDGE_CURVE('',#6257,#6255,#3151,.T.);
#8256=EDGE_CURVE('',#6258,#6256,#3152,.T.);
#8257=EDGE_CURVE('',#6259,#6260,#4124,.T.);
#8258=EDGE_CURVE('',#6259,#6257,#3153,.T.);
#8259=EDGE_CURVE('',#6260,#6258,#3154,.T.);
#8260=EDGE_CURVE('',#6261,#6262,#4125,.T.);
#8261=EDGE_CURVE('',#6261,#6259,#3155,.T.);
#8262=EDGE_CURVE('',#6262,#6260,#3156,.T.);
#8263=EDGE_CURVE('',#6263,#6264,#4126,.T.);
#8264=EDGE_CURVE('',#6263,#6261,#3157,.T.);
#8265=EDGE_CURVE('',#6264,#6262,#3158,.T.);
#8266=EDGE_CURVE('',#6265,#6266,#4127,.T.);
#8267=EDGE_CURVE('',#6265,#6263,#3159,.T.);
#8268=EDGE_CURVE('',#6266,#6264,#3160,.T.);
#8269=EDGE_CURVE('',#6267,#6268,#4128,.T.);
#8270=EDGE_CURVE('',#6267,#6265,#3161,.T.);
#8271=EDGE_CURVE('',#6268,#6266,#3162,.T.);
#8272=EDGE_CURVE('',#6269,#6270,#4129,.T.);
#8273=EDGE_CURVE('',#6269,#6267,#3163,.T.);
#8274=EDGE_CURVE('',#6270,#6268,#3164,.T.);
#8275=EDGE_CURVE('',#6271,#6272,#4130,.T.);
#8276=EDGE_CURVE('',#6271,#6269,#3165,.T.);
#8277=EDGE_CURVE('',#6272,#6270,#3166,.T.);
#8278=EDGE_CURVE('',#6273,#6274,#4131,.T.);
#8279=EDGE_CURVE('',#6273,#6271,#3167,.T.);
#8280=EDGE_CURVE('',#6274,#6272,#3168,.T.);
#8281=EDGE_CURVE('',#6275,#6276,#4132,.T.);
#8282=EDGE_CURVE('',#6275,#6273,#3169,.T.);
#8283=EDGE_CURVE('',#6276,#6274,#3170,.T.);
#8284=EDGE_CURVE('',#6277,#6278,#4133,.T.);
#8285=EDGE_CURVE('',#6277,#6275,#3171,.T.);
#8286=EDGE_CURVE('',#6278,#6276,#3172,.T.);
#8287=EDGE_CURVE('',#6279,#6280,#4134,.T.);
#8288=EDGE_CURVE('',#6279,#6277,#3173,.T.);
#8289=EDGE_CURVE('',#6280,#6278,#3174,.T.);
#8290=EDGE_CURVE('',#6281,#6282,#4135,.T.);
#8291=EDGE_CURVE('',#6281,#6279,#3175,.T.);
#8292=EDGE_CURVE('',#6282,#6280,#3176,.T.);
#8293=EDGE_CURVE('',#6283,#6284,#4136,.T.);
#8294=EDGE_CURVE('',#6283,#6281,#3177,.T.);
#8295=EDGE_CURVE('',#6284,#6282,#3178,.T.);
#8296=EDGE_CURVE('',#6285,#6286,#4137,.T.);
#8297=EDGE_CURVE('',#6285,#6283,#3179,.T.);
#8298=EDGE_CURVE('',#6286,#6284,#3180,.T.);
#8299=EDGE_CURVE('',#6287,#6288,#4138,.T.);
#8300=EDGE_CURVE('',#6287,#6285,#3181,.T.);
#8301=EDGE_CURVE('',#6288,#6286,#3182,.T.);
#8302=EDGE_CURVE('',#6289,#6290,#4139,.T.);
#8303=EDGE_CURVE('',#6289,#6287,#3183,.T.);
#8304=EDGE_CURVE('',#6290,#6288,#3184,.T.);
#8305=EDGE_CURVE('',#6291,#6292,#4140,.T.);
#8306=EDGE_CURVE('',#6291,#6289,#3185,.T.);
#8307=EDGE_CURVE('',#6292,#6290,#3186,.T.);
#8308=EDGE_CURVE('',#6293,#6294,#4141,.T.);
#8309=EDGE_CURVE('',#6293,#6291,#3187,.T.);
#8310=EDGE_CURVE('',#6294,#6292,#3188,.T.);
#8311=EDGE_CURVE('',#6295,#6296,#4142,.T.);
#8312=EDGE_CURVE('',#6295,#6293,#3189,.T.);
#8313=EDGE_CURVE('',#6296,#6294,#3190,.T.);
#8314=EDGE_CURVE('',#6297,#6298,#4143,.T.);
#8315=EDGE_CURVE('',#6297,#6295,#3191,.T.);
#8316=EDGE_CURVE('',#6298,#6296,#3192,.T.);
#8317=EDGE_CURVE('',#6299,#6300,#4144,.T.);
#8318=EDGE_CURVE('',#6299,#6297,#3193,.T.);
#8319=EDGE_CURVE('',#6300,#6298,#3194,.T.);
#8320=EDGE_CURVE('',#6301,#6302,#4145,.T.);
#8321=EDGE_CURVE('',#6301,#6299,#3195,.T.);
#8322=EDGE_CURVE('',#6302,#6300,#3196,.T.);
#8323=EDGE_CURVE('',#6303,#6304,#4146,.T.);
#8324=EDGE_CURVE('',#6303,#6301,#3197,.T.);
#8325=EDGE_CURVE('',#6304,#6302,#3198,.T.);
#8326=EDGE_CURVE('',#6305,#6306,#4147,.T.);
#8327=EDGE_CURVE('',#6305,#6303,#3199,.T.);
#8328=EDGE_CURVE('',#6306,#6304,#3200,.T.);
#8329=EDGE_CURVE('',#6307,#6308,#4148,.T.);
#8330=EDGE_CURVE('',#6307,#6305,#3201,.T.);
#8331=EDGE_CURVE('',#6308,#6306,#3202,.T.);
#8332=EDGE_CURVE('',#6309,#6310,#4149,.T.);
#8333=EDGE_CURVE('',#6309,#6307,#3203,.T.);
#8334=EDGE_CURVE('',#6310,#6308,#3204,.T.);
#8335=EDGE_CURVE('',#6311,#6312,#4150,.T.);
#8336=EDGE_CURVE('',#6311,#6309,#3205,.T.);
#8337=EDGE_CURVE('',#6312,#6310,#3206,.T.);
#8338=EDGE_CURVE('',#6313,#6314,#4151,.T.);
#8339=EDGE_CURVE('',#6313,#6311,#3207,.T.);
#8340=EDGE_CURVE('',#6314,#6312,#3208,.T.);
#8341=EDGE_CURVE('',#6315,#6316,#4152,.T.);
#8342=EDGE_CURVE('',#6315,#6313,#3209,.T.);
#8343=EDGE_CURVE('',#6316,#6314,#3210,.T.);
#8344=EDGE_CURVE('',#6317,#6318,#4153,.T.);
#8345=EDGE_CURVE('',#6317,#6315,#3211,.T.);
#8346=EDGE_CURVE('',#6318,#6316,#3212,.T.);
#8347=EDGE_CURVE('',#6319,#6320,#4154,.T.);
#8348=EDGE_CURVE('',#6319,#6317,#3213,.T.);
#8349=EDGE_CURVE('',#6320,#6318,#3214,.T.);
#8350=EDGE_CURVE('',#6321,#6322,#4155,.T.);
#8351=EDGE_CURVE('',#6321,#6319,#3215,.T.);
#8352=EDGE_CURVE('',#6322,#6320,#3216,.T.);
#8353=EDGE_CURVE('',#6323,#6324,#4156,.T.);
#8354=EDGE_CURVE('',#6323,#6321,#3217,.T.);
#8355=EDGE_CURVE('',#6324,#6322,#3218,.T.);
#8356=EDGE_CURVE('',#6325,#6326,#4157,.T.);
#8357=EDGE_CURVE('',#6325,#6327,#4158,.T.);
#8358=EDGE_CURVE('',#6327,#6328,#4159,.T.);
#8359=EDGE_CURVE('',#6326,#6328,#4160,.T.);
#8360=EDGE_CURVE('',#6329,#6325,#4161,.T.);
#8361=EDGE_CURVE('',#6329,#6330,#4162,.T.);
#8362=EDGE_CURVE('',#6330,#6327,#4163,.T.);
#8363=EDGE_CURVE('',#6331,#6329,#4164,.T.);
#8364=EDGE_CURVE('',#6331,#6332,#4165,.T.);
#8365=EDGE_CURVE('',#6332,#6330,#4166,.T.);
#8366=EDGE_CURVE('',#6333,#6331,#4167,.T.);
#8367=EDGE_CURVE('',#6333,#6334,#4168,.T.);
#8368=EDGE_CURVE('',#6334,#6332,#4169,.T.);
#8369=EDGE_CURVE('',#6335,#6333,#4170,.T.);
#8370=EDGE_CURVE('',#6335,#6336,#4171,.T.);
#8371=EDGE_CURVE('',#6336,#6334,#4172,.T.);
#8372=EDGE_CURVE('',#6326,#6335,#4173,.T.);
#8373=EDGE_CURVE('',#6328,#6336,#4174,.T.);
#8374=EDGE_CURVE('',#6337,#6337,#2308,.T.);
#8375=EDGE_CURVE('',#6337,#6338,#4175,.T.);
#8376=EDGE_CURVE('',#6338,#6338,#2309,.T.);
#8377=EDGE_CURVE('',#6339,#6339,#2310,.T.);
#8378=EDGE_CURVE('',#6340,#6340,#2311,.F.);
#8379=EDGE_CURVE('',#6340,#6339,#4176,.T.);
#8380=EDGE_CURVE('',#6253,#6247,#3219,.T.);
#8381=EDGE_CURVE('',#6250,#6254,#3220,.T.);
#8382=EDGE_CURVE('',#6244,#6249,#3221,.T.);
#8383=EDGE_CURVE('',#6341,#6174,#3222,.T.);
#8384=EDGE_CURVE('',#6341,#6324,#3223,.T.);
#8385=EDGE_CURVE('',#6342,#6341,#2312,.T.);
#8386=EDGE_CURVE('',#6342,#6323,#3224,.T.);
#8387=EDGE_CURVE('',#6173,#6342,#3225,.T.);
#8388=EDGE_CURVE('',#6248,#6243,#3226,.T.);
#8389=EDGE_CURVE('',#6343,#6343,#2313,.T.);
#8390=EDGE_CURVE('',#6344,#6344,#2314,.T.);
#8391=EDGE_CURVE('',#6344,#6343,#4177,.T.);
#11789=ORIENTED_EDGE('',*,*,#8131,.F.);
#11790=ORIENTED_EDGE('',*,*,#8132,.T.);
#11791=ORIENTED_EDGE('',*,*,#8133,.T.);
#11792=ORIENTED_EDGE('',*,*,#8134,.T.);
#11793=ORIENTED_EDGE('',*,*,#8135,.F.);
#11794=ORIENTED_EDGE('',*,*,#8136,.T.);
#11795=ORIENTED_EDGE('',*,*,#8131,.T.);
#11796=ORIENTED_EDGE('',*,*,#8137,.T.);
#11797=ORIENTED_EDGE('',*,*,#8138,.F.);
#11798=ORIENTED_EDGE('',*,*,#8139,.T.);
#11799=ORIENTED_EDGE('',*,*,#8135,.T.);
#11800=ORIENTED_EDGE('',*,*,#8140,.T.);
#11801=ORIENTED_EDGE('',*,*,#8141,.F.);
#11802=ORIENTED_EDGE('',*,*,#8142,.T.);
#11803=ORIENTED_EDGE('',*,*,#8138,.T.);
#11804=ORIENTED_EDGE('',*,*,#8143,.T.);
#11805=ORIENTED_EDGE('',*,*,#8144,.F.);
#11806=ORIENTED_EDGE('',*,*,#8145,.T.);
#11807=ORIENTED_EDGE('',*,*,#8141,.T.);
#11808=ORIENTED_EDGE('',*,*,#8146,.T.);
#11809=ORIENTED_EDGE('',*,*,#8147,.F.);
#11810=ORIENTED_EDGE('',*,*,#8148,.T.);
#11811=ORIENTED_EDGE('',*,*,#8144,.T.);
#11812=ORIENTED_EDGE('',*,*,#8149,.T.);
#11813=ORIENTED_EDGE('',*,*,#8150,.F.);
#11814=ORIENTED_EDGE('',*,*,#8151,.T.);
#11815=ORIENTED_EDGE('',*,*,#8147,.T.);
#11816=ORIENTED_EDGE('',*,*,#8152,.T.);
#11817=ORIENTED_EDGE('',*,*,#8153,.F.);
#11818=ORIENTED_EDGE('',*,*,#8154,.T.);
#11819=ORIENTED_EDGE('',*,*,#8150,.T.);
#11820=ORIENTED_EDGE('',*,*,#8155,.T.);
#11821=ORIENTED_EDGE('',*,*,#8156,.F.);
#11822=ORIENTED_EDGE('',*,*,#8157,.T.);
#11823=ORIENTED_EDGE('',*,*,#8153,.T.);
#11824=ORIENTED_EDGE('',*,*,#8158,.T.);
#11825=ORIENTED_EDGE('',*,*,#8159,.F.);
#11826=ORIENTED_EDGE('',*,*,#8160,.T.);
#11827=ORIENTED_EDGE('',*,*,#8156,.T.);
#11828=ORIENTED_EDGE('',*,*,#8161,.T.);
#11829=ORIENTED_EDGE('',*,*,#8162,.F.);
#11830=ORIENTED_EDGE('',*,*,#8163,.T.);
#11831=ORIENTED_EDGE('',*,*,#8159,.T.);
#11832=ORIENTED_EDGE('',*,*,#8164,.T.);
#11833=ORIENTED_EDGE('',*,*,#8165,.F.);
#11834=ORIENTED_EDGE('',*,*,#8166,.T.);
#11835=ORIENTED_EDGE('',*,*,#8162,.T.);
#11836=ORIENTED_EDGE('',*,*,#8167,.T.);
#11837=ORIENTED_EDGE('',*,*,#8168,.F.);
#11838=ORIENTED_EDGE('',*,*,#8169,.T.);
#11839=ORIENTED_EDGE('',*,*,#8165,.T.);
#11840=ORIENTED_EDGE('',*,*,#8170,.T.);
#11841=ORIENTED_EDGE('',*,*,#8171,.F.);
#11842=ORIENTED_EDGE('',*,*,#8172,.T.);
#11843=ORIENTED_EDGE('',*,*,#8168,.T.);
#11844=ORIENTED_EDGE('',*,*,#8173,.T.);
#11845=ORIENTED_EDGE('',*,*,#8174,.F.);
#11846=ORIENTED_EDGE('',*,*,#8175,.T.);
#11847=ORIENTED_EDGE('',*,*,#8171,.T.);
#11848=ORIENTED_EDGE('',*,*,#8176,.T.);
#11849=ORIENTED_EDGE('',*,*,#8177,.F.);
#11850=ORIENTED_EDGE('',*,*,#8178,.T.);
#11851=ORIENTED_EDGE('',*,*,#8174,.T.);
#11852=ORIENTED_EDGE('',*,*,#8179,.T.);
#11853=ORIENTED_EDGE('',*,*,#8180,.F.);
#11854=ORIENTED_EDGE('',*,*,#8181,.T.);
#11855=ORIENTED_EDGE('',*,*,#8177,.T.);
#11856=ORIENTED_EDGE('',*,*,#8182,.T.);
#11857=ORIENTED_EDGE('',*,*,#8183,.F.);
#11858=ORIENTED_EDGE('',*,*,#8184,.T.);
#11859=ORIENTED_EDGE('',*,*,#8180,.T.);
#11860=ORIENTED_EDGE('',*,*,#8185,.T.);
#11861=ORIENTED_EDGE('',*,*,#8186,.F.);
#11862=ORIENTED_EDGE('',*,*,#8187,.T.);
#11863=ORIENTED_EDGE('',*,*,#8183,.T.);
#11864=ORIENTED_EDGE('',*,*,#8188,.T.);
#11865=ORIENTED_EDGE('',*,*,#8189,.F.);
#11866=ORIENTED_EDGE('',*,*,#8190,.T.);
#11867=ORIENTED_EDGE('',*,*,#8186,.T.);
#11868=ORIENTED_EDGE('',*,*,#8191,.T.);
#11869=ORIENTED_EDGE('',*,*,#8192,.F.);
#11870=ORIENTED_EDGE('',*,*,#8193,.T.);
#11871=ORIENTED_EDGE('',*,*,#8189,.T.);
#11872=ORIENTED_EDGE('',*,*,#8194,.T.);
#11873=ORIENTED_EDGE('',*,*,#8195,.F.);
#11874=ORIENTED_EDGE('',*,*,#8196,.T.);
#11875=ORIENTED_EDGE('',*,*,#8192,.T.);
#11876=ORIENTED_EDGE('',*,*,#8197,.T.);
#11877=ORIENTED_EDGE('',*,*,#8198,.F.);
#11878=ORIENTED_EDGE('',*,*,#8199,.T.);
#11879=ORIENTED_EDGE('',*,*,#8195,.T.);
#11880=ORIENTED_EDGE('',*,*,#8200,.T.);
#11881=ORIENTED_EDGE('',*,*,#8201,.F.);
#11882=ORIENTED_EDGE('',*,*,#8202,.T.);
#11883=ORIENTED_EDGE('',*,*,#8198,.T.);
#11884=ORIENTED_EDGE('',*,*,#8203,.T.);
#11885=ORIENTED_EDGE('',*,*,#8204,.F.);
#11886=ORIENTED_EDGE('',*,*,#8205,.T.);
#11887=ORIENTED_EDGE('',*,*,#8201,.T.);
#11888=ORIENTED_EDGE('',*,*,#8206,.T.);
#11889=ORIENTED_EDGE('',*,*,#8207,.F.);
#11890=ORIENTED_EDGE('',*,*,#8208,.T.);
#11891=ORIENTED_EDGE('',*,*,#8204,.T.);
#11892=ORIENTED_EDGE('',*,*,#8209,.T.);
#11893=ORIENTED_EDGE('',*,*,#8210,.F.);
#11894=ORIENTED_EDGE('',*,*,#8211,.T.);
#11895=ORIENTED_EDGE('',*,*,#8207,.T.);
#11896=ORIENTED_EDGE('',*,*,#8212,.T.);
#11897=ORIENTED_EDGE('',*,*,#8213,.F.);
#11898=ORIENTED_EDGE('',*,*,#8214,.T.);
#11899=ORIENTED_EDGE('',*,*,#8210,.T.);
#11900=ORIENTED_EDGE('',*,*,#8215,.T.);
#11901=ORIENTED_EDGE('',*,*,#8216,.F.);
#11902=ORIENTED_EDGE('',*,*,#8217,.T.);
#11903=ORIENTED_EDGE('',*,*,#8213,.T.);
#11904=ORIENTED_EDGE('',*,*,#8218,.T.);
#11905=ORIENTED_EDGE('',*,*,#8219,.F.);
#11906=ORIENTED_EDGE('',*,*,#8220,.T.);
#11907=ORIENTED_EDGE('',*,*,#8216,.T.);
#11908=ORIENTED_EDGE('',*,*,#8221,.T.);
#11909=ORIENTED_EDGE('',*,*,#8222,.F.);
#11910=ORIENTED_EDGE('',*,*,#8223,.T.);
#11911=ORIENTED_EDGE('',*,*,#8219,.T.);
#11912=ORIENTED_EDGE('',*,*,#8224,.T.);
#11913=ORIENTED_EDGE('',*,*,#8225,.F.);
#11914=ORIENTED_EDGE('',*,*,#8226,.T.);
#11915=ORIENTED_EDGE('',*,*,#8222,.T.);
#11916=ORIENTED_EDGE('',*,*,#8227,.T.);
#11917=ORIENTED_EDGE('',*,*,#8228,.F.);
#11918=ORIENTED_EDGE('',*,*,#8229,.T.);
#11919=ORIENTED_EDGE('',*,*,#8225,.T.);
#11920=ORIENTED_EDGE('',*,*,#8230,.T.);
#11921=ORIENTED_EDGE('',*,*,#8231,.F.);
#11922=ORIENTED_EDGE('',*,*,#8232,.T.);
#11923=ORIENTED_EDGE('',*,*,#8228,.T.);
#11924=ORIENTED_EDGE('',*,*,#8233,.T.);
#11925=ORIENTED_EDGE('',*,*,#8234,.F.);
#11926=ORIENTED_EDGE('',*,*,#8235,.T.);
#11927=ORIENTED_EDGE('',*,*,#8231,.T.);
#11928=ORIENTED_EDGE('',*,*,#8236,.T.);
#11929=ORIENTED_EDGE('',*,*,#8237,.F.);
#11930=ORIENTED_EDGE('',*,*,#8238,.T.);
#11931=ORIENTED_EDGE('',*,*,#8234,.T.);
#11932=ORIENTED_EDGE('',*,*,#8239,.T.);
#11933=ORIENTED_EDGE('',*,*,#8240,.T.);
#11934=ORIENTED_EDGE('',*,*,#8241,.T.);
#11935=ORIENTED_EDGE('',*,*,#8242,.T.);
#11936=ORIENTED_EDGE('',*,*,#8243,.T.);
#11937=ORIENTED_EDGE('',*,*,#8244,.T.);
#11938=ORIENTED_EDGE('',*,*,#8245,.T.);
#11939=ORIENTED_EDGE('',*,*,#8246,.T.);
#11940=ORIENTED_EDGE('',*,*,#8241,.F.);
#11941=ORIENTED_EDGE('',*,*,#8247,.F.);
#11942=ORIENTED_EDGE('',*,*,#8248,.T.);
#11943=ORIENTED_EDGE('',*,*,#8249,.F.);
#11944=ORIENTED_EDGE('',*,*,#8250,.F.);
#11945=ORIENTED_EDGE('',*,*,#8251,.F.);
#11946=ORIENTED_EDGE('',*,*,#8252,.T.);
#11947=ORIENTED_EDGE('',*,*,#8247,.T.);
#11948=ORIENTED_EDGE('',*,*,#8253,.F.);
#11949=ORIENTED_EDGE('',*,*,#8254,.F.);
#11950=ORIENTED_EDGE('',*,*,#8255,.T.);
#11951=ORIENTED_EDGE('',*,*,#8251,.T.);
#11952=ORIENTED_EDGE('',*,*,#8256,.F.);
#11953=ORIENTED_EDGE('',*,*,#8257,.F.);
#11954=ORIENTED_EDGE('',*,*,#8258,.T.);
#11955=ORIENTED_EDGE('',*,*,#8254,.T.);
#11956=ORIENTED_EDGE('',*,*,#8259,.F.);
#11957=ORIENTED_EDGE('',*,*,#8260,.F.);
#11958=ORIENTED_EDGE('',*,*,#8261,.T.);
#11959=ORIENTED_EDGE('',*,*,#8257,.T.);
#11960=ORIENTED_EDGE('',*,*,#8262,.F.);
#11961=ORIENTED_EDGE('',*,*,#8263,.F.);
#11962=ORIENTED_EDGE('',*,*,#8264,.T.);
#11963=ORIENTED_EDGE('',*,*,#8260,.T.);
#11964=ORIENTED_EDGE('',*,*,#8265,.F.);
#11965=ORIENTED_EDGE('',*,*,#8266,.F.);
#11966=ORIENTED_EDGE('',*,*,#8267,.T.);
#11967=ORIENTED_EDGE('',*,*,#8263,.T.);
#11968=ORIENTED_EDGE('',*,*,#8268,.F.);
#11969=ORIENTED_EDGE('',*,*,#8269,.F.);
#11970=ORIENTED_EDGE('',*,*,#8270,.T.);
#11971=ORIENTED_EDGE('',*,*,#8266,.T.);
#11972=ORIENTED_EDGE('',*,*,#8271,.F.);
#11973=ORIENTED_EDGE('',*,*,#8272,.F.);
#11974=ORIENTED_EDGE('',*,*,#8273,.T.);
#11975=ORIENTED_EDGE('',*,*,#8269,.T.);
#11976=ORIENTED_EDGE('',*,*,#8274,.F.);
#11977=ORIENTED_EDGE('',*,*,#8275,.F.);
#11978=ORIENTED_EDGE('',*,*,#8276,.T.);
#11979=ORIENTED_EDGE('',*,*,#8272,.T.);
#11980=ORIENTED_EDGE('',*,*,#8277,.F.);
#11981=ORIENTED_EDGE('',*,*,#8278,.F.);
#11982=ORIENTED_EDGE('',*,*,#8279,.T.);
#11983=ORIENTED_EDGE('',*,*,#8275,.T.);
#11984=ORIENTED_EDGE('',*,*,#8280,.F.);
#11985=ORIENTED_EDGE('',*,*,#8281,.F.);
#11986=ORIENTED_EDGE('',*,*,#8282,.T.);
#11987=ORIENTED_EDGE('',*,*,#8278,.T.);
#11988=ORIENTED_EDGE('',*,*,#8283,.F.);
#11989=ORIENTED_EDGE('',*,*,#8284,.F.);
#11990=ORIENTED_EDGE('',*,*,#8285,.T.);
#11991=ORIENTED_EDGE('',*,*,#8281,.T.);
#11992=ORIENTED_EDGE('',*,*,#8286,.F.);
#11993=ORIENTED_EDGE('',*,*,#8287,.F.);
#11994=ORIENTED_EDGE('',*,*,#8288,.T.);
#11995=ORIENTED_EDGE('',*,*,#8284,.T.);
#11996=ORIENTED_EDGE('',*,*,#8289,.F.);
#11997=ORIENTED_EDGE('',*,*,#8290,.F.);
#11998=ORIENTED_EDGE('',*,*,#8291,.T.);
#11999=ORIENTED_EDGE('',*,*,#8287,.T.);
#12000=ORIENTED_EDGE('',*,*,#8292,.F.);
#12001=ORIENTED_EDGE('',*,*,#8293,.F.);
#12002=ORIENTED_EDGE('',*,*,#8294,.T.);
#12003=ORIENTED_EDGE('',*,*,#8290,.T.);
#12004=ORIENTED_EDGE('',*,*,#8295,.F.);
#12005=ORIENTED_EDGE('',*,*,#8296,.F.);
#12006=ORIENTED_EDGE('',*,*,#8297,.T.);
#12007=ORIENTED_EDGE('',*,*,#8293,.T.);
#12008=ORIENTED_EDGE('',*,*,#8298,.F.);
#12009=ORIENTED_EDGE('',*,*,#8299,.F.);
#12010=ORIENTED_EDGE('',*,*,#8300,.T.);
#12011=ORIENTED_EDGE('',*,*,#8296,.T.);
#12012=ORIENTED_EDGE('',*,*,#8301,.F.);
#12013=ORIENTED_EDGE('',*,*,#8302,.F.);
#12014=ORIENTED_EDGE('',*,*,#8303,.T.);
#12015=ORIENTED_EDGE('',*,*,#8299,.T.);
#12016=ORIENTED_EDGE('',*,*,#8304,.F.);
#12017=ORIENTED_EDGE('',*,*,#8305,.F.);
#12018=ORIENTED_EDGE('',*,*,#8306,.T.);
#12019=ORIENTED_EDGE('',*,*,#8302,.T.);
#12020=ORIENTED_EDGE('',*,*,#8307,.F.);
#12021=ORIENTED_EDGE('',*,*,#8308,.F.);
#12022=ORIENTED_EDGE('',*,*,#8309,.T.);
#12023=ORIENTED_EDGE('',*,*,#8305,.T.);
#12024=ORIENTED_EDGE('',*,*,#8310,.F.);
#12025=ORIENTED_EDGE('',*,*,#8311,.F.);
#12026=ORIENTED_EDGE('',*,*,#8312,.T.);
#12027=ORIENTED_EDGE('',*,*,#8308,.T.);
#12028=ORIENTED_EDGE('',*,*,#8313,.F.);
#12029=ORIENTED_EDGE('',*,*,#8314,.F.);
#12030=ORIENTED_EDGE('',*,*,#8315,.T.);
#12031=ORIENTED_EDGE('',*,*,#8311,.T.);
#12032=ORIENTED_EDGE('',*,*,#8316,.F.);
#12033=ORIENTED_EDGE('',*,*,#8317,.F.);
#12034=ORIENTED_EDGE('',*,*,#8318,.T.);
#12035=ORIENTED_EDGE('',*,*,#8314,.T.);
#12036=ORIENTED_EDGE('',*,*,#8319,.F.);
#12037=ORIENTED_EDGE('',*,*,#8320,.F.);
#12038=ORIENTED_EDGE('',*,*,#8321,.T.);
#12039=ORIENTED_EDGE('',*,*,#8317,.T.);
#12040=ORIENTED_EDGE('',*,*,#8322,.F.);
#12041=ORIENTED_EDGE('',*,*,#8323,.F.);
#12042=ORIENTED_EDGE('',*,*,#8324,.T.);
#12043=ORIENTED_EDGE('',*,*,#8320,.T.);
#12044=ORIENTED_EDGE('',*,*,#8325,.F.);
#12045=ORIENTED_EDGE('',*,*,#8326,.F.);
#12046=ORIENTED_EDGE('',*,*,#8327,.T.);
#12047=ORIENTED_EDGE('',*,*,#8323,.T.);
#12048=ORIENTED_EDGE('',*,*,#8328,.F.);
#12049=ORIENTED_EDGE('',*,*,#8329,.F.);
#12050=ORIENTED_EDGE('',*,*,#8330,.T.);
#12051=ORIENTED_EDGE('',*,*,#8326,.T.);
#12052=ORIENTED_EDGE('',*,*,#8331,.F.);
#12053=ORIENTED_EDGE('',*,*,#8332,.F.);
#12054=ORIENTED_EDGE('',*,*,#8333,.T.);
#12055=ORIENTED_EDGE('',*,*,#8329,.T.);
#12056=ORIENTED_EDGE('',*,*,#8334,.F.);
#12057=ORIENTED_EDGE('',*,*,#8335,.F.);
#12058=ORIENTED_EDGE('',*,*,#8336,.T.);
#12059=ORIENTED_EDGE('',*,*,#8332,.T.);
#12060=ORIENTED_EDGE('',*,*,#8337,.F.);
#12061=ORIENTED_EDGE('',*,*,#8338,.F.);
#12062=ORIENTED_EDGE('',*,*,#8339,.T.);
#12063=ORIENTED_EDGE('',*,*,#8335,.T.);
#12064=ORIENTED_EDGE('',*,*,#8340,.F.);
#12065=ORIENTED_EDGE('',*,*,#8341,.F.);
#12066=ORIENTED_EDGE('',*,*,#8342,.T.);
#12067=ORIENTED_EDGE('',*,*,#8338,.T.);
#12068=ORIENTED_EDGE('',*,*,#8343,.F.);
#12069=ORIENTED_EDGE('',*,*,#8344,.F.);
#12070=ORIENTED_EDGE('',*,*,#8345,.T.);
#12071=ORIENTED_EDGE('',*,*,#8341,.T.);
#12072=ORIENTED_EDGE('',*,*,#8346,.F.);
#12073=ORIENTED_EDGE('',*,*,#8347,.F.);
#12074=ORIENTED_EDGE('',*,*,#8348,.T.);
#12075=ORIENTED_EDGE('',*,*,#8344,.T.);
#12076=ORIENTED_EDGE('',*,*,#8349,.F.);
#12077=ORIENTED_EDGE('',*,*,#8350,.F.);
#12078=ORIENTED_EDGE('',*,*,#8351,.T.);
#12079=ORIENTED_EDGE('',*,*,#8347,.T.);
#12080=ORIENTED_EDGE('',*,*,#8352,.F.);
#12081=ORIENTED_EDGE('',*,*,#8353,.F.);
#12082=ORIENTED_EDGE('',*,*,#8354,.T.);
#12083=ORIENTED_EDGE('',*,*,#8350,.T.);
#12084=ORIENTED_EDGE('',*,*,#8355,.F.);
#12085=ORIENTED_EDGE('',*,*,#8356,.F.);
#12086=ORIENTED_EDGE('',*,*,#8357,.T.);
#12087=ORIENTED_EDGE('',*,*,#8358,.T.);
#12088=ORIENTED_EDGE('',*,*,#8359,.F.);
#12089=ORIENTED_EDGE('',*,*,#8360,.F.);
#12090=ORIENTED_EDGE('',*,*,#8361,.T.);
#12091=ORIENTED_EDGE('',*,*,#8362,.T.);
#12092=ORIENTED_EDGE('',*,*,#8357,.F.);
#12093=ORIENTED_EDGE('',*,*,#8363,.F.);
#12094=ORIENTED_EDGE('',*,*,#8364,.T.);
#12095=ORIENTED_EDGE('',*,*,#8365,.T.);
#12096=ORIENTED_EDGE('',*,*,#8361,.F.);
#12097=ORIENTED_EDGE('',*,*,#8366,.F.);
#12098=ORIENTED_EDGE('',*,*,#8367,.T.);
#12099=ORIENTED_EDGE('',*,*,#8368,.T.);
#12100=ORIENTED_EDGE('',*,*,#8364,.F.);
#12101=ORIENTED_EDGE('',*,*,#8369,.F.);
#12102=ORIENTED_EDGE('',*,*,#8370,.T.);
#12103=ORIENTED_EDGE('',*,*,#8371,.T.);
#12104=ORIENTED_EDGE('',*,*,#8367,.F.);
#12105=ORIENTED_EDGE('',*,*,#8372,.F.);
#12106=ORIENTED_EDGE('',*,*,#8359,.T.);
#12107=ORIENTED_EDGE('',*,*,#8373,.T.);
#12108=ORIENTED_EDGE('',*,*,#8370,.F.);
#12109=ORIENTED_EDGE('',*,*,#8373,.F.);
#12110=ORIENTED_EDGE('',*,*,#8358,.F.);
#12111=ORIENTED_EDGE('',*,*,#8362,.F.);
#12112=ORIENTED_EDGE('',*,*,#8365,.F.);
#12113=ORIENTED_EDGE('',*,*,#8368,.F.);
#12114=ORIENTED_EDGE('',*,*,#8371,.F.);
#12115=ORIENTED_EDGE('',*,*,#8374,.T.);
#12116=ORIENTED_EDGE('',*,*,#8375,.T.);
#12117=ORIENTED_EDGE('',*,*,#8376,.F.);
#12118=ORIENTED_EDGE('',*,*,#8375,.F.);
#12119=ORIENTED_EDGE('',*,*,#8240,.F.);
#12120=ORIENTED_EDGE('',*,*,#8374,.F.);
#12121=ORIENTED_EDGE('',*,*,#8377,.F.);
#12122=ORIENTED_EDGE('',*,*,#8376,.T.);
#12123=ORIENTED_EDGE('',*,*,#8378,.F.);
#12124=ORIENTED_EDGE('',*,*,#8379,.T.);
#12125=ORIENTED_EDGE('',*,*,#8377,.T.);
#12126=ORIENTED_EDGE('',*,*,#8379,.F.);
#12127=ORIENTED_EDGE('',*,*,#8249,.T.);
#12128=ORIENTED_EDGE('',*,*,#8380,.T.);
#12129=ORIENTED_EDGE('',*,*,#8242,.F.);
#12130=ORIENTED_EDGE('',*,*,#8246,.F.);
#12131=ORIENTED_EDGE('',*,*,#8381,.T.);
#12132=ORIENTED_EDGE('',*,*,#8381,.F.);
#12133=ORIENTED_EDGE('',*,*,#8245,.F.);
#12134=ORIENTED_EDGE('',*,*,#8382,.F.);
#12135=ORIENTED_EDGE('',*,*,#8239,.F.);
#12136=ORIENTED_EDGE('',*,*,#8236,.F.);
#12137=ORIENTED_EDGE('',*,*,#8233,.F.);
#12138=ORIENTED_EDGE('',*,*,#8230,.F.);
#12139=ORIENTED_EDGE('',*,*,#8227,.F.);
#12140=ORIENTED_EDGE('',*,*,#8224,.F.);
#12141=ORIENTED_EDGE('',*,*,#8221,.F.);
#12142=ORIENTED_EDGE('',*,*,#8218,.F.);
#12143=ORIENTED_EDGE('',*,*,#8215,.F.);
#12144=ORIENTED_EDGE('',*,*,#8212,.F.);
#12145=ORIENTED_EDGE('',*,*,#8209,.F.);
#12146=ORIENTED_EDGE('',*,*,#8206,.F.);
#12147=ORIENTED_EDGE('',*,*,#8203,.F.);
#12148=ORIENTED_EDGE('',*,*,#8200,.F.);
#12149=ORIENTED_EDGE('',*,*,#8197,.F.);
#12150=ORIENTED_EDGE('',*,*,#8194,.F.);
#12151=ORIENTED_EDGE('',*,*,#8191,.F.);
#12152=ORIENTED_EDGE('',*,*,#8188,.F.);
#12153=ORIENTED_EDGE('',*,*,#8185,.F.);
#12154=ORIENTED_EDGE('',*,*,#8182,.F.);
#12155=ORIENTED_EDGE('',*,*,#8179,.F.);
#12156=ORIENTED_EDGE('',*,*,#8176,.F.);
#12157=ORIENTED_EDGE('',*,*,#8173,.F.);
#12158=ORIENTED_EDGE('',*,*,#8170,.F.);
#12159=ORIENTED_EDGE('',*,*,#8167,.F.);
#12160=ORIENTED_EDGE('',*,*,#8164,.F.);
#12161=ORIENTED_EDGE('',*,*,#8161,.F.);
#12162=ORIENTED_EDGE('',*,*,#8158,.F.);
#12163=ORIENTED_EDGE('',*,*,#8155,.F.);
#12164=ORIENTED_EDGE('',*,*,#8152,.F.);
#12165=ORIENTED_EDGE('',*,*,#8149,.F.);
#12166=ORIENTED_EDGE('',*,*,#8146,.F.);
#12167=ORIENTED_EDGE('',*,*,#8143,.F.);
#12168=ORIENTED_EDGE('',*,*,#8140,.F.);
#12169=ORIENTED_EDGE('',*,*,#8137,.F.);
#12170=ORIENTED_EDGE('',*,*,#8134,.F.);
#12171=ORIENTED_EDGE('',*,*,#8383,.F.);
#12172=ORIENTED_EDGE('',*,*,#8384,.T.);
#12173=ORIENTED_EDGE('',*,*,#8355,.T.);
#12174=ORIENTED_EDGE('',*,*,#8352,.T.);
#12175=ORIENTED_EDGE('',*,*,#8349,.T.);
#12176=ORIENTED_EDGE('',*,*,#8346,.T.);
#12177=ORIENTED_EDGE('',*,*,#8343,.T.);
#12178=ORIENTED_EDGE('',*,*,#8340,.T.);
#12179=ORIENTED_EDGE('',*,*,#8337,.T.);
#12180=ORIENTED_EDGE('',*,*,#8334,.T.);
#12181=ORIENTED_EDGE('',*,*,#8331,.T.);
#12182=ORIENTED_EDGE('',*,*,#8328,.T.);
#12183=ORIENTED_EDGE('',*,*,#8325,.T.);
#12184=ORIENTED_EDGE('',*,*,#8322,.T.);
#12185=ORIENTED_EDGE('',*,*,#8319,.T.);
#12186=ORIENTED_EDGE('',*,*,#8316,.T.);
#12187=ORIENTED_EDGE('',*,*,#8313,.T.);
#12188=ORIENTED_EDGE('',*,*,#8310,.T.);
#12189=ORIENTED_EDGE('',*,*,#8307,.T.);
#12190=ORIENTED_EDGE('',*,*,#8304,.T.);
#12191=ORIENTED_EDGE('',*,*,#8301,.T.);
#12192=ORIENTED_EDGE('',*,*,#8298,.T.);
#12193=ORIENTED_EDGE('',*,*,#8295,.T.);
#12194=ORIENTED_EDGE('',*,*,#8292,.T.);
#12195=ORIENTED_EDGE('',*,*,#8289,.T.);
#12196=ORIENTED_EDGE('',*,*,#8286,.T.);
#12197=ORIENTED_EDGE('',*,*,#8283,.T.);
#12198=ORIENTED_EDGE('',*,*,#8280,.T.);
#12199=ORIENTED_EDGE('',*,*,#8277,.T.);
#12200=ORIENTED_EDGE('',*,*,#8274,.T.);
#12201=ORIENTED_EDGE('',*,*,#8271,.T.);
#12202=ORIENTED_EDGE('',*,*,#8268,.T.);
#12203=ORIENTED_EDGE('',*,*,#8265,.T.);
#12204=ORIENTED_EDGE('',*,*,#8262,.T.);
#12205=ORIENTED_EDGE('',*,*,#8259,.T.);
#12206=ORIENTED_EDGE('',*,*,#8256,.T.);
#12207=ORIENTED_EDGE('',*,*,#8253,.T.);
#12208=ORIENTED_EDGE('',*,*,#8250,.T.);
#12209=ORIENTED_EDGE('',*,*,#8353,.T.);
#12210=ORIENTED_EDGE('',*,*,#8384,.F.);
#12211=ORIENTED_EDGE('',*,*,#8385,.F.);
#12212=ORIENTED_EDGE('',*,*,#8386,.T.);
#12213=ORIENTED_EDGE('',*,*,#8380,.F.);
#12214=ORIENTED_EDGE('',*,*,#8248,.F.);
#12215=ORIENTED_EDGE('',*,*,#8252,.F.);
#12216=ORIENTED_EDGE('',*,*,#8255,.F.);
#12217=ORIENTED_EDGE('',*,*,#8258,.F.);
#12218=ORIENTED_EDGE('',*,*,#8261,.F.);
#12219=ORIENTED_EDGE('',*,*,#8264,.F.);
#12220=ORIENTED_EDGE('',*,*,#8267,.F.);
#12221=ORIENTED_EDGE('',*,*,#8270,.F.);
#12222=ORIENTED_EDGE('',*,*,#8273,.F.);
#12223=ORIENTED_EDGE('',*,*,#8276,.F.);
#12224=ORIENTED_EDGE('',*,*,#8279,.F.);
#12225=ORIENTED_EDGE('',*,*,#8282,.F.);
#12226=ORIENTED_EDGE('',*,*,#8285,.F.);
#12227=ORIENTED_EDGE('',*,*,#8288,.F.);
#12228=ORIENTED_EDGE('',*,*,#8291,.F.);
#12229=ORIENTED_EDGE('',*,*,#8294,.F.);
#12230=ORIENTED_EDGE('',*,*,#8297,.F.);
#12231=ORIENTED_EDGE('',*,*,#8300,.F.);
#12232=ORIENTED_EDGE('',*,*,#8303,.F.);
#12233=ORIENTED_EDGE('',*,*,#8306,.F.);
#12234=ORIENTED_EDGE('',*,*,#8309,.F.);
#12235=ORIENTED_EDGE('',*,*,#8312,.F.);
#12236=ORIENTED_EDGE('',*,*,#8315,.F.);
#12237=ORIENTED_EDGE('',*,*,#8318,.F.);
#12238=ORIENTED_EDGE('',*,*,#8321,.F.);
#12239=ORIENTED_EDGE('',*,*,#8324,.F.);
#12240=ORIENTED_EDGE('',*,*,#8327,.F.);
#12241=ORIENTED_EDGE('',*,*,#8330,.F.);
#12242=ORIENTED_EDGE('',*,*,#8333,.F.);
#12243=ORIENTED_EDGE('',*,*,#8336,.F.);
#12244=ORIENTED_EDGE('',*,*,#8339,.F.);
#12245=ORIENTED_EDGE('',*,*,#8342,.F.);
#12246=ORIENTED_EDGE('',*,*,#8345,.F.);
#12247=ORIENTED_EDGE('',*,*,#8348,.F.);
#12248=ORIENTED_EDGE('',*,*,#8351,.F.);
#12249=ORIENTED_EDGE('',*,*,#8354,.F.);
#12250=ORIENTED_EDGE('',*,*,#8386,.F.);
#12251=ORIENTED_EDGE('',*,*,#8387,.F.);
#12252=ORIENTED_EDGE('',*,*,#8132,.F.);
#12253=ORIENTED_EDGE('',*,*,#8136,.F.);
#12254=ORIENTED_EDGE('',*,*,#8139,.F.);
#12255=ORIENTED_EDGE('',*,*,#8142,.F.);
#12256=ORIENTED_EDGE('',*,*,#8145,.F.);
#12257=ORIENTED_EDGE('',*,*,#8148,.F.);
#12258=ORIENTED_EDGE('',*,*,#8151,.F.);
#12259=ORIENTED_EDGE('',*,*,#8154,.F.);
#12260=ORIENTED_EDGE('',*,*,#8157,.F.);
#12261=ORIENTED_EDGE('',*,*,#8160,.F.);
#12262=ORIENTED_EDGE('',*,*,#8163,.F.);
#12263=ORIENTED_EDGE('',*,*,#8166,.F.);
#12264=ORIENTED_EDGE('',*,*,#8169,.F.);
#12265=ORIENTED_EDGE('',*,*,#8172,.F.);
#12266=ORIENTED_EDGE('',*,*,#8175,.F.);
#12267=ORIENTED_EDGE('',*,*,#8178,.F.);
#12268=ORIENTED_EDGE('',*,*,#8181,.F.);
#12269=ORIENTED_EDGE('',*,*,#8184,.F.);
#12270=ORIENTED_EDGE('',*,*,#8187,.F.);
#12271=ORIENTED_EDGE('',*,*,#8190,.F.);
#12272=ORIENTED_EDGE('',*,*,#8193,.F.);
#12273=ORIENTED_EDGE('',*,*,#8196,.F.);
#12274=ORIENTED_EDGE('',*,*,#8199,.F.);
#12275=ORIENTED_EDGE('',*,*,#8202,.F.);
#12276=ORIENTED_EDGE('',*,*,#8205,.F.);
#12277=ORIENTED_EDGE('',*,*,#8208,.F.);
#12278=ORIENTED_EDGE('',*,*,#8211,.F.);
#12279=ORIENTED_EDGE('',*,*,#8214,.F.);
#12280=ORIENTED_EDGE('',*,*,#8217,.F.);
#12281=ORIENTED_EDGE('',*,*,#8220,.F.);
#12282=ORIENTED_EDGE('',*,*,#8223,.F.);
#12283=ORIENTED_EDGE('',*,*,#8226,.F.);
#12284=ORIENTED_EDGE('',*,*,#8229,.F.);
#12285=ORIENTED_EDGE('',*,*,#8232,.F.);
#12286=ORIENTED_EDGE('',*,*,#8235,.F.);
#12287=ORIENTED_EDGE('',*,*,#8238,.F.);
#12288=ORIENTED_EDGE('',*,*,#8388,.F.);
#12289=ORIENTED_EDGE('',*,*,#8243,.F.);
#12290=ORIENTED_EDGE('',*,*,#8244,.F.);
#12291=ORIENTED_EDGE('',*,*,#8388,.T.);
#12292=ORIENTED_EDGE('',*,*,#8237,.T.);
#12293=ORIENTED_EDGE('',*,*,#8382,.T.);
#12294=ORIENTED_EDGE('',*,*,#8389,.F.);
#12295=ORIENTED_EDGE('',*,*,#8378,.T.);
#12296=ORIENTED_EDGE('',*,*,#8390,.F.);
#12297=ORIENTED_EDGE('',*,*,#8391,.T.);
#12298=ORIENTED_EDGE('',*,*,#8389,.T.);
#12299=ORIENTED_EDGE('',*,*,#8391,.F.);
#12300=ORIENTED_EDGE('',*,*,#8390,.T.);
#12301=ORIENTED_EDGE('',*,*,#8356,.T.);
#12302=ORIENTED_EDGE('',*,*,#8372,.T.);
#12303=ORIENTED_EDGE('',*,*,#8369,.T.);
#12304=ORIENTED_EDGE('',*,*,#8366,.T.);
#12305=ORIENTED_EDGE('',*,*,#8363,.T.);
#12306=ORIENTED_EDGE('',*,*,#8360,.T.);
#12307=ORIENTED_EDGE('',*,*,#8383,.T.);
#12308=ORIENTED_EDGE('',*,*,#8133,.F.);
#12309=ORIENTED_EDGE('',*,*,#8387,.T.);
#12310=ORIENTED_EDGE('',*,*,#8385,.T.);
#13716=CYLINDRICAL_SURFACE('',#15483,5.91675);
#13717=CYLINDRICAL_SURFACE('',#15485,5.91675);
#13718=CYLINDRICAL_SURFACE('',#15486,5.91675);
#13719=CYLINDRICAL_SURFACE('',#15487,5.91675);
#13720=CYLINDRICAL_SURFACE('',#15488,5.91675);
#13721=CYLINDRICAL_SURFACE('',#15489,5.91675);
#13722=CYLINDRICAL_SURFACE('',#15490,5.91675);
#13723=CYLINDRICAL_SURFACE('',#15491,5.91675);
#13724=CYLINDRICAL_SURFACE('',#15492,5.91675);
#13725=CYLINDRICAL_SURFACE('',#15493,5.91675);
#13726=CYLINDRICAL_SURFACE('',#15494,5.91675);
#13727=CYLINDRICAL_SURFACE('',#15495,5.91675);
#13728=CYLINDRICAL_SURFACE('',#15496,5.91675);
#13729=CYLINDRICAL_SURFACE('',#15497,5.91675);
#13730=CYLINDRICAL_SURFACE('',#15498,5.91675);
#13731=CYLINDRICAL_SURFACE('',#15499,5.91675);
#13732=CYLINDRICAL_SURFACE('',#15500,5.91675);
#13733=CYLINDRICAL_SURFACE('',#15501,5.91675);
#13734=CYLINDRICAL_SURFACE('',#15502,5.91675);
#13735=CYLINDRICAL_SURFACE('',#15503,5.91675);
#13736=CYLINDRICAL_SURFACE('',#15504,5.91675);
#13737=CYLINDRICAL_SURFACE('',#15505,5.91675);
#13738=CYLINDRICAL_SURFACE('',#15506,5.91675);
#13739=CYLINDRICAL_SURFACE('',#15507,5.91675);
#13740=CYLINDRICAL_SURFACE('',#15508,5.91675);
#13741=CYLINDRICAL_SURFACE('',#15509,5.91675);
#13742=CYLINDRICAL_SURFACE('',#15510,5.91675);
#13743=CYLINDRICAL_SURFACE('',#15511,5.91675);
#13744=CYLINDRICAL_SURFACE('',#15512,5.91675);
#13745=CYLINDRICAL_SURFACE('',#15513,5.91675);
#13746=CYLINDRICAL_SURFACE('',#15514,5.91675);
#13747=CYLINDRICAL_SURFACE('',#15515,5.91675);
#13748=CYLINDRICAL_SURFACE('',#15516,5.91675);
#13749=CYLINDRICAL_SURFACE('',#15517,5.91675);
#13750=CYLINDRICAL_SURFACE('',#15518,5.91675);
#13751=CYLINDRICAL_SURFACE('',#15519,5.91675);
#13752=CYLINDRICAL_SURFACE('',#15520,5.91675);
#13753=CYLINDRICAL_SURFACE('',#15524,4.91825);
#13754=CYLINDRICAL_SURFACE('',#15526,4.91825);
#13755=CYLINDRICAL_SURFACE('',#15527,4.91825);
#13756=CYLINDRICAL_SURFACE('',#15528,4.91825);
#13757=CYLINDRICAL_SURFACE('',#15529,4.91825);
#13758=CYLINDRICAL_SURFACE('',#15530,4.91825);
#13759=CYLINDRICAL_SURFACE('',#15531,4.91825);
#13760=CYLINDRICAL_SURFACE('',#15532,4.91825);
#13761=CYLINDRICAL_SURFACE('',#15533,4.91825);
#13762=CYLINDRICAL_SURFACE('',#15534,4.91825);
#13763=CYLINDRICAL_SURFACE('',#15535,4.91825);
#13764=CYLINDRICAL_SURFACE('',#15536,4.91825);
#13765=CYLINDRICAL_SURFACE('',#15537,4.91825);
#13766=CYLINDRICAL_SURFACE('',#15538,4.91825);
#13767=CYLINDRICAL_SURFACE('',#15539,4.91825);
#13768=CYLINDRICAL_SURFACE('',#15540,4.91825);
#13769=CYLINDRICAL_SURFACE('',#15541,4.91825);
#13770=CYLINDRICAL_SURFACE('',#15542,4.91825);
#13771=CYLINDRICAL_SURFACE('',#15543,4.91825);
#13772=CYLINDRICAL_SURFACE('',#15544,4.91825);
#13773=CYLINDRICAL_SURFACE('',#15545,4.91825);
#13774=CYLINDRICAL_SURFACE('',#15546,4.91825);
#13775=CYLINDRICAL_SURFACE('',#15547,4.91825);
#13776=CYLINDRICAL_SURFACE('',#15548,4.91825);
#13777=CYLINDRICAL_SURFACE('',#15549,4.91825);
#13778=CYLINDRICAL_SURFACE('',#15550,4.91825);
#13779=CYLINDRICAL_SURFACE('',#15551,4.91825);
#13780=CYLINDRICAL_SURFACE('',#15552,4.91825);
#13781=CYLINDRICAL_SURFACE('',#15553,4.91825);
#13782=CYLINDRICAL_SURFACE('',#15554,4.91825);
#13783=CYLINDRICAL_SURFACE('',#15555,4.91825);
#13784=CYLINDRICAL_SURFACE('',#15556,4.91825);
#13785=CYLINDRICAL_SURFACE('',#15557,4.91825);
#13786=CYLINDRICAL_SURFACE('',#15558,4.91825);
#13787=CYLINDRICAL_SURFACE('',#15559,4.91825);
#13788=CYLINDRICAL_SURFACE('',#15560,4.91825);
#13789=CYLINDRICAL_SURFACE('',#15568,5.);
#13790=CYLINDRICAL_SURFACE('',#15574,5.91675);
#13791=CYLINDRICAL_SURFACE('',#15577,4.91825);
#13792=CYLINDRICAL_SURFACE('',#15579,5.91675);
#13793=CYLINDRICAL_SURFACE('',#15582,10.);
#14445=ADVANCED_FACE('',(#1017),#13716,.T.);
#14446=ADVANCED_FACE('',(#1018),#13717,.T.);
#14447=ADVANCED_FACE('',(#1019),#13718,.T.);
#14448=ADVANCED_FACE('',(#1020),#13719,.T.);
#14449=ADVANCED_FACE('',(#1021),#13720,.T.);
#14450=ADVANCED_FACE('',(#1022),#13721,.T.);
#14451=ADVANCED_FACE('',(#1023),#13722,.T.);
#14452=ADVANCED_FACE('',(#1024),#13723,.T.);
#14453=ADVANCED_FACE('',(#1025),#13724,.T.);
#14454=ADVANCED_FACE('',(#1026),#13725,.T.);
#14455=ADVANCED_FACE('',(#1027),#13726,.T.);
#14456=ADVANCED_FACE('',(#1028),#13727,.T.);
#14457=ADVANCED_FACE('',(#1029),#13728,.T.);
#14458=ADVANCED_FACE('',(#1030),#13729,.T.);
#14459=ADVANCED_FACE('',(#1031),#13730,.T.);
#14460=ADVANCED_FACE('',(#1032),#13731,.T.);
#14461=ADVANCED_FACE('',(#1033),#13732,.T.);
#14462=ADVANCED_FACE('',(#1034),#13733,.T.);
#14463=ADVANCED_FACE('',(#1035),#13734,.T.);
#14464=ADVANCED_FACE('',(#1036),#13735,.T.);
#14465=ADVANCED_FACE('',(#1037),#13736,.T.);
#14466=ADVANCED_FACE('',(#1038),#13737,.T.);
#14467=ADVANCED_FACE('',(#1039),#13738,.T.);
#14468=ADVANCED_FACE('',(#1040),#13739,.T.);
#14469=ADVANCED_FACE('',(#1041),#13740,.T.);
#14470=ADVANCED_FACE('',(#1042),#13741,.T.);
#14471=ADVANCED_FACE('',(#1043),#13742,.T.);
#14472=ADVANCED_FACE('',(#1044),#13743,.T.);
#14473=ADVANCED_FACE('',(#1045),#13744,.T.);
#14474=ADVANCED_FACE('',(#1046),#13745,.T.);
#14475=ADVANCED_FACE('',(#1047),#13746,.T.);
#14476=ADVANCED_FACE('',(#1048),#13747,.T.);
#14477=ADVANCED_FACE('',(#1049),#13748,.T.);
#14478=ADVANCED_FACE('',(#1050),#13749,.T.);
#14479=ADVANCED_FACE('',(#1051),#13750,.T.);
#14480=ADVANCED_FACE('',(#1052),#13751,.T.);
#14481=ADVANCED_FACE('',(#1053),#13752,.T.);
#14482=ADVANCED_FACE('',(#1054),#13753,.T.);
#14483=ADVANCED_FACE('',(#1055),#13754,.T.);
#14484=ADVANCED_FACE('',(#1056),#13755,.T.);
#14485=ADVANCED_FACE('',(#1057),#13756,.T.);
#14486=ADVANCED_FACE('',(#1058),#13757,.T.);
#14487=ADVANCED_FACE('',(#1059),#13758,.T.);
#14488=ADVANCED_FACE('',(#1060),#13759,.T.);
#14489=ADVANCED_FACE('',(#1061),#13760,.T.);
#14490=ADVANCED_FACE('',(#1062),#13761,.T.);
#14491=ADVANCED_FACE('',(#1063),#13762,.T.);
#14492=ADVANCED_FACE('',(#1064),#13763,.T.);
#14493=ADVANCED_FACE('',(#1065),#13764,.T.);
#14494=ADVANCED_FACE('',(#1066),#13765,.T.);
#14495=ADVANCED_FACE('',(#1067),#13766,.T.);
#14496=ADVANCED_FACE('',(#1068),#13767,.T.);
#14497=ADVANCED_FACE('',(#1069),#13768,.T.);
#14498=ADVANCED_FACE('',(#1070),#13769,.T.);
#14499=ADVANCED_FACE('',(#1071),#13770,.T.);
#14500=ADVANCED_FACE('',(#1072),#13771,.T.);
#14501=ADVANCED_FACE('',(#1073),#13772,.T.);
#14502=ADVANCED_FACE('',(#1074),#13773,.T.);
#14503=ADVANCED_FACE('',(#1075),#13774,.T.);
#14504=ADVANCED_FACE('',(#1076),#13775,.T.);
#14505=ADVANCED_FACE('',(#1077),#13776,.T.);
#14506=ADVANCED_FACE('',(#1078),#13777,.T.);
#14507=ADVANCED_FACE('',(#1079),#13778,.T.);
#14508=ADVANCED_FACE('',(#1080),#13779,.T.);
#14509=ADVANCED_FACE('',(#1081),#13780,.T.);
#14510=ADVANCED_FACE('',(#1082),#13781,.T.);
#14511=ADVANCED_FACE('',(#1083),#13782,.T.);
#14512=ADVANCED_FACE('',(#1084),#13783,.T.);
#14513=ADVANCED_FACE('',(#1085),#13784,.T.);
#14514=ADVANCED_FACE('',(#1086),#13785,.T.);
#14515=ADVANCED_FACE('',(#1087),#13786,.T.);
#14516=ADVANCED_FACE('',(#1088),#13787,.T.);
#14517=ADVANCED_FACE('',(#1089),#13788,.T.);
#14518=ADVANCED_FACE('',(#1090),#479,.F.);
#14519=ADVANCED_FACE('',(#1091),#480,.F.);
#14520=ADVANCED_FACE('',(#1092),#481,.F.);
#14521=ADVANCED_FACE('',(#1093),#482,.F.);
#14522=ADVANCED_FACE('',(#1094),#483,.F.);
#14523=ADVANCED_FACE('',(#1095),#484,.F.);
#14524=ADVANCED_FACE('',(#1096),#485,.F.);
#14525=ADVANCED_FACE('',(#1097),#13789,.T.);
#14526=ADVANCED_FACE('',(#1098,#351),#486,.F.);
#14527=ADVANCED_FACE('',(#1099,#352),#487,.F.);
#14528=ADVANCED_FACE('',(#1100),#13790,.T.);
#14529=ADVANCED_FACE('',(#1101),#488,.F.);
#14530=ADVANCED_FACE('',(#1102),#292,.F.);
#14531=ADVANCED_FACE('',(#1103),#13791,.T.);
#14532=ADVANCED_FACE('',(#1104),#293,.F.);
#14533=ADVANCED_FACE('',(#1105),#13792,.T.);
#14534=ADVANCED_FACE('',(#1106,#353),#489,.F.);
#14535=ADVANCED_FACE('',(#1107),#13793,.T.);
#14536=ADVANCED_FACE('',(#1108,#354),#490,.T.);
#14537=ADVANCED_FACE('',(#1109),#491,.F.);
#14735=CLOSED_SHELL('',(#14445,#14446,#14447,#14448,#14449,#14450,#14451,
#14452,#14453,#14454,#14455,#14456,#14457,#14458,#14459,#14460,#14461,#14462,
#14463,#14464,#14465,#14466,#14467,#14468,#14469,#14470,#14471,#14472,#14473,
#14474,#14475,#14476,#14477,#14478,#14479,#14480,#14481,#14482,#14483,#14484,
#14485,#14486,#14487,#14488,#14489,#14490,#14491,#14492,#14493,#14494,#14495,
#14496,#14497,#14498,#14499,#14500,#14501,#14502,#14503,#14504,#14505,#14506,
#14507,#14508,#14509,#14510,#14511,#14512,#14513,#14514,#14515,#14516,#14517,
#14518,#14519,#14520,#14521,#14522,#14523,#14524,#14525,#14526,#14527,#14528,
#14529,#14530,#14531,#14532,#14533,#14534,#14535,#14536,#14537));
#15482=AXIS2_PLACEMENT_3D('',#50424,#17655,#17656);
#15483=AXIS2_PLACEMENT_3D('',#50425,#17657,#17658);
#15484=AXIS2_PLACEMENT_3D('',#50447,#17660,#17661);
#15485=AXIS2_PLACEMENT_3D('',#50458,#17662,#17663);
#15486=AXIS2_PLACEMENT_3D('',#50542,#17665,#17666);
#15487=AXIS2_PLACEMENT_3D('',#50632,#17668,#17669);
#15488=AXIS2_PLACEMENT_3D('',#50716,#17671,#17672);
#15489=AXIS2_PLACEMENT_3D('',#50806,#17674,#17675);
#15490=AXIS2_PLACEMENT_3D('',#50896,#17677,#17678);
#15491=AXIS2_PLACEMENT_3D('',#50980,#17680,#17681);
#15492=AXIS2_PLACEMENT_3D('',#51070,#17683,#17684);
#15493=AXIS2_PLACEMENT_3D('',#51154,#17686,#17687);
#15494=AXIS2_PLACEMENT_3D('',#51244,#17689,#17690);
#15495=AXIS2_PLACEMENT_3D('',#51328,#17692,#17693);
#15496=AXIS2_PLACEMENT_3D('',#51418,#17695,#17696);
#15497=AXIS2_PLACEMENT_3D('',#51508,#17698,#17699);
#15498=AXIS2_PLACEMENT_3D('',#51592,#17701,#17702);
#15499=AXIS2_PLACEMENT_3D('',#51682,#17704,#17705);
#15500=AXIS2_PLACEMENT_3D('',#51766,#17707,#17708);
#15501=AXIS2_PLACEMENT_3D('',#51856,#17710,#17711);
#15502=AXIS2_PLACEMENT_3D('',#51940,#17713,#17714);
#15503=AXIS2_PLACEMENT_3D('',#52027,#17716,#17717);
#15504=AXIS2_PLACEMENT_3D('',#52117,#17719,#17720);
#15505=AXIS2_PLACEMENT_3D('',#52201,#17722,#17723);
#15506=AXIS2_PLACEMENT_3D('',#52291,#17725,#17726);
#15507=AXIS2_PLACEMENT_3D('',#52375,#17728,#17729);
#15508=AXIS2_PLACEMENT_3D('',#52465,#17731,#17732);
#15509=AXIS2_PLACEMENT_3D('',#52552,#17734,#17735);
#15510=AXIS2_PLACEMENT_3D('',#52639,#17737,#17738);
#15511=AXIS2_PLACEMENT_3D('',#52729,#17740,#17741);
#15512=AXIS2_PLACEMENT_3D('',#52813,#17743,#17744);
#15513=AXIS2_PLACEMENT_3D('',#52903,#17746,#17747);
#15514=AXIS2_PLACEMENT_3D('',#52987,#17749,#17750);
#15515=AXIS2_PLACEMENT_3D('',#53077,#17752,#17753);
#15516=AXIS2_PLACEMENT_3D('',#53164,#17755,#17756);
#15517=AXIS2_PLACEMENT_3D('',#53251,#17758,#17759);
#15518=AXIS2_PLACEMENT_3D('',#53341,#17761,#17762);
#15519=AXIS2_PLACEMENT_3D('',#53425,#17764,#17765);
#15520=AXIS2_PLACEMENT_3D('',#53515,#17767,#17768);
#15521=AXIS2_PLACEMENT_3D('',#53517,#17769,#17770);
#15522=AXIS2_PLACEMENT_3D('',#53521,#17772,#17773);
#15523=AXIS2_PLACEMENT_3D('',#53558,#17775,#17776);
#15524=AXIS2_PLACEMENT_3D('',#53559,#17777,#17778);
#15525=AXIS2_PLACEMENT_3D('',#53580,#17780,#17781);
#15526=AXIS2_PLACEMENT_3D('',#53594,#17782,#17783);
#15527=AXIS2_PLACEMENT_3D('',#53631,#17785,#17786);
#15528=AXIS2_PLACEMENT_3D('',#53668,#17788,#17789);
#15529=AXIS2_PLACEMENT_3D('',#53705,#17791,#17792);
#15530=AXIS2_PLACEMENT_3D('',#53743,#17794,#17795);
#15531=AXIS2_PLACEMENT_3D('',#53779,#17797,#17798);
#15532=AXIS2_PLACEMENT_3D('',#53817,#17800,#17801);
#15533=AXIS2_PLACEMENT_3D('',#53854,#17803,#17804);
#15534=AXIS2_PLACEMENT_3D('',#53891,#17806,#17807);
#15535=AXIS2_PLACEMENT_3D('',#53928,#17809,#17810);
#15536=AXIS2_PLACEMENT_3D('',#53965,#17812,#17813);
#15537=AXIS2_PLACEMENT_3D('',#54003,#17815,#17816);
#15538=AXIS2_PLACEMENT_3D('',#54039,#17818,#17819);
#15539=AXIS2_PLACEMENT_3D('',#54077,#17821,#17822);
#15540=AXIS2_PLACEMENT_3D('',#54114,#17824,#17825);
#15541=AXIS2_PLACEMENT_3D('',#54151,#17827,#17828);
#15542=AXIS2_PLACEMENT_3D('',#54188,#17830,#17831);
#15543=AXIS2_PLACEMENT_3D('',#54225,#17833,#17834);
#15544=AXIS2_PLACEMENT_3D('',#54263,#17836,#17837);
#15545=AXIS2_PLACEMENT_3D('',#54299,#17839,#17840);
#15546=AXIS2_PLACEMENT_3D('',#54337,#17842,#17843);
#15547=AXIS2_PLACEMENT_3D('',#54374,#17845,#17846);
#15548=AXIS2_PLACEMENT_3D('',#54411,#17848,#17849);
#15549=AXIS2_PLACEMENT_3D('',#54448,#17851,#17852);
#15550=AXIS2_PLACEMENT_3D('',#54485,#17854,#17855);
#15551=AXIS2_PLACEMENT_3D('',#54523,#17857,#17858);
#15552=AXIS2_PLACEMENT_3D('',#54560,#17860,#17861);
#15553=AXIS2_PLACEMENT_3D('',#54597,#17863,#17864);
#15554=AXIS2_PLACEMENT_3D('',#54634,#17866,#17867);
#15555=AXIS2_PLACEMENT_3D('',#54671,#17869,#17870);
#15556=AXIS2_PLACEMENT_3D('',#54708,#17872,#17873);
#15557=AXIS2_PLACEMENT_3D('',#54745,#17875,#17876);
#15558=AXIS2_PLACEMENT_3D('',#54783,#17878,#17879);
#15559=AXIS2_PLACEMENT_3D('',#54820,#17881,#17882);
#15560=AXIS2_PLACEMENT_3D('',#54857,#17884,#17885);
#15561=AXIS2_PLACEMENT_3D('',#54894,#17887,#17888);
#15562=AXIS2_PLACEMENT_3D('',#54903,#17893,#17894);
#15563=AXIS2_PLACEMENT_3D('',#54909,#17898,#17899);
#15564=AXIS2_PLACEMENT_3D('',#54915,#17903,#17904);
#15565=AXIS2_PLACEMENT_3D('',#54921,#17908,#17909);
#15566=AXIS2_PLACEMENT_3D('',#54927,#17913,#17914);
#15567=AXIS2_PLACEMENT_3D('',#54930,#17917,#17918);
#15568=AXIS2_PLACEMENT_3D('',#54931,#17919,#17920);
#15569=AXIS2_PLACEMENT_3D('',#54933,#17921,#17922);
#15570=AXIS2_PLACEMENT_3D('',#54936,#17924,#17925);
#15571=AXIS2_PLACEMENT_3D('',#54937,#17926,#17927);
#15572=AXIS2_PLACEMENT_3D('',#54938,#17928,#17929);
#15573=AXIS2_PLACEMENT_3D('',#54940,#17930,#17931);
#15574=AXIS2_PLACEMENT_3D('',#54941,#17932,#17933);
#15575=AXIS2_PLACEMENT_3D('',#54943,#17934,#17935);
#15576=AXIS2_PLACEMENT_3D('',#54945,#17937,#17938);
#15577=AXIS2_PLACEMENT_3D('',#57196,#17939,#17940);
#15578=AXIS2_PLACEMENT_3D('',#57198,#17941,#17942);
#15579=AXIS2_PLACEMENT_3D('',#59225,#17943,#17944);
#15580=AXIS2_PLACEMENT_3D('',#59226,#17945,#17946);
#15581=AXIS2_PLACEMENT_3D('',#59228,#17947,#17948);
#15582=AXIS2_PLACEMENT_3D('',#59229,#17949,#17950);
#15583=AXIS2_PLACEMENT_3D('',#59231,#17951,#17952);
#15584=AXIS2_PLACEMENT_3D('',#59233,#17954,#17955);
#15585=AXIS2_PLACEMENT_3D('',#59234,#17956,#17957);
#17655=DIRECTION('axis',(0.,0.,1.));
#17656=DIRECTION('refdir',(1.,0.,0.));
#17657=DIRECTION('center_axis',(0.,0.,1.));
#17658=DIRECTION('ref_axis',(1.,0.,0.));
#17659=DIRECTION('',(0.,0.,-1.));
#17660=DIRECTION('center_axis',(0.,0.,-1.));
#17661=DIRECTION('ref_axis',(1.,0.,0.));
#17662=DIRECTION('center_axis',(0.,0.,1.));
#17663=DIRECTION('ref_axis',(1.,0.,0.));
#17664=DIRECTION('',(0.,0.,-1.));
#17665=DIRECTION('center_axis',(0.,0.,1.));
#17666=DIRECTION('ref_axis',(1.,0.,0.));
#17667=DIRECTION('',(0.,0.,-1.));
#17668=DIRECTION('center_axis',(0.,0.,1.));
#17669=DIRECTION('ref_axis',(1.,0.,0.));
#17670=DIRECTION('',(0.,0.,-1.));
#17671=DIRECTION('center_axis',(0.,0.,1.));
#17672=DIRECTION('ref_axis',(1.,0.,0.));
#17673=DIRECTION('',(0.,0.,-1.));
#17674=DIRECTION('center_axis',(0.,0.,1.));
#17675=DIRECTION('ref_axis',(1.,0.,0.));
#17676=DIRECTION('',(0.,0.,-1.));
#17677=DIRECTION('center_axis',(0.,0.,1.));
#17678=DIRECTION('ref_axis',(1.,0.,0.));
#17679=DIRECTION('',(0.,0.,-1.));
#17680=DIRECTION('center_axis',(0.,0.,1.));
#17681=DIRECTION('ref_axis',(1.,0.,0.));
#17682=DIRECTION('',(0.,0.,-1.));
#17683=DIRECTION('center_axis',(0.,0.,1.));
#17684=DIRECTION('ref_axis',(1.,0.,0.));
#17685=DIRECTION('',(0.,0.,-1.));
#17686=DIRECTION('center_axis',(0.,0.,1.));
#17687=DIRECTION('ref_axis',(1.,0.,0.));
#17688=DIRECTION('',(0.,0.,-1.));
#17689=DIRECTION('center_axis',(0.,0.,1.));
#17690=DIRECTION('ref_axis',(1.,0.,0.));
#17691=DIRECTION('',(0.,0.,-1.));
#17692=DIRECTION('center_axis',(0.,0.,1.));
#17693=DIRECTION('ref_axis',(1.,0.,0.));
#17694=DIRECTION('',(0.,0.,-1.));
#17695=DIRECTION('center_axis',(0.,0.,1.));
#17696=DIRECTION('ref_axis',(1.,0.,0.));
#17697=DIRECTION('',(0.,0.,-1.));
#17698=DIRECTION('center_axis',(0.,0.,1.));
#17699=DIRECTION('ref_axis',(1.,0.,0.));
#17700=DIRECTION('',(0.,0.,-1.));
#17701=DIRECTION('center_axis',(0.,0.,1.));
#17702=DIRECTION('ref_axis',(1.,0.,0.));
#17703=DIRECTION('',(0.,0.,-1.));
#17704=DIRECTION('center_axis',(0.,0.,1.));
#17705=DIRECTION('ref_axis',(1.,0.,0.));
#17706=DIRECTION('',(0.,0.,-1.));
#17707=DIRECTION('center_axis',(0.,0.,1.));
#17708=DIRECTION('ref_axis',(1.,0.,0.));
#17709=DIRECTION('',(0.,0.,-1.));
#17710=DIRECTION('center_axis',(0.,0.,1.));
#17711=DIRECTION('ref_axis',(1.,0.,0.));
#17712=DIRECTION('',(0.,0.,-1.));
#17713=DIRECTION('center_axis',(0.,0.,1.));
#17714=DIRECTION('ref_axis',(1.,0.,0.));
#17715=DIRECTION('',(0.,0.,-1.));
#17716=DIRECTION('center_axis',(0.,0.,1.));
#17717=DIRECTION('ref_axis',(1.,0.,0.));
#17718=DIRECTION('',(0.,0.,-1.));
#17719=DIRECTION('center_axis',(0.,0.,1.));
#17720=DIRECTION('ref_axis',(1.,0.,0.));
#17721=DIRECTION('',(0.,0.,-1.));
#17722=DIRECTION('center_axis',(0.,0.,1.));
#17723=DIRECTION('ref_axis',(1.,0.,0.));
#17724=DIRECTION('',(0.,0.,-1.));
#17725=DIRECTION('center_axis',(0.,0.,1.));
#17726=DIRECTION('ref_axis',(1.,0.,0.));
#17727=DIRECTION('',(0.,0.,-1.));
#17728=DIRECTION('center_axis',(0.,0.,1.));
#17729=DIRECTION('ref_axis',(1.,0.,0.));
#17730=DIRECTION('',(0.,0.,-1.));
#17731=DIRECTION('center_axis',(0.,0.,1.));
#17732=DIRECTION('ref_axis',(1.,0.,0.));
#17733=DIRECTION('',(0.,0.,-1.));
#17734=DIRECTION('center_axis',(0.,0.,1.));
#17735=DIRECTION('ref_axis',(1.,0.,0.));
#17736=DIRECTION('',(0.,0.,-1.));
#17737=DIRECTION('center_axis',(0.,0.,1.));
#17738=DIRECTION('ref_axis',(1.,0.,0.));
#17739=DIRECTION('',(0.,0.,-1.));
#17740=DIRECTION('center_axis',(0.,0.,1.));
#17741=DIRECTION('ref_axis',(1.,0.,0.));
#17742=DIRECTION('',(0.,0.,-1.));
#17743=DIRECTION('center_axis',(0.,0.,1.));
#17744=DIRECTION('ref_axis',(1.,0.,0.));
#17745=DIRECTION('',(0.,0.,-1.));
#17746=DIRECTION('center_axis',(0.,0.,1.));
#17747=DIRECTION('ref_axis',(1.,0.,0.));
#17748=DIRECTION('',(0.,0.,-1.));
#17749=DIRECTION('center_axis',(0.,0.,1.));
#17750=DIRECTION('ref_axis',(1.,0.,0.));
#17751=DIRECTION('',(0.,0.,-1.));
#17752=DIRECTION('center_axis',(0.,0.,1.));
#17753=DIRECTION('ref_axis',(1.,0.,0.));
#17754=DIRECTION('',(0.,0.,-1.));
#17755=DIRECTION('center_axis',(0.,0.,1.));
#17756=DIRECTION('ref_axis',(1.,0.,0.));
#17757=DIRECTION('',(0.,0.,-1.));
#17758=DIRECTION('center_axis',(0.,0.,1.));
#17759=DIRECTION('ref_axis',(1.,0.,0.));
#17760=DIRECTION('',(0.,0.,-1.));
#17761=DIRECTION('center_axis',(0.,0.,1.));
#17762=DIRECTION('ref_axis',(1.,0.,0.));
#17763=DIRECTION('',(0.,0.,-1.));
#17764=DIRECTION('center_axis',(0.,0.,1.));
#17765=DIRECTION('ref_axis',(1.,0.,0.));
#17766=DIRECTION('',(0.,0.,-1.));
#17767=DIRECTION('center_axis',(0.,0.,1.));
#17768=DIRECTION('ref_axis',(1.,0.,0.));
#17769=DIRECTION('center_axis',(0.,0.,-1.));
#17770=DIRECTION('ref_axis',(1.,0.,0.));
#17771=DIRECTION('',(0.,0.,-1.));
#17772=DIRECTION('center_axis',(0.,0.,1.));
#17773=DIRECTION('ref_axis',(1.,0.,0.));
#17774=DIRECTION('',(0.,0.,-1.));
#17775=DIRECTION('center_axis',(0.,0.,1.));
#17776=DIRECTION('ref_axis',(1.,0.,0.));
#17777=DIRECTION('center_axis',(0.,0.,1.));
#17778=DIRECTION('ref_axis',(0.968645259382149,-0.248447904954922,0.));
#17779=DIRECTION('',(0.,0.,1.));
#17780=DIRECTION('center_axis',(0.,0.,1.));
#17781=DIRECTION('ref_axis',(1.,-3.01021172098358E-13,0.));
#17782=DIRECTION('center_axis',(0.,0.,1.));
#17783=DIRECTION('ref_axis',(1.,-3.01021172098358E-13,0.));
#17784=DIRECTION('',(0.,0.,1.));
#17785=DIRECTION('center_axis',(0.,0.,1.));
#17786=DIRECTION('ref_axis',(1.,-3.01021172098358E-13,0.));
#17787=DIRECTION('',(0.,0.,1.));
#17788=DIRECTION('center_axis',(0.,0.,1.));
#17789=DIRECTION('ref_axis',(1.,-3.01021172098358E-13,0.));
#17790=DIRECTION('',(0.,0.,1.));
#17791=DIRECTION('center_axis',(0.,0.,1.));
#17792=DIRECTION('ref_axis',(1.,-3.01021172098358E-13,0.));
#17793=DIRECTION('',(0.,0.,1.));
#17794=DIRECTION('center_axis',(0.,0.,1.));
#17795=DIRECTION('ref_axis',(1.,-3.01021172098358E-13,0.));
#17796=DIRECTION('',(0.,0.,1.));
#17797=DIRECTION('center_axis',(0.,0.,1.));
#17798=DIRECTION('ref_axis',(1.,-3.01021172098358E-13,0.));
#17799=DIRECTION('',(0.,0.,1.));
#17800=DIRECTION('center_axis',(0.,0.,1.));
#17801=DIRECTION('ref_axis',(1.,-3.01021172098358E-13,0.));
#17802=DIRECTION('',(0.,0.,1.));
#17803=DIRECTION('center_axis',(0.,0.,1.));
#17804=DIRECTION('ref_axis',(1.,-3.01021172098358E-13,0.));
#17805=DIRECTION('',(0.,0.,1.));
#17806=DIRECTION('center_axis',(0.,0.,1.));
#17807=DIRECTION('ref_axis',(1.,-3.01021172098358E-13,0.));
#17808=DIRECTION('',(0.,0.,1.));
#17809=DIRECTION('center_axis',(0.,0.,1.));
#17810=DIRECTION('ref_axis',(1.,-3.01021172098358E-13,0.));
#17811=DIRECTION('',(0.,0.,1.));
#17812=DIRECTION('center_axis',(0.,0.,1.));
#17813=DIRECTION('ref_axis',(1.,-3.01021172098358E-13,0.));
#17814=DIRECTION('',(0.,0.,1.));
#17815=DIRECTION('center_axis',(0.,0.,1.));
#17816=DIRECTION('ref_axis',(1.,-3.01021172098358E-13,0.));
#17817=DIRECTION('',(0.,0.,1.));
#17818=DIRECTION('center_axis',(0.,0.,1.));
#17819=DIRECTION('ref_axis',(1.,-3.01021172098358E-13,0.));
#17820=DIRECTION('',(0.,0.,1.));
#17821=DIRECTION('center_axis',(0.,0.,1.));
#17822=DIRECTION('ref_axis',(1.,-3.01021172098358E-13,0.));
#17823=DIRECTION('',(0.,0.,1.));
#17824=DIRECTION('center_axis',(0.,0.,1.));
#17825=DIRECTION('ref_axis',(1.,-3.01021172098358E-13,0.));
#17826=DIRECTION('',(0.,0.,1.));
#17827=DIRECTION('center_axis',(0.,0.,1.));
#17828=DIRECTION('ref_axis',(1.,-3.01021172098358E-13,0.));
#17829=DIRECTION('',(0.,0.,1.));
#17830=DIRECTION('center_axis',(0.,0.,1.));
#17831=DIRECTION('ref_axis',(1.,-3.01021172098358E-13,0.));
#17832=DIRECTION('',(0.,0.,1.));
#17833=DIRECTION('center_axis',(0.,0.,1.));
#17834=DIRECTION('ref_axis',(1.,-3.01021172098358E-13,0.));
#17835=DIRECTION('',(0.,0.,1.));
#17836=DIRECTION('center_axis',(0.,0.,1.));
#17837=DIRECTION('ref_axis',(1.,-3.01021172098358E-13,0.));
#17838=DIRECTION('',(0.,0.,1.));
#17839=DIRECTION('center_axis',(0.,0.,1.));
#17840=DIRECTION('ref_axis',(1.,-3.01021172098358E-13,0.));
#17841=DIRECTION('',(0.,0.,1.));
#17842=DIRECTION('center_axis',(0.,0.,1.));
#17843=DIRECTION('ref_axis',(1.,-3.01021172098358E-13,0.));
#17844=DIRECTION('',(0.,0.,1.));
#17845=DIRECTION('center_axis',(0.,0.,1.));
#17846=DIRECTION('ref_axis',(1.,-3.01021172098358E-13,0.));
#17847=DIRECTION('',(0.,0.,1.));
#17848=DIRECTION('center_axis',(0.,0.,1.));
#17849=DIRECTION('ref_axis',(1.,-3.01021172098358E-13,0.));
#17850=DIRECTION('',(0.,0.,1.));
#17851=DIRECTION('center_axis',(0.,0.,1.));
#17852=DIRECTION('ref_axis',(1.,-3.01021172098358E-13,0.));
#17853=DIRECTION('',(0.,0.,1.));
#17854=DIRECTION('center_axis',(0.,0.,1.));
#17855=DIRECTION('ref_axis',(1.,-3.01021172098358E-13,0.));
#17856=DIRECTION('',(0.,0.,1.));
#17857=DIRECTION('center_axis',(0.,0.,1.));
#17858=DIRECTION('ref_axis',(1.,-3.01021172098358E-13,0.));
#17859=DIRECTION('',(0.,0.,1.));
#17860=DIRECTION('center_axis',(0.,0.,1.));
#17861=DIRECTION('ref_axis',(1.,-3.01021172098358E-13,0.));
#17862=DIRECTION('',(0.,0.,1.));
#17863=DIRECTION('center_axis',(0.,0.,1.));
#17864=DIRECTION('ref_axis',(1.,-3.01021172098358E-13,0.));
#17865=DIRECTION('',(0.,0.,1.));
#17866=DIRECTION('center_axis',(0.,0.,1.));
#17867=DIRECTION('ref_axis',(1.,-3.01021172098358E-13,0.));
#17868=DIRECTION('',(0.,0.,1.));
#17869=DIRECTION('center_axis',(0.,0.,1.));
#17870=DIRECTION('ref_axis',(1.,-3.01021172098358E-13,0.));
#17871=DIRECTION('',(0.,0.,1.));
#17872=DIRECTION('center_axis',(0.,0.,1.));
#17873=DIRECTION('ref_axis',(1.,-3.01021172098358E-13,0.));
#17874=DIRECTION('',(0.,0.,1.));
#17875=DIRECTION('center_axis',(0.,0.,1.));
#17876=DIRECTION('ref_axis',(1.,-3.01021172098358E-13,0.));
#17877=DIRECTION('',(0.,0.,1.));
#17878=DIRECTION('center_axis',(0.,0.,1.));
#17879=DIRECTION('ref_axis',(1.,-3.01021172098358E-13,0.));
#17880=DIRECTION('',(0.,0.,1.));
#17881=DIRECTION('center_axis',(0.,0.,1.));
#17882=DIRECTION('ref_axis',(1.,-3.01021172098358E-13,0.));
#17883=DIRECTION('',(0.,0.,1.));
#17884=DIRECTION('center_axis',(0.,0.,1.));
#17885=DIRECTION('ref_axis',(1.,-3.01021172098358E-13,0.));
#17886=DIRECTION('',(0.,0.,1.));
#17887=DIRECTION('center_axis',(0.866025403784439,0.5,0.));
#17888=DIRECTION('ref_axis',(0.5,-0.866025403784439,0.));
#17889=DIRECTION('',(0.5,-0.866025403784439,0.));
#17890=DIRECTION('',(0.,0.,-1.));
#17891=DIRECTION('',(0.5,-0.866025403784439,0.));
#17892=DIRECTION('',(0.,0.,-1.));
#17893=DIRECTION('center_axis',(1.20185167898973E-16,1.,0.));
#17894=DIRECTION('ref_axis',(1.,-1.20185167898973E-16,0.));
#17895=DIRECTION('',(1.,-1.20185167898973E-16,0.));
#17896=DIRECTION('',(0.,0.,-1.));
#17897=DIRECTION('',(1.,-1.20185167898973E-16,0.));
#17898=DIRECTION('center_axis',(-0.866025403784439,0.5,0.));
#17899=DIRECTION('ref_axis',(0.5,0.866025403784439,0.));
#17900=DIRECTION('',(0.5,0.866025403784439,0.));
#17901=DIRECTION('',(0.,0.,-1.));
#17902=DIRECTION('',(0.5,0.866025403784439,0.));
#17903=DIRECTION('center_axis',(-0.866025403784439,-0.5,0.));
#17904=DIRECTION('ref_axis',(-0.5,0.866025403784439,0.));
#17905=DIRECTION('',(-0.5,0.866025403784439,0.));
#17906=DIRECTION('',(0.,0.,-1.));
#17907=DIRECTION('',(-0.5,0.866025403784439,0.));
#17908=DIRECTION('center_axis',(-2.40370335797945E-16,-1.,0.));
#17909=DIRECTION('ref_axis',(-1.,2.40370335797945E-16,0.));
#17910=DIRECTION('',(-1.,2.40370335797945E-16,0.));
#17911=DIRECTION('',(0.,0.,-1.));
#17912=DIRECTION('',(-1.,2.40370335797945E-16,0.));
#17913=DIRECTION('center_axis',(0.866025403784439,-0.5,0.));
#17914=DIRECTION('ref_axis',(-0.5,-0.866025403784439,0.));
#17915=DIRECTION('',(-0.5,-0.866025403784439,0.));
#17916=DIRECTION('',(-0.5,-0.866025403784439,0.));
#17917=DIRECTION('center_axis',(0.,0.,-1.));
#17918=DIRECTION('ref_axis',(-1.,0.,0.));
#17919=DIRECTION('center_axis',(0.,0.,1.));
#17920=DIRECTION('ref_axis',(1.,0.,0.));
#17921=DIRECTION('center_axis',(0.,0.,1.));
#17922=DIRECTION('ref_axis',(1.,0.,0.));
#17923=DIRECTION('',(0.,0.,1.));
#17924=DIRECTION('center_axis',(0.,0.,1.));
#17925=DIRECTION('ref_axis',(1.,0.,0.));
#17926=DIRECTION('center_axis',(0.,0.,-1.));
#17927=DIRECTION('ref_axis',(-1.,0.,0.));
#17928=DIRECTION('center_axis',(0.,0.,1.));
#17929=DIRECTION('ref_axis',(1.,0.,0.));
#17930=DIRECTION('center_axis',(0.,0.,1.));
#17931=DIRECTION('ref_axis',(1.,0.,0.));
#17932=DIRECTION('center_axis',(0.,0.,1.));
#17933=DIRECTION('ref_axis',(1.,0.,0.));
#17934=DIRECTION('center_axis',(0.,0.,-1.));
#17935=DIRECTION('ref_axis',(1.,0.,0.));
#17936=DIRECTION('',(0.,0.,-1.));
#17937=DIRECTION('center_axis',(0.,0.,1.));
#17938=DIRECTION('ref_axis',(1.,0.,0.));
#17939=DIRECTION('center_axis',(0.,0.,1.));
#17940=DIRECTION('ref_axis',(0.889074521506822,0.457762487767855,0.));
#17941=DIRECTION('center_axis',(0.,0.,-1.));
#17942=DIRECTION('ref_axis',(1.,-3.01021172098358E-13,0.));
#17943=DIRECTION('center_axis',(0.,0.,1.));
#17944=DIRECTION('ref_axis',(1.,0.,0.));
#17945=DIRECTION('center_axis',(0.,0.,1.));
#17946=DIRECTION('ref_axis',(1.,0.,0.));
#17947=DIRECTION('center_axis',(0.,0.,1.));
#17948=DIRECTION('ref_axis',(1.,0.,0.));
#17949=DIRECTION('center_axis',(0.,0.,1.));
#17950=DIRECTION('ref_axis',(1.,0.,0.));
#17951=DIRECTION('center_axis',(0.,0.,1.));
#17952=DIRECTION('ref_axis',(1.,0.,0.));
#17953=DIRECTION('',(0.,0.,-1.));
#17954=DIRECTION('center_axis',(0.,0.,1.));
#17955=DIRECTION('ref_axis',(1.,0.,0.));
#17956=DIRECTION('center_axis',(0.,0.,1.));
#17957=DIRECTION('ref_axis',(1.,0.,0.));
#50424=CARTESIAN_POINT('',(0.,0.,0.));
#50425=CARTESIAN_POINT('Origin',(0.,0.,0.));
#50426=CARTESIAN_POINT('',(-5.91687703775647,0.000148475150406543,0.563375192204898));
#50427=CARTESIAN_POINT('',(-5.91673042899974,9.84771958866994E-5,0.311624807795177));
#50428=CARTESIAN_POINT('',(-5.91675,-7.2459289488551E-16,0.));
#50429=CARTESIAN_POINT('',(2.58391981634401,5.32271443393357,0.));
#50430=CARTESIAN_POINT('Ctrl Pts',(-5.91687703775647,0.000148475150406543,
0.563375192204898));
#50431=CARTESIAN_POINT('Ctrl Pts',(-5.91706992944422,0.187583717190912,
0.554551266666524));
#50432=CARTESIAN_POINT('Ctrl Pts',(-5.90834010273356,0.37500100085716,0.54572734112815));
#50433=CARTESIAN_POINT('Ctrl Pts',(-5.89055564988372,0.561555006704539,
0.536903415589775));
#50434=CARTESIAN_POINT('Ctrl Pts',(-5.79705517096023,1.54234924530742,0.490512263115791));
#50435=CARTESIAN_POINT('Ctrl Pts',(-5.4532798607574,2.49928201164809,0.444121110641807));
#50436=CARTESIAN_POINT('Ctrl Pts',(-4.90126263075179,3.31535838460278,0.397729958167823));
#50437=CARTESIAN_POINT('Ctrl Pts',(-4.34924540074619,4.13143475755746,0.351338805693839));
#50438=CARTESIAN_POINT('Ctrl Pts',(-3.5889862509378,4.80665473712616,0.304947653219855));
#50439=CARTESIAN_POINT('Ctrl Pts',(-2.71343949032745,5.25844743535226,0.258556500745871));
#50440=CARTESIAN_POINT('Ctrl Pts',(-1.83789272971711,5.71024013357837,0.212165348271887));
#50441=CARTESIAN_POINT('Ctrl Pts',(-0.847058358304818,5.93860555046189,
0.165774195797903));
#50442=CARTESIAN_POINT('Ctrl Pts',(0.137915404672155,5.91564817616819,0.119383043323919));
#50443=CARTESIAN_POINT('Ctrl Pts',(0.982826263370534,5.89595533199605,0.0795886955492792));
#50444=CARTESIAN_POINT('Ctrl Pts',(1.82342476052313,5.69133378081125,0.0397943477746398));
#50445=CARTESIAN_POINT('Ctrl Pts',(2.58415070483638,5.32291852118006,2.34187669256869E-16));
#50446=CARTESIAN_POINT('',(-2.58391981634374,5.3227144339337,0.));
#50447=CARTESIAN_POINT('Origin',(0.,0.,0.));
#50448=CARTESIAN_POINT('Ctrl Pts',(-2.58391981634373,5.3227144339337,-1.4432899320127E-14));
#50449=CARTESIAN_POINT('Ctrl Pts',(-3.47048393011347,4.89233053668302,0.0463911524739698));
#50450=CARTESIAN_POINT('Ctrl Pts',(-4.24698760664896,4.23637732443745,0.0927823049479542));
#50451=CARTESIAN_POINT('Ctrl Pts',(-4.81877652593489,3.43418004707672,0.139173457421938));
#50452=CARTESIAN_POINT('Ctrl Pts',(-5.39056544522082,2.63198276971599,0.185564609895923));
#50453=CARTESIAN_POINT('Ctrl Pts',(-5.7576396072572,1.6835414272401,0.231955762369907));
#50454=CARTESIAN_POINT('Ctrl Pts',(-5.8750816086466,0.705274673425957,0.278346914843891));
#50455=CARTESIAN_POINT('Ctrl Pts',(-5.9031632732299,0.471360413377589,0.289439545827653));
#50456=CARTESIAN_POINT('Ctrl Pts',(-5.91697246107877,0.235740914355538,
0.300532176811415));
#50457=CARTESIAN_POINT('Ctrl Pts',(-5.91673042899974,9.84771958866994E-5,
0.311624807795177));
#50458=CARTESIAN_POINT('Origin',(0.,0.,0.));
#50459=CARTESIAN_POINT('',(-5.91673471741553,-0.000155036278603748,2.3133751922049));
#50460=CARTESIAN_POINT('',(-5.91688804929001,-0.00014628683568293,2.06162480779517));
#50461=CARTESIAN_POINT('',(-5.91675,-7.2459289488551E-16,0.));
#50462=CARTESIAN_POINT('Ctrl Pts',(-5.91673471741553,-0.000155036278603748,
2.3133751922049));
#50463=CARTESIAN_POINT('Ctrl Pts',(-5.91595960263358,0.753200890966211,
2.277911763021));
#50464=CARTESIAN_POINT('Ctrl Pts',(-5.7715386236145,1.50684545302749,2.2424483338371));
#50465=CARTESIAN_POINT('Ctrl Pts',(-5.49078916335747,2.20572500170222,2.2069849046532));
#50466=CARTESIAN_POINT('Ctrl Pts',(-5.12352938849944,3.11995773242299,2.16059375217922));
#50467=CARTESIAN_POINT('Ctrl Pts',(-4.52297996781033,3.94047482528974,2.11420259970523));
#50468=CARTESIAN_POINT('Ctrl Pts',(-3.7625685915058,4.56695369006312,2.06781144723125));
#50469=CARTESIAN_POINT('Ctrl Pts',(-3.00215721520126,5.19343255483651,2.02142029475727));
#50470=CARTESIAN_POINT('Ctrl Pts',(-2.0818838832813,5.62587319151652,1.97502914228328));
#50471=CARTESIAN_POINT('Ctrl Pts',(-1.11426813628014,5.81140215018564,1.9286379898093));
#50472=CARTESIAN_POINT('Ctrl Pts',(-0.14665238927898,5.99693110885477,1.88224683733531));
#50473=CARTESIAN_POINT('Ctrl Pts',(0.868305772803379,5.93554838951301,1.83585568486133));
#50474=CARTESIAN_POINT('Ctrl Pts',(1.80650992910795,5.63475911385226,1.78946453238734));
#50475=CARTESIAN_POINT('Ctrl Pts',(2.74471408541252,5.33396983819152,1.74307337991336));
#50476=CARTESIAN_POINT('Ctrl Pts',(3.6061642359393,4.79377400621179,1.69668222743938));
#50477=CARTESIAN_POINT('Ctrl Pts',(4.28553300547993,4.08022000735929,1.65029107496539));
#50478=CARTESIAN_POINT('Ctrl Pts',(4.96490177502057,3.36666600850679,1.60389992249141));
#50479=CARTESIAN_POINT('Ctrl Pts',(5.46218916357505,2.47975384278151,1.55750877001742));
#50480=CARTESIAN_POINT('Ctrl Pts',(5.71659307223213,1.52792409666675,1.51111761754344));
#50481=CARTESIAN_POINT('Ctrl Pts',(5.97099698088921,0.57609435055201,1.46472646506946));
#50482=CARTESIAN_POINT('Ctrl Pts',(5.98251740964889,-0.440652975952207,
1.41833531259547));
#50483=CARTESIAN_POINT('Ctrl Pts',(5.74974578753971,-1.39800276984277,1.37194416012149));
#50484=CARTESIAN_POINT('Ctrl Pts',(5.51697416543054,-2.35535256373333,1.3255530076475));
#50485=CARTESIAN_POINT('Ctrl Pts',(5.03991049245251,-3.25330482501024,1.27916185517352));
#50486=CARTESIAN_POINT('Ctrl Pts',(4.37688415573885,-3.98206902990049,1.23277070269954));
#50487=CARTESIAN_POINT('Ctrl Pts',(3.71385781902519,-4.71083323479075,1.18637955022555));
#50488=CARTESIAN_POINT('Ctrl Pts',(2.86486881857591,-5.27040938329436,1.13998839775157));
#50489=CARTESIAN_POINT('Ctrl Pts',(1.93372094913206,-5.59237972963765,1.09359724527758));
#50490=CARTESIAN_POINT('Ctrl Pts',(1.0025730796882,-5.91435007598094,1.0472060928036));
#50491=CARTESIAN_POINT('Ctrl Pts',(-0.0107336587502209,-5.9987146201639,
1.00081494032962));
#50492=CARTESIAN_POINT('Ctrl Pts',(-0.982304785849564,-5.83515784283796,
0.954423787855632));
#50493=CARTESIAN_POINT('Ctrl Pts',(-1.95387591294891,-5.67160106551203,
0.908032635381648));
#50494=CARTESIAN_POINT('Ctrl Pts',(-2.88371142870917,-5.2601229666772,0.861641482907664));
#50495=CARTESIAN_POINT('Ctrl Pts',(-3.65812259986032,-4.65103488155748,
0.81525033043368));
#50496=CARTESIAN_POINT('Ctrl Pts',(-4.43253377101147,-4.04194679643775,
0.768859177959696));
#50497=CARTESIAN_POINT('Ctrl Pts',(-5.05152059755351,-3.23524872503314,
0.722468025485712));
#50498=CARTESIAN_POINT('Ctrl Pts',(-5.43940118700244,-2.32957183389829,
0.676076873011728));
#50499=CARTESIAN_POINT('Ctrl Pts',(-5.75350414307619,-1.59616109747218,
0.638509646076118));
#50500=CARTESIAN_POINT('Ctrl Pts',(-5.91605581529983,-0.797843557176284,
0.600942419140508));
#50501=CARTESIAN_POINT('Ctrl Pts',(-5.91687703775647,0.000148475150406543,
0.563375192204898));
#50502=CARTESIAN_POINT('Ctrl Pts',(-5.91673042899974,9.84771958866994E-5,
0.311624807795177));
#50503=CARTESIAN_POINT('Ctrl Pts',(-5.91596024431085,-0.749753351848488,
0.346923329285399));
#50504=CARTESIAN_POINT('Ctrl Pts',(-5.77290544891175,-1.49983745567011,
0.382221850775621));
#50505=CARTESIAN_POINT('Ctrl Pts',(-5.49469559885405,-2.1959450698255,0.417520372265843));
#50506=CARTESIAN_POINT('Ctrl Pts',(-5.12905774692967,-3.11080589411043,
0.463911524739827));
#50507=CARTESIAN_POINT('Ctrl Pts',(-4.5299722023385,-3.93243537752791,0.510302677213811));
#50508=CARTESIAN_POINT('Ctrl Pts',(-3.77067614149761,-4.56027540020292,
0.556693829687796));
#50509=CARTESIAN_POINT('Ctrl Pts',(-3.01138008065672,-5.18811542287793,
0.60308498216178));
#50510=CARTESIAN_POINT('Ctrl Pts',(-2.09187350356611,-5.62216598481048,
0.649476134635763));
#50511=CARTESIAN_POINT('Ctrl Pts',(-1.12458814094342,-5.80940752171066,
0.695867287109747));
#50512=CARTESIAN_POINT('Ctrl Pts',(-0.157302778320717,-5.99664905861084,
0.742258439583731));
#50513=CARTESIAN_POINT('Ctrl Pts',(0.857761369834063,-5.93708157047865,
0.788649592057716));
#50514=CARTESIAN_POINT('Ctrl Pts',(1.79649797196632,-5.63796225118424,0.8350407445317));
#50515=CARTESIAN_POINT('Ctrl Pts',(2.73523457409856,-5.33884293188984,0.881431897005684));
#50516=CARTESIAN_POINT('Ctrl Pts',(3.59764363020828,-4.80017178143322,0.927823049479668));
#50517=CARTESIAN_POINT('Ctrl Pts',(4.27827895860187,-4.08782410095791,0.974214201953652));
#50518=CARTESIAN_POINT('Ctrl Pts',(4.95891428699546,-3.37547642048261,1.02060535442764));
#50519=CARTESIAN_POINT('Ctrl Pts',(5.45777588767292,-2.48945220998862,1.06699650690162));
#50520=CARTESIAN_POINT('Ctrl Pts',(5.71386998951821,-1.53807662974237,1.1133876593756));
#50521=CARTESIAN_POINT('Ctrl Pts',(5.9699640913635,-0.586701049496119,1.15977881184959));
#50522=CARTESIAN_POINT('Ctrl Pts',(5.98329069437662,0.430025900502397,1.20616996432357));
#50523=CARTESIAN_POINT('Ctrl Pts',(5.75221997711583,1.38778803550136,1.25256111679756));
#50524=CARTESIAN_POINT('Ctrl Pts',(5.52114925985504,2.34555017050033,1.29895226927154));
#50525=CARTESIAN_POINT('Ctrl Pts',(5.04568122232034,3.24434749049973,1.34534342174553));
#50526=CARTESIAN_POINT('Ctrl Pts',(4.38395037427107,3.97428806732987,1.39173457421951));
#50527=CARTESIAN_POINT('Ctrl Pts',(3.7222195262218,4.70422864416001,1.43812572669349));
#50528=CARTESIAN_POINT('Ctrl Pts',(2.87422586765797,5.26531247782086,1.48451687916748));
#50529=CARTESIAN_POINT('Ctrl Pts',(1.94365137477809,5.58893631816464,1.53090803164146));
#50530=CARTESIAN_POINT('Ctrl Pts',(1.01307688189823,5.91256015850842,1.57729918411544));
#50531=CARTESIAN_POINT('Ctrl Pts',(-7.84452976816674E-5,5.99872400553511,
1.62369033658943));
#50532=CARTESIAN_POINT('Ctrl Pts',(-0.971938559216247,5.83689329055121,
1.67008148906341));
#50533=CARTESIAN_POINT('Ctrl Pts',(-1.94379867313481,5.67506257556731,1.7164726415374));
#50534=CARTESIAN_POINT('Ctrl Pts',(-2.87436357377604,5.26523729857281,1.76286379401138));
#50535=CARTESIAN_POINT('Ctrl Pts',(-3.64985542413063,4.65752553934663,1.80925494648536));
#50536=CARTESIAN_POINT('Ctrl Pts',(-4.42534727448522,4.04981378012046,1.85564609895935));
#50537=CARTESIAN_POINT('Ctrl Pts',(-5.04576607455317,3.2442155386626,1.90203725143333));
#50538=CARTESIAN_POINT('Ctrl Pts',(-5.43525473989259,2.33922944038597,1.94842840390732));
#50539=CARTESIAN_POINT('Ctrl Pts',(-5.75204442873269,1.603161128288,1.9861605385366));
#50540=CARTESIAN_POINT('Ctrl Pts',(-5.91606589125939,0.801344330739464,
2.02389267316589));
#50541=CARTESIAN_POINT('Ctrl Pts',(-5.91688804929001,-0.00014628683568293,
2.06162480779517));
#50542=CARTESIAN_POINT('Origin',(0.,0.,0.));
#50543=CARTESIAN_POINT('',(-5.91644339103703,0.000127799667652695,4.0633751922049));
#50544=CARTESIAN_POINT('',(-5.9163416407139,9.66719635090206E-5,3.81162480779517));
#50545=CARTESIAN_POINT('',(-5.91675,-7.2459289488551E-16,0.));
#50546=CARTESIAN_POINT('Ctrl Pts',(-5.91644339103703,0.000127799667652695,
4.0633751922049));
#50547=CARTESIAN_POINT('Ctrl Pts',(-5.91670480388819,0.333943128373217,
4.04766341184946));
#50548=CARTESIAN_POINT('Ctrl Pts',(-5.88892930320423,0.667715421417966,
4.03195163149402));
#50549=CARTESIAN_POINT('Ctrl Pts',(-5.83272798953327,0.996630632830126,
4.01623985113858));
#50550=CARTESIAN_POINT('Ctrl Pts',(-5.66678602415662,1.96779719565392,3.9698486986646));
#50551=CARTESIAN_POINT('Ctrl Pts',(-5.25302630322936,2.89661946143809,3.92345754619061));
#50552=CARTESIAN_POINT('Ctrl Pts',(-4.64203820294044,3.66953263245096,3.87706639371663));
#50553=CARTESIAN_POINT('Ctrl Pts',(-4.03105010265153,4.44244580346383,3.83067524124264));
#50554=CARTESIAN_POINT('Ctrl Pts',(-3.22283362300099,5.05944987970539,3.78428408876866));
#50555=CARTESIAN_POINT('Ctrl Pts',(-2.3162073909918,5.44510530110238,3.73789293629468));
#50556=CARTESIAN_POINT('Ctrl Pts',(-1.40958115898261,5.83076072249937,3.69150178382069));
#50557=CARTESIAN_POINT('Ctrl Pts',(-0.404545174614808,5.98506748905176,
3.64511063134671));
#50558=CARTESIAN_POINT('Ctrl Pts',(0.576017301791694,5.88915889463181,3.59871947887272));
#50559=CARTESIAN_POINT('Ctrl Pts',(1.55657977819819,5.79325030021187,3.55232832639874));
#50560=CARTESIAN_POINT('Ctrl Pts',(2.51266874664338,5.4471263448196,3.50593717392476));
#50561=CARTESIAN_POINT('Ctrl Pts',(3.32738557720147,4.89310674712962,3.45954602145077));
#50562=CARTESIAN_POINT('Ctrl Pts',(4.14210240775957,4.33908714943965,3.41315486897679));
#50563=CARTESIAN_POINT('Ctrl Pts',(4.81544710043059,3.57717190945197,3.36676371650281));
#50564=CARTESIAN_POINT('Ctrl Pts',(5.26509146752643,2.70051851627927,3.32037256402882));
#50565=CARTESIAN_POINT('Ctrl Pts',(5.71473583462227,1.82386512310658,3.27398141155484));
#50566=CARTESIAN_POINT('Ctrl Pts',(5.94067987614295,0.832473576748882,3.22759025908085));
#50567=CARTESIAN_POINT('Ctrl Pts',(5.91529797379783,-0.152441134100985,
3.18119910660687));
#50568=CARTESIAN_POINT('Ctrl Pts',(5.8899160714527,-1.13735584495085,3.13480795413288));
#50569=CARTESIAN_POINT('Ctrl Pts',(5.61320822524177,-2.11579372029289,3.0884168016589));
#50570=CARTESIAN_POINT('Ctrl Pts',(5.11900681811302,-2.96812358473493,3.04202564918492));
#50571=CARTESIAN_POINT('Ctrl Pts',(4.62480541098426,-3.82045344917698,2.99563449671093));
#50572=CARTESIAN_POINT('Ctrl Pts',(3.91311044293768,-4.54667530271904,2.94924334423695));
#50573=CARTESIAN_POINT('Ctrl Pts',(3.07093909483548,-5.05799579814922,2.90285219176296));
#50574=CARTESIAN_POINT('Ctrl Pts',(2.22876774673328,-5.5693162935794,2.85646103928898));
#50575=CARTESIAN_POINT('Ctrl Pts',(1.25612001857547,-5.86573543089771,2.81006988681499));
#50576=CARTESIAN_POINT('Ctrl Pts',(0.271919138825607,-5.91101077649929,
2.76367873434101));
#50577=CARTESIAN_POINT('Ctrl Pts',(-0.712281740924255,-5.95628612210086,
2.71728758186703));
#50578=CARTESIAN_POINT('Ctrl Pts',(-1.70803577226616,-5.7504176759857,2.67089642939304));
#50579=CARTESIAN_POINT('Ctrl Pts',(-2.59359457629318,-5.31857646296406,
2.62450527691906));
#50580=CARTESIAN_POINT('Ctrl Pts',(-3.4791533803202,-4.88673524994243,2.57811412444507));
#50581=CARTESIAN_POINT('Ctrl Pts',(-4.25451695703233,-4.22892127001432,
2.53172297197109));
#50582=CARTESIAN_POINT('Ctrl Pts',(-4.82488352247588,-3.42556380939725,
2.48533181949711));
#50583=CARTESIAN_POINT('Ctrl Pts',(-5.39525008791944,-2.62220634878019,
2.43894066702312));
#50584=CARTESIAN_POINT('Ctrl Pts',(-5.76061964209443,-1.67330540747417,
2.39254951454914));
#50585=CARTESIAN_POINT('Ctrl Pts',(-5.87631935466844,-0.694880752533762,
2.34615836207515));
#50586=CARTESIAN_POINT('Ctrl Pts',(-5.9035731385545,-0.464406765163384,
2.33523063878507));
#50587=CARTESIAN_POINT('Ctrl Pts',(-5.91697356177012,-0.2322946037521,2.32430291549498));
#50588=CARTESIAN_POINT('Ctrl Pts',(-5.91673471741553,-0.000155036278603748,
2.3133751922049));
#50589=CARTESIAN_POINT('Ctrl Pts',(-5.91688804929001,-0.00014628683568293,
2.06162480779517));
#50590=CARTESIAN_POINT('Ctrl Pts',(-5.9170767235097,-0.184077612962022,
2.07028382563987));
#50591=CARTESIAN_POINT('Ctrl Pts',(-5.90867065616891,-0.367991761119495,
2.07894284348457));
#50592=CARTESIAN_POINT('Ctrl Pts',(-5.89154378039528,-0.551090172782567,
2.08760186132927));
#50593=CARTESIAN_POINT('Ctrl Pts',(-5.7997856249477,-1.53204973257906,2.13399301380325));
#50594=CARTESIAN_POINT('Ctrl Pts',(-5.45771078344167,-2.48959489707664,
2.18038416627724));
#50595=CARTESIAN_POINT('Ctrl Pts',(-4.90714389560134,-3.30664895829955,
2.22677531875122));
#50596=CARTESIAN_POINT('Ctrl Pts',(-4.35657700776102,-4.12370301952246,
2.27316647122521));
#50597=CARTESIAN_POINT('Ctrl Pts',(-3.5975180735864,-4.8002659774707,2.31955762369919));
#50598=CARTESIAN_POINT('Ctrl Pts',(-2.72277535071871,-5.2536161718274,2.36594877617318));
#50599=CARTESIAN_POINT('Ctrl Pts',(-1.84803262785102,-5.7069663661841,2.41233992864716));
#50600=CARTESIAN_POINT('Ctrl Pts',(-0.857606116290267,-5.93710379694926,
2.45873108112114));
#50601=CARTESIAN_POINT('Ctrl Pts',(0.127407188700409,-5.91589012195794,
2.50512223359512));
#50602=CARTESIAN_POINT('Ctrl Pts',(1.11242049369109,-5.89467644696662,2.55151338606911));
#50603=CARTESIAN_POINT('Ctrl Pts',(2.09202059211168,-5.62211166621882,2.5979045385431));
#50604=CARTESIAN_POINT('Ctrl Pts',(2.94643420589685,-5.13152160469756,2.64429569101708));
#50605=CARTESIAN_POINT('Ctrl Pts',(3.80084781968202,-4.6409315431763,2.69068684349107));
#50606=CARTESIAN_POINT('Ctrl Pts',(4.53007494883177,-3.93231620088159,2.73707799596505));
#50607=CARTESIAN_POINT('Ctrl Pts',(5.04495479883511,-3.09231621821586,2.78346914843903));
#50608=CARTESIAN_POINT('Ctrl Pts',(5.55983464883846,-2.25231623555014,2.82986030091301));
#50609=CARTESIAN_POINT('Ctrl Pts',(5.8603672196954,-1.2809316125134,2.876251453387));
#50610=CARTESIAN_POINT('Ctrl Pts',(5.90980713825542,-0.296931141983866,
2.92264260586099));
#50611=CARTESIAN_POINT('Ctrl Pts',(5.95924705681544,0.687069328545672,2.96903375833497));
#50612=CARTESIAN_POINT('Ctrl Pts',(5.75759432307854,1.68368564656801,3.01542491080895));
#50613=CARTESIAN_POINT('Ctrl Pts',(5.32950451737138,2.57106400410279,3.06181606328293));
#50614=CARTESIAN_POINT('Ctrl Pts',(4.90141471166422,3.45844236163756,3.10820721575692));
#50615=CARTESIAN_POINT('Ctrl Pts',(4.24688783398681,4.23658275868477,3.1545983682309));
#50616=CARTESIAN_POINT('Ctrl Pts',(3.44595126436467,4.81034389605935,3.20098952070489));
#50617=CARTESIAN_POINT('Ctrl Pts',(2.64501469474253,5.38410503343392,3.24738067317887));
#50618=CARTESIAN_POINT('Ctrl Pts',(1.69766843317566,5.75348691113586,3.29377182565286));
#50619=CARTESIAN_POINT('Ctrl Pts',(0.719742160493715,5.87332612209818,3.34016297812684));
#50620=CARTESIAN_POINT('Ctrl Pts',(-0.258184112188229,5.9931653330605,3.38655413060082));
#50621=CARTESIAN_POINT('Ctrl Pts',(-1.26669039598524,5.8634618772832,3.43294528307481));
#50622=CARTESIAN_POINT('Ctrl Pts',(-2.18246912567144,5.50007427494718,3.47933643554879));
#50623=CARTESIAN_POINT('Ctrl Pts',(-3.09824785535763,5.13668667261115,3.52572758802278));
#50624=CARTESIAN_POINT('Ctrl Pts',(-3.92129903093301,4.5396149237164,3.57211874049676));
#50625=CARTESIAN_POINT('Ctrl Pts',(-4.55099022386481,3.78186151208579,3.61850989297074));
#50626=CARTESIAN_POINT('Ctrl Pts',(-5.1806814167966,3.02410810045518,3.66490104544473));
#50627=CARTESIAN_POINT('Ctrl Pts',(-5.61701262708482,2.10567302608871,3.71129219791871));
#50628=CARTESIAN_POINT('Ctrl Pts',(-5.80663471844869,1.1388510705313,3.7576833503927));
#50629=CARTESIAN_POINT('Ctrl Pts',(-5.88012927806763,0.764125987907549,
3.77566383619352));
#50630=CARTESIAN_POINT('Ctrl Pts',(-5.91656278747803,0.382132148291471,
3.79364432199434));
#50631=CARTESIAN_POINT('Ctrl Pts',(-5.9163416407139,9.66719635090206E-5,
3.81162480779517));
#50632=CARTESIAN_POINT('Origin',(0.,0.,0.));
#50633=CARTESIAN_POINT('',(-5.91715997915649,-8.5820353065702E-5,5.8133751922049));
#50634=CARTESIAN_POINT('',(-5.91724023967068,-3.97281055962929E-5,5.56162480779517));
#50635=CARTESIAN_POINT('',(-5.91675,-7.2459289488551E-16,0.));
#50636=CARTESIAN_POINT('Ctrl Pts',(-5.91715997915649,-8.5820353065702E-5,
5.8133751922049));
#50637=CARTESIAN_POINT('Ctrl Pts',(-5.91652656950878,0.899403380088141,
5.77102390820393));
#50638=CARTESIAN_POINT('Ctrl Pts',(-5.70841092001078,1.79917564355866,5.72867262420298));
#50639=CARTESIAN_POINT('Ctrl Pts',(-5.31219160137594,2.60664704332045,5.68632134020201));
#50640=CARTESIAN_POINT('Ctrl Pts',(-4.87817711379845,3.49114274890233,5.63993018772803));
#50641=CARTESIAN_POINT('Ctrl Pts',(-4.21846113592855,4.26488866108608,5.59353903525404));
#50642=CARTESIAN_POINT('Ctrl Pts',(-3.41370550625442,4.83328078376878,5.54714788278006));
#50643=CARTESIAN_POINT('Ctrl Pts',(-2.60894987658029,5.40167290645147,5.50075673030607));
#50644=CARTESIAN_POINT('Ctrl Pts',(-1.65915459510192,5.76471123963312,5.45436557783209));
#50645=CARTESIAN_POINT('Ctrl Pts',(-0.680448778229052,5.87800798556678,
5.40797442535811));
#50646=CARTESIAN_POINT('Ctrl Pts',(0.298257038643818,5.99130473150045,5.36158327288412));
#50647=CARTESIAN_POINT('Ctrl Pts',(1.30587339091119,5.85485989018613,5.31519212041014));
#50648=CARTESIAN_POINT('Ctrl Pts',(2.21920152306157,5.4853562343955,5.26880096793615));
#50649=CARTESIAN_POINT('Ctrl Pts',(3.13252965521195,5.11585257860486,5.22240981546217));
#50650=CARTESIAN_POINT('Ctrl Pts',(3.95156956724534,4.5132901083379,5.17601866298818));
#50651=CARTESIAN_POINT('Ctrl Pts',(4.5761792778911,3.75134264427823,5.1296275105142));
#50652=CARTESIAN_POINT('Ctrl Pts',(5.20078898853687,2.98939518021855,5.08323635804022));
#50653=CARTESIAN_POINT('Ctrl Pts',(5.630968497795,2.06806272236615,5.03684520556623));
#50654=CARTESIAN_POINT('Ctrl Pts',(5.81412082262937,1.09999430818887,4.99045405309225));
#50655=CARTESIAN_POINT('Ctrl Pts',(5.99727314746373,0.131925894011578,4.94406290061826));
#50656=CARTESIAN_POINT('Ctrl Pts',(5.93339828787432,-0.882878476490609,
4.89767174814428));
#50657=CARTESIAN_POINT('Ctrl Pts',(5.63030606472418,-1.82034118662145,4.85128059567029));
#50658=CARTESIAN_POINT('Ctrl Pts',(5.32721384157405,-2.75780389675229,4.80488944319631));
#50659=CARTESIAN_POINT('Ctrl Pts',(4.78490425486322,-3.61792494651176,4.75849829072233));
#50660=CARTESIAN_POINT('Ctrl Pts',(4.06968415445011,-4.29553946567809,4.71210713824835));
#50661=CARTESIAN_POINT('Ctrl Pts',(3.354464054037,-4.97315398484442,4.66571598577436));
#50662=CARTESIAN_POINT('Ctrl Pts',(2.4663334399216,-5.46826197341759,4.61932483330037));
#50663=CARTESIAN_POINT('Ctrl Pts',(1.51388184237951,-5.72032780402434,4.57293368082639));
#50664=CARTESIAN_POINT('Ctrl Pts',(0.561430244837424,-5.9723936346311,4.5265425283524));
#50665=CARTESIAN_POINT('Ctrl Pts',(-0.455342336131384,-5.98141730727146,
4.48015137587842));
#50666=CARTESIAN_POINT('Ctrl Pts',(-1.41211763561221,-5.74629551984348,
4.43376022340444));
#50667=CARTESIAN_POINT('Ctrl Pts',(-2.36889293509303,-5.5111737324155,4.38736907093045));
#50668=CARTESIAN_POINT('Ctrl Pts',(-3.26567095308587,-5.03190648491918,
4.34097791845647));
#50669=CARTESIAN_POINT('Ctrl Pts',(-3.99280486266284,-4.36709259655396,
4.29458676598249));
#50670=CARTESIAN_POINT('Ctrl Pts',(-4.7199387722398,-3.70227870818874,4.2481956135085));
#50671=CARTESIAN_POINT('Ctrl Pts',(-5.27742857340089,-2.85191817895462,
4.20180446103452));
#50672=CARTESIAN_POINT('Ctrl Pts',(-5.59711136906842,-1.91998248440585,
4.15541330856053));
#50673=CARTESIAN_POINT('Ctrl Pts',(-5.80852382435676,-1.30367526979957,
4.12473393644199));
#50674=CARTESIAN_POINT('Ctrl Pts',(-5.91593294715633,-0.651691692239068,
4.09405456432344));
#50675=CARTESIAN_POINT('Ctrl Pts',(-5.91644339103703,0.000127799667652695,
4.0633751922049));
#50676=CARTESIAN_POINT('Ctrl Pts',(-5.9163416407139,9.66719635090206E-5,
3.81162480779517));
#50677=CARTESIAN_POINT('Ctrl Pts',(-5.91599221038866,-0.603551232520732,
3.84003547446833));
#50678=CARTESIAN_POINT('Ctrl Pts',(-5.82412843901308,-1.20730308986252,
3.86844614114149));
#50679=CARTESIAN_POINT('Ctrl Pts',(-5.64235352522039,-1.78264836992076,
3.89685680781465));
#50680=CARTESIAN_POINT('Ctrl Pts',(-5.34553726818872,-2.72211701806704,
3.94324796028863));
#50681=CARTESIAN_POINT('Ctrl Pts',(-4.80899178168586,-3.58584547761124,
3.98963911276262));
#50682=CARTESIAN_POINT('Ctrl Pts',(-4.09831915331625,-4.26822780927827,
4.0360302652366));
#50683=CARTESIAN_POINT('Ctrl Pts',(-3.38764652494664,-4.95061014094529,
4.08242141771058));
#50684=CARTESIAN_POINT('Ctrl Pts',(-2.50284675471028,-5.45164634473513,
4.12881257018457));
#50685=CARTESIAN_POINT('Ctrl Pts',(-1.55210211885185,-5.71007596508149,
4.17520372265855));
#50686=CARTESIAN_POINT('Ctrl Pts',(-0.601357482993406,-5.96850558542785,
4.22159487513254));
#50687=CARTESIAN_POINT('Ctrl Pts',(0.415332018487122,-5.98432862233073,
4.26798602760652));
#50688=CARTESIAN_POINT('Ctrl Pts',(1.3736582785981,-5.75561043226334,4.31437718008051));
#50689=CARTESIAN_POINT('Ctrl Pts',(2.33198453870906,-5.52689224219595,4.36076833255449));
#50690=CARTESIAN_POINT('Ctrl Pts',(3.23194755745048,-5.0536328251583,4.40715948502848));
#50691=CARTESIAN_POINT('Ctrl Pts',(3.9635110857423,-4.39369643780044,4.45355063750246));
#50692=CARTESIAN_POINT('Ctrl Pts',(4.69507461403412,-3.73376005044257,4.49994178997644));
#50693=CARTESIAN_POINT('Ctrl Pts',(5.25823865187635,-2.88714669276451,4.54633294245043));
#50694=CARTESIAN_POINT('Ctrl Pts',(5.58414652732743,-1.95736968293639,4.59272409492441));
#50695=CARTESIAN_POINT('Ctrl Pts',(5.9100544027785,-1.02759267310829,4.63911524739839));
#50696=CARTESIAN_POINT('Ctrl Pts',(5.99870611583842,-0.0146520111301307,
4.68550639987238));
#50697=CARTESIAN_POINT('Ctrl Pts',(5.83926244114294,0.957602557326817,4.73189755234636));
#50698=CARTESIAN_POINT('Ctrl Pts',(5.67981876644747,1.92985712578377,4.77828870482035));
#50699=CARTESIAN_POINT('Ctrl Pts',(5.27227970399659,2.86142560071952,4.82467985729433));
#50700=CARTESIAN_POINT('Ctrl Pts',(4.66647404547604,3.63840741221214,4.87107100976832));
#50701=CARTESIAN_POINT('Ctrl Pts',(4.06066838695548,4.41538922370475,4.9174621622423));
#50702=CARTESIAN_POINT('Ctrl Pts',(3.25659613236525,5.03778437175423,4.96385331471628));
#50703=CARTESIAN_POINT('Ctrl Pts',(2.35256920457551,5.42949414329037,5.01024446719026));
#50704=CARTESIAN_POINT('Ctrl Pts',(1.44854227678578,5.82120391482652,5.05663561966425));
#50705=CARTESIAN_POINT('Ctrl Pts',(0.444560675796532,5.98222830984934,5.10302677213823));
#50706=CARTESIAN_POINT('Ctrl Pts',(-0.536621254916168,5.8928792744391,5.14941792461222));
#50707=CARTESIAN_POINT('Ctrl Pts',(-1.51780318562888,5.80353023902886,5.1958090770862));
#50708=CARTESIAN_POINT('Ctrl Pts',(-2.47618544606504,5.46380777318558,5.24220022956019));
#50709=CARTESIAN_POINT('Ctrl Pts',(-3.29458901116783,4.91524890131046,5.28859138203417));
#50710=CARTESIAN_POINT('Ctrl Pts',(-4.11299257627063,4.36669002943535,5.33498253450816));
#50711=CARTESIAN_POINT('Ctrl Pts',(-4.79141744604006,3.6092947515284,5.38137368698214));
#50712=CARTESIAN_POINT('Ctrl Pts',(-5.24691429211759,2.73566791214026,5.42776483945613));
#50713=CARTESIAN_POINT('Ctrl Pts',(-5.6850207710679,1.89539518178708,5.47238482890248));
#50714=CARTESIAN_POINT('Ctrl Pts',(-5.91689657222713,0.947596653160506,
5.51700481834882));
#50715=CARTESIAN_POINT('Ctrl Pts',(-5.91724023967068,-3.97281055962929E-5,
5.56162480779517));
#50716=CARTESIAN_POINT('Origin',(0.,0.,0.));
#50717=CARTESIAN_POINT('',(-5.9162413557982,1.18844204999302E-5,7.5633751922049));
#50718=CARTESIAN_POINT('',(-5.9162507091618,-3.31417769469161E-5,7.31162480779517));
#50719=CARTESIAN_POINT('',(-5.91675,-7.2459289488551E-16,0.));
#50720=CARTESIAN_POINT('Ctrl Pts',(-5.9162413557982,1.18844204999302E-5,
7.5633751922049));
#50721=CARTESIAN_POINT('Ctrl Pts',(-5.91627481843442,0.480214766201657,
7.5407755570324));
#50722=CARTESIAN_POINT('Ctrl Pts',(-5.8584953203415,0.960409734025278,7.51817592185989));
#50723=CARTESIAN_POINT('Ctrl Pts',(-5.74281060135014,1.42622397091085,7.49557628668739));
#50724=CARTESIAN_POINT('Ctrl Pts',(-5.5053400671281,2.38241902109478,7.4491851342134));
#50725=CARTESIAN_POINT('Ctrl Pts',(-5.02387213814794,3.27801744753458,7.40279398173942));
#50726=CARTESIAN_POINT('Ctrl Pts',(-4.35727470548306,4.00351664903967,7.35640282926544));
#50727=CARTESIAN_POINT('Ctrl Pts',(-3.69067727281818,4.72901585054476,7.31001167679145));
#50728=CARTESIAN_POINT('Ctrl Pts',(-2.83895033646859,5.28441582711515,7.26362052431747));
#50729=CARTESIAN_POINT('Ctrl Pts',(-1.90623243920183,5.60180919934935,7.21722937184349));
#50730=CARTESIAN_POINT('Ctrl Pts',(-0.973514541935027,5.91920257158355,
7.1708382193695));
#50731=CARTESIAN_POINT('Ctrl Pts',(0.0401943162489465,5.99858933948154,
7.12444706689551));
#50732=CARTESIAN_POINT('Ctrl Pts',(1.01095046423141,5.83026307957459,7.07805591442153));
#50733=CARTESIAN_POINT('Ctrl Pts',(1.98170661221383,5.66193681966765,7.03166476194754));
#50734=CARTESIAN_POINT('Ctrl Pts',(2.90951004999477,5.24589753195577,6.98527360947356));
#50735=CARTESIAN_POINT('Ctrl Pts',(3.68092054941919,4.6330133096122,6.93888245699958));
#50736=CARTESIAN_POINT('Ctrl Pts',(4.45233104884364,4.02012908726862,6.89249130452559));
#50737=CARTESIAN_POINT('Ctrl Pts',(5.06734860991157,3.21039993029335,6.84610015205162));
#50738=CARTESIAN_POINT('Ctrl Pts',(5.45077655883864,2.30282941699889,6.79970899957763));
#50739=CARTESIAN_POINT('Ctrl Pts',(5.83420450776571,1.39525890370445,6.75331784710365));
#50740=CARTESIAN_POINT('Ctrl Pts',(5.98604284455189,0.389847034090864,6.70692669462966));
#50741=CARTESIAN_POINT('Ctrl Pts',(5.88772667186408,-0.590476972963932,
6.66053554215567));
#50742=CARTESIAN_POINT('Ctrl Pts',(5.78941049917627,-1.57080098001873,6.61414438968169));
#50743=CARTESIAN_POINT('Ctrl Pts',(5.44093981701448,-2.52603712451473,6.56775323720771));
#50744=CARTESIAN_POINT('Ctrl Pts',(4.88492127251973,-3.33939104919812,6.52136208473372));
#50745=CARTESIAN_POINT('Ctrl Pts',(4.32890272802498,-4.15274497388151,6.47497093225974));
#50746=CARTESIAN_POINT('Ctrl Pts',(3.56533632119724,-4.82421667875231,6.42857977978575));
#50747=CARTESIAN_POINT('Ctrl Pts',(2.68758142523437,-5.27170698170104,6.38218862731177));
#50748=CARTESIAN_POINT('Ctrl Pts',(1.80982652927149,-5.71919728464978,6.33579747483778));
#50749=CARTESIAN_POINT('Ctrl Pts',(0.81788314417347,-5.94270618567646,6.2894063223638));
#50750=CARTESIAN_POINT('Ctrl Pts',(-0.166966269421853,-5.91490580508732,
6.24301516988982));
#50751=CARTESIAN_POINT('Ctrl Pts',(-1.15181568301718,-5.88710542449819,
6.19662401741583));
#50752=CARTESIAN_POINT('Ctrl Pts',(-2.12957112510979,-5.60799576229324,
6.15023286494185));
#50753=CARTESIAN_POINT('Ctrl Pts',(-2.98068485970938,-5.11170286551161,
6.10384171246786));
#50754=CARTESIAN_POINT('Ctrl Pts',(-3.83179859430896,-4.61540996872999,
6.05745055999388));
#50755=CARTESIAN_POINT('Ctrl Pts',(-4.55627062141552,-3.90193383737169,
6.0110594075199));
#50756=CARTESIAN_POINT('Ctrl Pts',(-5.06552154080239,-3.05850943072722,
5.96466825504591));
#50757=CARTESIAN_POINT('Ctrl Pts',(-5.57477246018926,-2.21508502408275,
5.91827710257193));
#50758=CARTESIAN_POINT('Ctrl Pts',(-5.86880227185644,-1.24171234215211,
5.87188595009794));
#50759=CARTESIAN_POINT('Ctrl Pts',(-5.91166067904749,-0.257403251696779,
5.82549479762396));
#50760=CARTESIAN_POINT('Ctrl Pts',(-5.91539290639649,-0.171686923255304,
5.82145492915094));
#50761=CARTESIAN_POINT('Ctrl Pts',(-5.91722039979607,-0.085887659622042,
5.81741506067792));
#50762=CARTESIAN_POINT('Ctrl Pts',(-5.91715997915649,-8.5820353065702E-5,
5.8133751922049));
#50763=CARTESIAN_POINT('Ctrl Pts',(-5.91724023967068,-3.97281055962929E-5,
5.56162480779517));
#50764=CARTESIAN_POINT('Ctrl Pts',(-5.9172538813384,-0.0376555712056591,
5.56339597082281));
#50765=CARTESIAN_POINT('Ctrl Pts',(-5.9169027107474,-0.0752711588191768,
5.56516713385044));
#50766=CARTESIAN_POINT('Ctrl Pts',(-5.9161851454377,-0.112879755686916,
5.56693829687808));
#50767=CARTESIAN_POINT('Ctrl Pts',(-5.89739033029467,-1.09794218325665,
5.61332944935206));
#50768=CARTESIAN_POINT('Ctrl Pts',(-5.62723187762299,-2.07820863752684,
5.65972060182604));
#50769=CARTESIAN_POINT('Ctrl Pts',(-5.13874139224443,-2.93382436726798,
5.70611175430003));
#50770=CARTESIAN_POINT('Ctrl Pts',(-4.65025090686588,-3.78944009700913,
5.75250290677401));
#50771=CARTESIAN_POINT('Ctrl Pts',(-3.94342838878045,-4.52040510222124,
5.798894059248));
#50772=CARTESIAN_POINT('Ctrl Pts',(-3.10469527646488,-5.03734610232792,
5.84528521172198));
#50773=CARTESIAN_POINT('Ctrl Pts',(-2.26596216414931,-5.55428710243459,
5.89167636419597));
#50774=CARTESIAN_POINT('Ctrl Pts',(-1.2953184576036,-5.85720409743582,5.93806751666994));
#50775=CARTESIAN_POINT('Ctrl Pts',(-0.311442358528609,-5.90906017668256,
5.98445866914393));
#50776=CARTESIAN_POINT('Ctrl Pts',(0.672433740546371,-5.96091625592931,
6.03084982161791));
#50777=CARTESIAN_POINT('Ctrl Pts',(1.66954223215063,-5.76171141942157,6.0772409740919));
#50778=CARTESIAN_POINT('Ctrl Pts',(2.55796913086782,-5.3358019490859,6.12363212656589));
#50779=CARTESIAN_POINT('Ctrl Pts',(3.44639602958501,-4.90989247875023,6.17002327903987));
#50780=CARTESIAN_POINT('Ctrl Pts',(4.22614133541513,-4.25727837458664,6.21641443151385));
#50781=CARTESIAN_POINT('Ctrl Pts',(4.80186752125472,-3.45775314657664,6.26280558398784));
#50782=CARTESIAN_POINT('Ctrl Pts',(5.37759370709432,-2.65822791856663,6.30919673646182));
#50783=CARTESIAN_POINT('Ctrl Pts',(5.74930077294337,-1.71179156671023,6.35558788893581));
#50784=CARTESIAN_POINT('Ctrl Pts',(5.87154101658429,-0.734162519412394,
6.40197904140979));
#50785=CARTESIAN_POINT('Ctrl Pts',(5.99378126022521,0.243466527885433,6.44837019388378));
#50786=CARTESIAN_POINT('Ctrl Pts',(5.86655468165799,1.25228827062469,6.49476134635776));
#50787=CARTESIAN_POINT('Ctrl Pts',(5.50541695950198,2.16895657318664,6.54115249883174));
#50788=CARTESIAN_POINT('Ctrl Pts',(5.14427923734597,3.08562487574861,6.58754365130572));
#50789=CARTESIAN_POINT('Ctrl Pts',(4.54923037160118,3.91013973813327,6.63393480377971));
#50790=CARTESIAN_POINT('Ctrl Pts',(3.79302551313757,4.54168977045208,6.6803259562537));
#50791=CARTESIAN_POINT('Ctrl Pts',(3.03682065467397,5.17323980277089,6.72671710872768));
#50792=CARTESIAN_POINT('Ctrl Pts',(2.11945980349156,5.61182500502386,6.77310826120166));
#50793=CARTESIAN_POINT('Ctrl Pts',(1.15310639854836,5.80382065091337,6.81949941367564));
#50794=CARTESIAN_POINT('Ctrl Pts',(0.186752993605153,5.99581629680288,6.86589056614963));
#50795=CARTESIAN_POINT('Ctrl Pts',(-0.82859296509884,5.94122238632894,6.91228171862361));
#50796=CARTESIAN_POINT('Ctrl Pts',(-1.76878764221949,5.6467139816953,6.9586728710976));
#50797=CARTESIAN_POINT('Ctrl Pts',(-2.70898231934014,5.35220557706166,7.00506402357158));
#50798=CARTESIAN_POINT('Ctrl Pts',(-3.57402571487744,4.81778267826832,7.05145517604557));
#50799=CARTESIAN_POINT('Ctrl Pts',(-4.25815111558402,4.10878784937751,7.09784632851955));
#50800=CARTESIAN_POINT('Ctrl Pts',(-4.94227651629061,3.39979302048667,7.14423748099354));
#50801=CARTESIAN_POINT('Ctrl Pts',(-5.44548392216648,2.51622626149834,7.19062863346752));
#50802=CARTESIAN_POINT('Ctrl Pts',(-5.70624741014717,1.56611909142644,7.23701978594151));
#50803=CARTESIAN_POINT('Ctrl Pts',(-5.84603172017157,1.05680670169657,7.2618881265594));
#50804=CARTESIAN_POINT('Ctrl Pts',(-5.9161478310269,0.528373392570541,7.28675646717728));
#50805=CARTESIAN_POINT('Ctrl Pts',(-5.9162507091618,-3.31417769469161E-5,
7.31162480779517));
#50806=CARTESIAN_POINT('Origin',(0.,0.,0.));
#50807=CARTESIAN_POINT('',(-5.9172084520385,6.25597485048868E-5,9.3133751922049));
#50808=CARTESIAN_POINT('',(-5.91710638445669,0.000104510447198684,9.06162480779517));
#50809=CARTESIAN_POINT('',(-5.91675,-7.2459289488551E-16,0.));
#50810=CARTESIAN_POINT('Ctrl Pts',(-5.9172084520385,6.25597485048868E-5,
9.3133751922049));
#50811=CARTESIAN_POINT('Ctrl Pts',(-5.91724119307767,0.0605488496737315,
9.31052720586085));
#50812=CARTESIAN_POINT('Ctrl Pts',(-5.91633311693352,0.121034154618972,
9.30767921951681));
#50813=CARTESIAN_POINT('Ctrl Pts',(-5.91447796966348,0.181490397943491,
9.30483123317277));
#50814=CARTESIAN_POINT('Ctrl Pts',(-5.88425927846571,1.16626857566792,9.25844008069878));
#50815=CARTESIAN_POINT('Ctrl Pts',(-5.60274948328953,2.14333568866362,9.2120489282248));
#50816=CARTESIAN_POINT('Ctrl Pts',(-5.10436808948731,2.99322816123395,9.16565777575082));
#50817=CARTESIAN_POINT('Ctrl Pts',(-4.60598669568509,3.84312063380428,9.11926662327683));
#50818=CARTESIAN_POINT('Ctrl Pts',(-3.89073370325683,4.56583846594923,9.07287547080284));
#50819=CARTESIAN_POINT('Ctrl Pts',(-3.04606132389475,5.07301673851495,9.02648431832886));
#50820=CARTESIAN_POINT('Ctrl Pts',(-2.20138894453265,5.58019501108068,8.98009316585487));
#50821=CARTESIAN_POINT('Ctrl Pts',(-1.22729717823674,5.87183372406716,8.9337020133809));
#50822=CARTESIAN_POINT('Ctrl Pts',(-0.242885812432634,5.91227493443085,
8.88731086090691));
#50823=CARTESIAN_POINT('Ctrl Pts',(0.74152555337144,5.95271614479453,8.84091970843293));
#50824=CARTESIAN_POINT('Ctrl Pts',(1.7362565186837,5.74195985253542,8.79452855595894));
#50825=CARTESIAN_POINT('Ctrl Pts',(2.61968379233836,5.30577470746167,8.74813740348495));
#50826=CARTESIAN_POINT('Ctrl Pts',(3.50311106599304,4.86958956238792,8.70174625101097));
#50827=CARTESIAN_POINT('Ctrl Pts',(4.27523464799013,4.20797556449952,8.655355098537));
#50828=CARTESIAN_POINT('Ctrl Pts',(4.84164890052009,3.40182661849086,8.60896394606301));
#50829=CARTESIAN_POINT('Ctrl Pts',(5.40806315305005,2.5956776724822,8.56257279358903));
#50830=CARTESIAN_POINT('Ctrl Pts',(5.76876807611289,1.64499377835328,8.51618164111504));
#50831=CARTESIAN_POINT('Ctrl Pts',(5.87966117223702,0.666012700981533,8.46979048864105));
#50832=CARTESIAN_POINT('Ctrl Pts',(5.99055426836114,-0.312968376390219,
8.42339933616706));
#50833=CARTESIAN_POINT('Ctrl Pts',(5.85163553754656,-1.32024663700481,8.37700818369309));
#50834=CARTESIAN_POINT('Ctrl Pts',(5.47989022890625,-2.23266466297967,8.3306170312191));
#50835=CARTESIAN_POINT('Ctrl Pts',(5.10814492026594,-3.14508268895454,8.28422587874512));
#50836=CARTESIAN_POINT('Ctrl Pts',(4.50357303379992,-3.96264048028968,8.23783472627113));
#50837=CARTESIAN_POINT('Ctrl Pts',(3.74009407653309,-4.58537727094101,8.19144357379715));
#50838=CARTESIAN_POINT('Ctrl Pts',(2.97661511926626,-5.20811406159233,8.14505242132316));
#50839=CARTESIAN_POINT('Ctrl Pts',(2.05422909119864,-5.63602985155983,8.09866126884918));
#50840=CARTESIAN_POINT('Ctrl Pts',(1.08571384721853,-5.81680443715776,8.0522701163752));
#50841=CARTESIAN_POINT('Ctrl Pts',(0.117198603238411,-5.9975790227557,8.00587896390121));
#50842=CARTESIAN_POINT('Ctrl Pts',(-0.897445856654189,-5.93121240398407,
7.95948781142723));
#50843=CARTESIAN_POINT('Ctrl Pts',(-1.83416146763716,-5.62581906292901,
7.91309665895325));
#50844=CARTESIAN_POINT('Ctrl Pts',(-2.77087707862012,-5.32042572187395,
7.86670550647926));
#50845=CARTESIAN_POINT('Ctrl Pts',(-3.62966384069345,-4.77600565853546,
7.82031435400528));
#50846=CARTESIAN_POINT('Ctrl Pts',(-4.30552002368566,-4.05912376552159,
7.77392320153129));
#50847=CARTESIAN_POINT('Ctrl Pts',(-4.98137620667786,-3.34224187250773,
7.72753204905731));
#50848=CARTESIAN_POINT('Ctrl Pts',(-5.47430181058894,-2.45289814981848,
7.68114089658332));
#50849=CARTESIAN_POINT('Ctrl Pts',(-5.72402804281252,-1.49983045150984,
7.63474974410934));
#50850=CARTESIAN_POINT('Ctrl Pts',(-5.852099143825,-1.01105348813285,7.61095822680786));
#50851=CARTESIAN_POINT('Ctrl Pts',(-5.91620612837604,-0.505516416497265,
7.58716670950638));
#50852=CARTESIAN_POINT('Ctrl Pts',(-5.9162413557982,1.18844204999302E-5,
7.5633751922049));
#50853=CARTESIAN_POINT('Ctrl Pts',(-5.9162507091618,-3.31417769469161E-5,
7.31162480779517));
#50854=CARTESIAN_POINT('Ctrl Pts',(-5.91633974713885,-0.457353338449392,
7.33314761965127));
#50855=CARTESIAN_POINT('Ctrl Pts',(-5.86398614648453,-0.914653479769718,
7.35467043150736));
#50856=CARTESIAN_POINT('Ctrl Pts',(-5.75896623194724,-1.35952067054277,
7.37619324336345));
#50857=CARTESIAN_POINT('Ctrl Pts',(-5.53260199568109,-2.31840568128467,
7.42258439583744));
#50858=CARTESIAN_POINT('Ctrl Pts',(-5.06155395306328,-3.21952812161301,
7.46897554831142));
#50859=CARTESIAN_POINT('Ctrl Pts',(-4.40341598147186,-3.95270998284213,
7.51536670078541));
#50860=CARTESIAN_POINT('Ctrl Pts',(-3.74527800988045,-4.68589184407125,
7.56175785325939));
#50861=CARTESIAN_POINT('Ctrl Pts',(-2.90005010931545,-5.25113312620114,
7.60814900573337));
#50862=CARTESIAN_POINT('Ctrl Pts',(-1.97107620153722,-5.57932317777661,
7.65454015820736));
#50863=CARTESIAN_POINT('Ctrl Pts',(-1.042102293759,-5.90751322935207,7.70093131068134));
#50864=CARTESIAN_POINT('Ctrl Pts',(-0.0293823787675436,-5.9986520503731,
7.74732246315532));
#50865=CARTESIAN_POINT('Ctrl Pts',(0.943260787952951,-5.84159632294564,
7.79371361562931));
#50866=CARTESIAN_POINT('Ctrl Pts',(1.91590395467344,-5.68454059551817,7.84010476810329));
#50867=CARTESIAN_POINT('Ctrl Pts',(2.84847037312298,-5.27929031964222,7.88649592057728));
#50868=CARTESIAN_POINT('Ctrl Pts',(3.62693745729823,-4.67539444273835,7.93288707305126));
#50869=CARTESIAN_POINT('Ctrl Pts',(4.4054045414735,-4.07149856583446,7.97927822552525));
#50870=CARTESIAN_POINT('Ctrl Pts',(5.02977229137448,-3.26895708790266,8.02566937799923));
#50871=CARTESIAN_POINT('Ctrl Pts',(5.4237008087887,-2.36589476754282,8.07206053047321));
#50872=CARTESIAN_POINT('Ctrl Pts',(5.81762932620292,-1.46283244718296,8.1184516829472));
#50873=CARTESIAN_POINT('Ctrl Pts',(5.98111861113038,-0.45924928439506,8.16484283542118));
#50874=CARTESIAN_POINT('Ctrl Pts',(5.89417923366829,0.522149093396754,8.21123398789517));
#50875=CARTESIAN_POINT('Ctrl Pts',(5.80723985620622,1.50354747118852,8.25762514036915));
#50876=CARTESIAN_POINT('Ctrl Pts',(5.46987181635464,2.46276106398421,8.30401629284313));
#50877=CARTESIAN_POINT('Ctrl Pts',(4.9233242686807,3.28250920177862,8.35040744531711));
#50878=CARTESIAN_POINT('Ctrl Pts',(4.37677672100673,4.10225733957307,8.3967985977911));
#50879=CARTESIAN_POINT('Ctrl Pts',(3.62104966551037,4.78254002236623,8.44318975026509));
#50880=CARTESIAN_POINT('Ctrl Pts',(2.74854397732036,5.24018077160298,8.48958090273907));
#50881=CARTESIAN_POINT('Ctrl Pts',(1.87603828913037,5.69782152083972,8.53597205521306));
#50882=CARTESIAN_POINT('Ctrl Pts',(0.886753968246731,5.93282033652007,8.58236320768704));
#50883=CARTESIAN_POINT('Ctrl Pts',(-0.0983516418876641,5.91644449554626,
8.62875436016102));
#50884=CARTESIAN_POINT('Ctrl Pts',(-1.08345725202206,5.90006865457244,8.67514551263501));
#50885=CARTESIAN_POINT('Ctrl Pts',(-2.0643841514072,5.63231815694446,8.72153666510899));
#50886=CARTESIAN_POINT('Ctrl Pts',(-2.92119683782535,5.14593019278544,8.76792781758298));
#50887=CARTESIAN_POINT('Ctrl Pts',(-3.7780095242435,4.65954222862642,8.81431897005696));
#50888=CARTESIAN_POINT('Ctrl Pts',(-4.51070799769467,3.95451679793635,8.86071012253094));
#50889=CARTESIAN_POINT('Ctrl Pts',(-5.02970703073467,3.11705561376756,8.90710127500493));
#50890=CARTESIAN_POINT('Ctrl Pts',(-5.54870606377467,2.27959442959876,8.95349242747891));
#50891=CARTESIAN_POINT('Ctrl Pts',(-5.8540056564035,1.30969749195124,8.9998835799529));
#50892=CARTESIAN_POINT('Ctrl Pts',(-5.90827758366193,0.325951696942433,
9.04627473242688));
#50893=CARTESIAN_POINT('Ctrl Pts',(-5.91426348204536,0.217449886494213,
9.05139142421631));
#50894=CARTESIAN_POINT('Ctrl Pts',(-5.91719565645419,0.108779606217447,
9.05650811600574));
#50895=CARTESIAN_POINT('Ctrl Pts',(-5.91710638445669,0.000104510447198684,
9.06162480779517));
#50896=CARTESIAN_POINT('Origin',(0.,0.,0.));
#50897=CARTESIAN_POINT('',(-5.91638614209071,-0.000112643280536506,11.0633751922049));
#50898=CARTESIAN_POINT('',(-5.91650151471712,-0.000138897455152014,10.8116248077952));
#50899=CARTESIAN_POINT('',(-5.91675,-7.2459289488551E-16,0.));
#50900=CARTESIAN_POINT('Ctrl Pts',(-5.91638614209071,-0.000112643280536506,
11.0633751922049));
#50901=CARTESIAN_POINT('Ctrl Pts',(-5.91595937575435,0.6264012739477,11.0338877022153));
#50902=CARTESIAN_POINT('Ctrl Pts',(-5.81687601168185,1.25304699970507,11.0044002122258));
#50903=CARTESIAN_POINT('Ctrl Pts',(-5.62129813760519,1.84797068871148,10.9749127222362));
#50904=CARTESIAN_POINT('Ctrl Pts',(-5.31360552015834,2.78393355217811,10.9285215697622));
#50905=CARTESIAN_POINT('Ctrl Pts',(-4.76707826302969,3.64138084810558,10.8821304172882));
#50906=CARTESIAN_POINT('Ctrl Pts',(-4.04853890019245,4.31547461953014,10.8357392648142));
#50907=CARTESIAN_POINT('Ctrl Pts',(-3.32999953735522,4.9895683909547,10.7893481123403));
#50908=CARTESIAN_POINT('Ctrl Pts',(-2.4394480688094,5.48030863787637,10.7429569598663));
#50909=CARTESIAN_POINT('Ctrl Pts',(-1.48577001670525,5.72769376587471,10.6965658073923));
#50910=CARTESIAN_POINT('Ctrl Pts',(-0.53209196460107,5.97507889387305,10.6501746549183));
#50911=CARTESIAN_POINT('Ctrl Pts',(0.484712671061443,5.97910890294806,10.6037835024443));
#50912=CARTESIAN_POINT('Ctrl Pts',(1.44032170611958,5.73929105387252,10.5573923499703));
#50913=CARTESIAN_POINT('Ctrl Pts',(2.39593074117771,5.49947320479697,10.5110011974964));
#50914=CARTESIAN_POINT('Ctrl Pts',(3.29034417563147,5.01580749757088,10.4646100450224));
#50915=CARTESIAN_POINT('Ctrl Pts',(4.01420429432519,4.34743054016985,10.4182188925484));
#50916=CARTESIAN_POINT('Ctrl Pts',(4.7380644130189,3.67905358276882,10.3718277400744));
#50917=CARTESIAN_POINT('Ctrl Pts',(5.29137121595257,2.82596537519285,10.3254365876004));
#50918=CARTESIAN_POINT('Ctrl Pts',(5.60647325088044,1.89247089947045,10.2790454351264));
#50919=CARTESIAN_POINT('Ctrl Pts',(5.92157528580831,0.958976423748022,10.2326542826525));
#50920=CARTESIAN_POINT('Ctrl Pts',(5.99847255273037,-0.0549243201208414,
10.1862631301785));
#50921=CARTESIAN_POINT('Ctrl Pts',(5.82776301329569,-1.02526419963007,10.1398719777045));
#50922=CARTESIAN_POINT('Ctrl Pts',(5.65705347386101,-1.99560407913926,10.0934808252305));
#50923=CARTESIAN_POINT('Ctrl Pts',(5.23873712806962,-2.92238309428882,10.0470896727565));
#50924=CARTESIAN_POINT('Ctrl Pts',(4.62396047934579,-3.69228627054141,10.0006985202825));
#50925=CARTESIAN_POINT('Ctrl Pts',(4.00918383062193,-4.46218944679403,9.95430736780855));
#50926=CARTESIAN_POINT('Ctrl Pts',(3.19794687896562,-5.07521678414965,9.90791621533456));
#50927=CARTESIAN_POINT('Ctrl Pts',(2.28943755701025,-5.45641494854737,9.86152506286057));
#50928=CARTESIAN_POINT('Ctrl Pts',(1.3809282350549,-5.83761311294508,9.81513391038659));
#50929=CARTESIAN_POINT('Ctrl Pts',(0.375146542800495,-5.9869821043849,9.76874275791261));
#50930=CARTESIAN_POINT('Ctrl Pts',(-0.604933083576789,-5.88625894627263,
9.72235160543862));
#50931=CARTESIAN_POINT('Ctrl Pts',(-1.58501270995407,-5.78553578816036,
9.67596045296464));
#50932=CARTESIAN_POINT('Ctrl Pts',(-2.53939027045424,-5.434720480496,9.62956930049065));
#50933=CARTESIAN_POINT('Ctrl Pts',(-3.35137638476191,-4.87670634197308,
9.58317814801667));
#50934=CARTESIAN_POINT('Ctrl Pts',(-4.16336249906959,-4.31869220345017,
9.53678699554269));
#50935=CARTESIAN_POINT('Ctrl Pts',(-4.83295716718478,-3.55347923406871,
9.4903958430687));
#50936=CARTESIAN_POINT('Ctrl Pts',(-5.2782907076327,-2.6746281281514,9.44400469059472));
#50937=CARTESIAN_POINT('Ctrl Pts',(-5.69628490050886,-1.84973032614273,
9.40046152446478));
#50938=CARTESIAN_POINT('Ctrl Pts',(-5.91670787080818,-0.924718760325417,
9.35691835833484));
#50939=CARTESIAN_POINT('Ctrl Pts',(-5.9172084520385,6.25597485048868E-5,
9.3133751922049));
#50940=CARTESIAN_POINT('Ctrl Pts',(-5.91710638445669,0.000104510447198684,
9.06162480779517));
#50941=CARTESIAN_POINT('Ctrl Pts',(-5.9163862602626,-0.876537302731103,
9.10289926847972));
#50942=CARTESIAN_POINT('Ctrl Pts',(-5.71905903720832,-1.75349246259044,
9.14417372916428));
#50943=CARTESIAN_POINT('Ctrl Pts',(-5.34206720605816,-2.54485883307889,
9.18544818984883));
#50944=CARTESIAN_POINT('Ctrl Pts',(-4.91834063930793,-3.43432891572131,
9.23183934232282));
#50945=CARTESIAN_POINT('Ctrl Pts',(-4.26764324391943,-4.2156744286361,9.27823049479681));
#50946=CARTESIAN_POINT('Ctrl Pts',(-3.46953417864001,-4.79336219136322,
9.32462164727079));
#50947=CARTESIAN_POINT('Ctrl Pts',(-2.6714251133606,-5.37104995409033,9.37101279974477));
#50948=CARTESIAN_POINT('Ctrl Pts',(-1.72590437819026,-5.74507996662981,
9.41740395221876));
#50949=CARTESIAN_POINT('Ctrl Pts',(-0.748578451349749,-5.86972050582619,
9.46379510469274));
#50950=CARTESIAN_POINT('Ctrl Pts',(0.228747475490778,-5.99436104502257,
9.51018625716672));
#50951=CARTESIAN_POINT('Ctrl Pts',(1.23787859400146,-5.86961211087585,9.55657740964071));
#50952=CARTESIAN_POINT('Ctrl Pts',(2.15543094195436,-5.51072644655923,9.60296856211469));
#50953=CARTESIAN_POINT('Ctrl Pts',(3.07298328990726,-5.15184078224262,9.64935971458867));
#50954=CARTESIAN_POINT('Ctrl Pts',(3.89895686730239,-4.55881838775608,9.69575086706266));
#50955=CARTESIAN_POINT('Ctrl Pts',(4.53236193078007,-3.80416664234851,9.74214201953664));
#50956=CARTESIAN_POINT('Ctrl Pts',(5.16576699425776,-3.04951489694093,9.78853317201063));
#50957=CARTESIAN_POINT('Ctrl Pts',(5.60660354381802,-2.13323380061229,9.83492432448461));
#50958=CARTESIAN_POINT('Ctrl Pts',(5.80097158650461,-1.1673547733692,9.8813154769586));
#50959=CARTESIAN_POINT('Ctrl Pts',(5.99533962919119,-0.201475746126127,
9.92770662943258));
#50960=CARTESIAN_POINT('Ctrl Pts',(5.94323916500412,0.814001212031379,9.97409778190656));
#50961=CARTESIAN_POINT('Ctrl Pts',(5.65104038864595,1.75491624878051,10.0204889343805));
#50962=CARTESIAN_POINT('Ctrl Pts',(5.35884161228778,2.69583128552964,10.0668800868545));
#50963=CARTESIAN_POINT('Ctrl Pts',(4.82654452375848,3.56218440087041,10.1132712393285));
#50964=CARTESIAN_POINT('Ctrl Pts',(4.119231769565,4.24804874535922,10.1596623918025));
#50965=CARTESIAN_POINT('Ctrl Pts',(3.41191901537151,4.93391308984804,10.2060535442765));
#50966=CARTESIAN_POINT('Ctrl Pts',(2.52959059551382,5.43928866348491,10.2524446967505));
#50967=CARTESIAN_POINT('Ctrl Pts',(1.58012662034769,5.70238444670387,10.2988358492245));
#50968=CARTESIAN_POINT('Ctrl Pts',(0.630662645181565,5.96548022992282,10.3452270016984));
#50969=CARTESIAN_POINT('Ctrl Pts',(-0.38593688529298,5.98629622272385,10.3916181541724));
#50970=CARTESIAN_POINT('Ctrl Pts',(-1.34537486461655,5.76228730522868,10.4380093066464));
#50971=CARTESIAN_POINT('Ctrl Pts',(-2.30481284394012,5.53827838773352,10.4844004591204));
#50972=CARTESIAN_POINT('Ctrl Pts',(-3.20708927211268,5.06944455994216,10.5307916115944));
#50973=CARTESIAN_POINT('Ctrl Pts',(-3.94188504521335,4.41310897267051,10.5771827640684));
#50974=CARTESIAN_POINT('Ctrl Pts',(-4.67668081831403,3.75677338539885,10.6235739165423));
#50975=CARTESIAN_POINT('Ctrl Pts',(-5.2439959363428,2.91293603864686,10.6699650690163));
#50976=CARTESIAN_POINT('Ctrl Pts',(-5.574466185066,1.98477083460466,10.7163562214903));
#50977=CARTESIAN_POINT('Ctrl Pts',(-5.80068341064102,1.3494127104016,10.7481124169253));
#50978=CARTESIAN_POINT('Ctrl Pts',(-5.91591913630772,0.674539978541786,
10.7798686123602));
#50979=CARTESIAN_POINT('Ctrl Pts',(-5.91650151471712,-0.000138897455152014,
10.8116248077952));
#50980=CARTESIAN_POINT('Origin',(0.,0.,0.));
#50981=CARTESIAN_POINT('',(-5.91681535977711,0.000152256150380351,12.8133751922049));
#50982=CARTESIAN_POINT('',(-5.91666319015572,0.00015412212114384,12.5616248077952));
#50983=CARTESIAN_POINT('',(-5.91675,-7.2459289488551E-16,0.));
#50984=CARTESIAN_POINT('Ctrl Pts',(-5.91681535977711,0.00015225615038035,
12.8133751922049));
#50985=CARTESIAN_POINT('Ctrl Pts',(-5.91703012865227,0.206964346823776,
12.8036393510438));
#50986=CARTESIAN_POINT('Ctrl Pts',(-5.90639892222455,0.413754466608288,
12.7939035098827));
#50987=CARTESIAN_POINT('Ctrl Pts',(-5.88475572670746,0.619385546460389,
12.7841676687216));
#50988=CARTESIAN_POINT('Ctrl Pts',(-5.7816261905285,1.59921488230794,12.7377765162476));
#50989=CARTESIAN_POINT('Ctrl Pts',(-5.42846837276787,2.55272810394278,12.6913853637736));
#50990=CARTESIAN_POINT('Ctrl Pts',(-4.86846200502615,3.3633415116216,12.6449942112996));
#50991=CARTESIAN_POINT('Ctrl Pts',(-4.30845563728443,4.17395491930043,12.5986030588256));
#50992=CARTESIAN_POINT('Ctrl Pts',(-3.54160071956163,4.84166851302325,12.5522119063517));
#50993=CARTESIAN_POINT('Ctrl Pts',(-2.66165870313702,5.28484260562179,12.5058207538777));
#50994=CARTESIAN_POINT('Ctrl Pts',(-1.78171668671241,5.72801669822032,12.4594296014037));
#50995=CARTESIAN_POINT('Ctrl Pts',(-0.78868757158598,5.94665128969457,12.4130384489297));
#50996=CARTESIAN_POINT('Ctrl Pts',(0.196013432083201,5.91401447010601,12.3666472964557));
#50997=CARTESIAN_POINT('Ctrl Pts',(1.18071443575238,5.88137765051745,12.3202561439817));
#50998=CARTESIAN_POINT('Ctrl Pts',(2.15708732796432,5.59746941986609,12.2738649915078));
#50999=CARTESIAN_POINT('Ctrl Pts',(3.005753413678,5.09700253426888,12.2274738390338));
#51000=CARTESIAN_POINT('Ctrl Pts',(3.85441949939168,4.59653564867167,12.1810826865598));
#51001=CARTESIAN_POINT('Ctrl Pts',(4.5753787786071,3.87951010812861,12.1346915340858));
#51002=CARTESIAN_POINT('Ctrl Pts',(5.08048134608114,3.03359484939929,12.0883003816118));
#51003=CARTESIAN_POINT('Ctrl Pts',(5.58558391355517,2.18767959066998,12.0419092291378));
#51004=CARTESIAN_POINT('Ctrl Pts',(5.87482976928782,1.2128746137544,11.9955180766638));
#51005=CARTESIAN_POINT('Ctrl Pts',(5.91285353896481,0.228366908574042,11.9491269241899));
#51006=CARTESIAN_POINT('Ctrl Pts',(5.95087730864179,-0.756140796606319,
11.9027357717159));
#51007=CARTESIAN_POINT('Ctrl Pts',(5.73767899226313,-1.75035123005147,11.8563446192419));
#51008=CARTESIAN_POINT('Ctrl Pts',(5.29932581987711,-2.63270474473765,11.8099534667679));
#51009=CARTESIAN_POINT('Ctrl Pts',(4.86097264749109,-3.51505825942384,11.7635623142939));
#51010=CARTESIAN_POINT('Ctrl Pts',(4.19746461909773,-4.28555485535106,11.7171711618199));
#51011=CARTESIAN_POINT('Ctrl Pts',(3.38992721780971,-4.84998782226649,11.670780009346));
#51012=CARTESIAN_POINT('Ctrl Pts',(2.5823898165217,-5.41442078918191,11.624388856872));
#51013=CARTESIAN_POINT('Ctrl Pts',(1.63082304233903,-5.77279012708554,11.577997704398));
#51014=CARTESIAN_POINT('Ctrl Pts',(0.651572607696405,-5.88127890471792,
11.531606551924));
#51015=CARTESIAN_POINT('Ctrl Pts',(-0.327677826946226,-5.9897676823503,
11.48521539945));
#51016=CARTESIAN_POINT('Ctrl Pts',(-1.33461192204882,-5.84837589971142,
11.438824246976));
#51017=CARTESIAN_POINT('Ctrl Pts',(-2.24611433999348,-5.47439117983507,
11.3924330945021));
#51018=CARTESIAN_POINT('Ctrl Pts',(-3.15761675793815,-5.1004064599587,11.3460419420281));
#51019=CARTESIAN_POINT('Ctrl Pts',(-3.97368749872487,-4.49382880284485,
11.2996507895541));
#51020=CARTESIAN_POINT('Ctrl Pts',(-4.59454761429665,-3.72882295612721,
11.2532596370801));
#51021=CARTESIAN_POINT('Ctrl Pts',(-5.21540772986842,-2.96381710940959,
11.2068684846061));
#51022=CARTESIAN_POINT('Ctrl Pts',(-5.64105722022526,-2.04038307308817,
11.1604773321321));
#51023=CARTESIAN_POINT('Ctrl Pts',(-5.81945297652116,-1.07142683942457,
11.1140861796581));
#51024=CARTESIAN_POINT('Ctrl Pts',(-5.88445549299818,-0.718365786560998,
11.0971825171737));
#51025=CARTESIAN_POINT('Ctrl Pts',(-5.91663078529745,-0.359260871982291,
11.0802788546893));
#51026=CARTESIAN_POINT('Ctrl Pts',(-5.91638614209071,-0.000112643280536506,
11.0633751922049));
#51027=CARTESIAN_POINT('Ctrl Pts',(-5.91650151471712,-0.000138897455152014,
10.8116248077952));
#51028=CARTESIAN_POINT('Ctrl Pts',(-5.91676990590458,-0.31106708737575,
10.8262597648342));
#51029=CARTESIAN_POINT('Ctrl Pts',(-5.89268752645461,-0.621954105016895,
10.8408947218732));
#51030=CARTESIAN_POINT('Ctrl Pts',(-5.84389498008895,-0.928913330743386,
10.8555296789123));
#51031=CARTESIAN_POINT('Ctrl Pts',(-5.68922814697106,-1.90193923071684,
10.9019208313862));
#51032=CARTESIAN_POINT('Ctrl Pts',(-5.28626910131762,-2.83549796933134,
10.9483119838602));
#51033=CARTESIAN_POINT('Ctrl Pts',(-4.68428664750531,-3.61544563205493,
10.9947031363342));
#51034=CARTESIAN_POINT('Ctrl Pts',(-4.08230419369302,-4.39539329477851,
11.0410942888082));
#51035=CARTESIAN_POINT('Ctrl Pts',(-3.28129833172186,-5.0217298816112,11.0874854412822));
#51036=CARTESIAN_POINT('Ctrl Pts',(-2.37920606423197,-5.41787476952573,
11.1338765937562));
#51037=CARTESIAN_POINT('Ctrl Pts',(-1.47711379674208,-5.81401965744026,
11.1802677462301));
#51038=CARTESIAN_POINT('Ctrl Pts',(-0.473935123733492,-5.97997284643662,
11.2266588987041));
#51039=CARTESIAN_POINT('Ctrl Pts',(0.507673783333144,-5.89544365116467,
11.2730500511781));
#51040=CARTESIAN_POINT('Ctrl Pts',(1.48928269039977,-5.81091445589273,11.3194412036521));
#51041=CARTESIAN_POINT('Ctrl Pts',(2.44932183152441,-5.47590287635248,11.3658323561261));
#51042=CARTESIAN_POINT('Ctrl Pts',(3.27040959895255,-4.9313699485458,11.4122235086001));
#51043=CARTESIAN_POINT('Ctrl Pts',(4.09149736638069,-4.38683702073912,11.4586146610741));
#51044=CARTESIAN_POINT('Ctrl Pts',(4.77363376011235,-3.63278274466601,11.505005813548));
#51045=CARTESIAN_POINT('Ctrl Pts',(5.23341565294764,-2.7614034688586,11.551396966022));
#51046=CARTESIAN_POINT('Ctrl Pts',(5.69319754578292,-1.89002419305118,11.597788118496));
#51047=CARTESIAN_POINT('Ctrl Pts',(5.93062493772184,-0.901319917509466,
11.64417927097));
#51048=CARTESIAN_POINT('Ctrl Pts',(5.91666816966309,0.0838229350308153,
11.690570423444));
#51049=CARTESIAN_POINT('Ctrl Pts',(5.90271140160435,1.0689657875711,11.736961575918));
#51050=CARTESIAN_POINT('Ctrl Pts',(5.63737047354794,2.05054721710995,11.7833527283919));
#51051=CARTESIAN_POINT('Ctrl Pts',(5.15308796351401,2.90855169364903,11.8297438808659));
#51052=CARTESIAN_POINT('Ctrl Pts',(4.66880545348009,3.7665561701881,11.8761350333399));
#51053=CARTESIAN_POINT('Ctrl Pts',(3.96558136146864,4.5009836937274,11.9225261858139));
#51054=CARTESIAN_POINT('Ctrl Pts',(3.12939715531371,5.02203763015134,11.9689173382879));
#51055=CARTESIAN_POINT('Ctrl Pts',(2.29321294915875,5.54309156657529,12.0153084907619));
#51056=CARTESIAN_POINT('Ctrl Pts',(1.32406862886034,5.85077191588387,12.0616996432359));
#51057=CARTESIAN_POINT('Ctrl Pts',(0.340459069876811,5.90745936389581,12.1080907957098));
#51058=CARTESIAN_POINT('Ctrl Pts',(-0.643150489106702,5.96414681190774,
12.1544819481838));
#51059=CARTESIAN_POINT('Ctrl Pts',(-1.6412252867753,5.76984135862302,12.2008731006578));
#51060=CARTESIAN_POINT('Ctrl Pts',(-2.5317331898637,5.34830025051737,12.2472642531318));
#51061=CARTESIAN_POINT('Ctrl Pts',(-3.42224109295211,4.92675914241172,12.2936554056058));
#51062=CARTESIAN_POINT('Ctrl Pts',(-4.20518210146036,4.27798237948509,12.3400465580798));
#51063=CARTESIAN_POINT('Ctrl Pts',(-4.78482795763426,3.48129428951119,12.3864377105537));
#51064=CARTESIAN_POINT('Ctrl Pts',(-5.36447381380816,2.68460619953728,12.4328288630277));
#51065=CARTESIAN_POINT('Ctrl Pts',(-5.74082451764775,1.7400067825161,12.4792200155017));
#51066=CARTESIAN_POINT('Ctrl Pts',(-5.86786460082069,0.762989869380371,
12.5256111679757));
#51067=CARTESIAN_POINT('Ctrl Pts',(-5.90073851142677,0.510169138624673,
12.5376157145822));
#51068=CARTESIAN_POINT('Ctrl Pts',(-5.91691836162161,0.25517770356015,12.5496202611887));
#51069=CARTESIAN_POINT('Ctrl Pts',(-5.91666319015572,0.00015412212114384,
12.5616248077952));
#51070=CARTESIAN_POINT('Origin',(0.,0.,0.));
#51071=CARTESIAN_POINT('',(-5.91679636992553,-0.000153270388958127,14.5633751922049));
#51072=CARTESIAN_POINT('',(-5.91694833112707,-0.000138697138948813,14.3116248077952));
#51073=CARTESIAN_POINT('',(-5.91675,-7.2459289488551E-16,0.));
#51074=CARTESIAN_POINT('Ctrl Pts',(-5.91679636992553,-0.000153270388958127,
14.5633751922049));
#51075=CARTESIAN_POINT('Ctrl Pts',(-5.91599400906461,0.77255147152922,14.5269998473983));
#51076=CARTESIAN_POINT('Ctrl Pts',(-5.76385503515043,1.54556283765356,14.4906245025916));
#51077=CARTESIAN_POINT('Ctrl Pts',(-5.46885912034106,2.25955047300182,14.454249157785));
#51078=CARTESIAN_POINT('Ctrl Pts',(-5.09263724434586,3.17013178658265,14.407858005311));
#51079=CARTESIAN_POINT('Ctrl Pts',(-4.48405747423019,3.98471055593761,14.361466852837));
#51080=CARTESIAN_POINT('Ctrl Pts',(-3.71752935102522,4.60369025266104,14.315075700363));
#51081=CARTESIAN_POINT('Ctrl Pts',(-2.95100122782026,5.22266994938447,14.2686845478891));
#51082=CARTESIAN_POINT('Ctrl Pts',(-2.026524751526,5.64605057347636,14.2222933954151));
#51083=CARTESIAN_POINT('Ctrl Pts',(-1.05713337095738,5.82206642474891,14.1759022429411));
#51084=CARTESIAN_POINT('Ctrl Pts',(-0.0877419903887519,5.99808227602147,
14.1295110904671));
#51085=CARTESIAN_POINT('Ctrl Pts',(0.926564294454247,5.92673335447469,14.0831199379931));
#51086=CARTESIAN_POINT('Ctrl Pts',(1.86176876657516,5.61674331601378,14.0367287855192));
#51087=CARTESIAN_POINT('Ctrl Pts',(2.7969732386961,5.30675327755287,13.9903376330452));
#51088=CARTESIAN_POINT('Ctrl Pts',(3.65307589809495,4.75812212217783,13.9439464805712));
#51089=CARTESIAN_POINT('Ctrl Pts',(4.32540319318566,4.03792962228907,13.8975553280972));
#51090=CARTESIAN_POINT('Ctrl Pts',(4.99773048827635,3.31773712240034,13.8511641756232));
#51091=CARTESIAN_POINT('Ctrl Pts',(5.48628241905891,2.4259832779979,13.8047730231492));
#51092=CARTESIAN_POINT('Ctrl Pts',(5.73132495110672,1.47170062274971,13.7583818706752));
#51093=CARTESIAN_POINT('Ctrl Pts',(5.97636748315454,0.517417967501514,13.7119907182013));
#51094=CARTESIAN_POINT('Ctrl Pts',(5.97790061646761,-0.499393498592441,
13.6655995657273));
#51095=CARTESIAN_POINT('Ctrl Pts',(5.73573689863335,-1.45441075622952,13.6192084132533));
#51096=CARTESIAN_POINT('Ctrl Pts',(5.4935731807991,-2.40942801386659,13.5728172607793));
#51097=CARTESIAN_POINT('Ctrl Pts',(5.00771261181753,-3.30265106304676,13.5264261083053));
#51098=CARTESIAN_POINT('Ctrl Pts',(4.33756015997436,-4.0248677340732,13.4800349558313));
#51099=CARTESIAN_POINT('Ctrl Pts',(3.66740770813118,-4.74708440509965,13.4336438033574));
#51100=CARTESIAN_POINT('Ctrl Pts',(2.8129633734264,-5.29829469797234,13.3872526508834));
#51101=CARTESIAN_POINT('Ctrl Pts',(1.87869794819343,-5.61110349553759,13.3408614984094));
#51102=CARTESIAN_POINT('Ctrl Pts',(0.944432522960453,-5.92391229310283,
13.2944703459354));
#51103=CARTESIAN_POINT('Ctrl Pts',(-0.069653992800721,-5.99831959536062,
13.2480791934614));
#51104=CARTESIAN_POINT('Ctrl Pts',(-1.0395717527149,-5.82522780577186,13.2016880409874));
#51105=CARTESIAN_POINT('Ctrl Pts',(-2.00948951262906,-5.65213601618309,
13.1552968885134));
#51106=CARTESIAN_POINT('Ctrl Pts',(-2.93523851669623,-5.23154513474778,
13.1089057360395));
#51107=CARTESIAN_POINT('Ctrl Pts',(-3.70362972728275,-4.61487976672933,
13.0625145835655));
#51108=CARTESIAN_POINT('Ctrl Pts',(-4.47202093786928,-3.99821439871089,
13.0161234310915));
#51109=CARTESIAN_POINT('Ctrl Pts',(-5.08305435497515,-3.1854745441093,12.9697322786175));
#51110=CARTESIAN_POINT('Ctrl Pts',(-5.46202043622944,-2.27603189177837,
12.9233411261435));
#51111=CARTESIAN_POINT('Ctrl Pts',(-5.7614551116923,-1.55744867569876,12.8866858148307));
#51112=CARTESIAN_POINT('Ctrl Pts',(-5.91600675784442,-0.778492489737632,
12.8500305035178));
#51113=CARTESIAN_POINT('Ctrl Pts',(-5.91681535977711,0.00015225615038035,
12.8133751922049));
#51114=CARTESIAN_POINT('Ctrl Pts',(-5.91666319015572,0.00015412212114384,
12.5616248077952));
#51115=CARTESIAN_POINT('Ctrl Pts',(-5.91593226037439,-0.730352049358422,
12.5960114136627));
#51116=CARTESIAN_POINT('Ctrl Pts',(-5.78034933477605,-1.46112198701044,
12.6303980195302));
#51117=CARTESIAN_POINT('Ctrl Pts',(-5.51600270409303,-2.14189231353492,
12.6647846253976));
#51118=CARTESIAN_POINT('Ctrl Pts',(-5.15937126168614,-3.06032317406425,
12.7111757778716));
#51119=CARTESIAN_POINT('Ctrl Pts',(-4.56837891436605,-3.88775048587267,
12.7575669303456));
#51120=CARTESIAN_POINT('Ctrl Pts',(-3.81528483254303,-4.52300676109474,
12.8039580828196));
#51121=CARTESIAN_POINT('Ctrl Pts',(-3.06219075072002,-5.1582630363168,12.8503492352936));
#51122=CARTESIAN_POINT('Ctrl Pts',(-2.14699493439408,-5.60134827495253,
12.8967403877676));
#51123=CARTESIAN_POINT('Ctrl Pts',(-1.18159610907414,-5.79808754240245,
12.9431315402415));
#51124=CARTESIAN_POINT('Ctrl Pts',(-0.216197283754185,-5.99482680985238,
12.9895226927155));
#51125=CARTESIAN_POINT('Ctrl Pts',(0.79940455055973,-5.9452201061165,13.0359138451895));
#51126=CARTESIAN_POINT('Ctrl Pts',(1.74103427324652,-5.65533271998409,13.0823049976635));
#51127=CARTESIAN_POINT('Ctrl Pts',(2.68266399593328,-5.36544533385168,13.1286961501375));
#51128=CARTESIAN_POINT('Ctrl Pts',(3.55032160699291,-4.83527726532272,13.1750873026115));
#51129=CARTESIAN_POINT('Ctrl Pts',(4.2379207595215,-4.12965085090232,13.2214784550854));
#51130=CARTESIAN_POINT('Ctrl Pts',(4.92551991205011,-3.42402443648192,13.2678696075594));
#51131=CARTESIAN_POINT('Ctrl Pts',(5.43306060604772,-2.54293967617006,13.3142607600334));
#51132=CARTESIAN_POINT('Ctrl Pts',(5.69848709804486,-1.59412462115041,13.3606519125074));
#51133=CARTESIAN_POINT('Ctrl Pts',(5.963913590042,-0.645309566130763,13.4070430649814));
#51134=CARTESIAN_POINT('Ctrl Pts',(5.98722588003867,0.371235783596643,13.4534342174554));
#51135=CARTESIAN_POINT('Ctrl Pts',(5.76557363208187,1.3312209461182,13.4998253699294));
#51136=CARTESIAN_POINT('Ctrl Pts',(5.54392138412507,2.29120610863978,13.5462165224033));
#51137=CARTESIAN_POINT('Ctrl Pts',(5.07730459821478,3.19463108395547,13.5926076748773));
#51138=CARTESIAN_POINT('Ctrl Pts',(4.42277535294775,3.93103633813013,13.6389988273513));
#51139=CARTESIAN_POINT('Ctrl Pts',(3.76824610768071,4.66744159230479,13.6853899798253));
#51140=CARTESIAN_POINT('Ctrl Pts',(2.92580440305693,5.23682712533842,13.7317811322993));
#51141=CARTESIAN_POINT('Ctrl Pts',(1.99845349956049,5.56957557848316,13.7781722847733));
#51142=CARTESIAN_POINT('Ctrl Pts',(1.07110259606408,5.9023240316279,13.8245634372472));
#51143=CARTESIAN_POINT('Ctrl Pts',(0.0588424936950185,5.99843540488377,
13.8709545897212));
#51144=CARTESIAN_POINT('Ctrl Pts',(-0.914560272212906,5.84615839871205,
13.9173457421952));
#51145=CARTESIAN_POINT('Ctrl Pts',(-1.88796303812086,5.69388139254032,13.9637368946692));
#51146=CARTESIAN_POINT('Ctrl Pts',(-2.82250846756768,5.29321600694098,14.0101280471432));
#51147=CARTESIAN_POINT('Ctrl Pts',(-3.60393200577741,4.69315060615732,14.0565191996172));
#51148=CARTESIAN_POINT('Ctrl Pts',(-4.38535554398713,4.09308520537367,14.1029103520911));
#51149=CARTESIAN_POINT('Ctrl Pts',(-5.01365719095976,3.29361978940572,14.1493015045651));
#51150=CARTESIAN_POINT('Ctrl Pts',(-5.41201606063222,2.39250301437647,14.1956926570391));
#51151=CARTESIAN_POINT('Ctrl Pts',(-5.7438508902712,1.64186846274086,14.2343367072911));
#51152=CARTESIAN_POINT('Ctrl Pts',(-5.91612913741916,0.82069834722353,14.2729807575432));
#51153=CARTESIAN_POINT('Ctrl Pts',(-5.91694833112707,-0.000138697138948813,
14.3116248077952));
#51154=CARTESIAN_POINT('Origin',(0.,0.,0.));
#51155=CARTESIAN_POINT('',(-5.91639886804204,0.000116455658438486,16.3133751922049));
#51156=CARTESIAN_POINT('',(-5.91630979238255,8.1702894319434E-5,16.0616248077952));
#51157=CARTESIAN_POINT('',(-5.91675,-7.2459289488551E-16,0.));
#51158=CARTESIAN_POINT('Ctrl Pts',(-5.91639886804204,0.000116455658438486,
16.3133751922049));
#51159=CARTESIAN_POINT('Ctrl Pts',(-5.91664831842101,0.35331412429619,16.2967514962267));
#51160=CARTESIAN_POINT('Ctrl Pts',(-5.88553605112261,0.706468355663527,
16.2801278002486));
#51161=CARTESIAN_POINT('Ctrl Pts',(-5.82265747229035,1.05387303721164,16.2635041042704));
#51162=CARTESIAN_POINT('Ctrl Pts',(-5.64718447628607,2.02336282895428,16.2171129517964));
#51163=CARTESIAN_POINT('Ctrl Pts',(-5.22432159535791,2.9480762396989,16.1707217993224));
#51164=CARTESIAN_POINT('Ctrl Pts',(-4.60577122651949,3.71495085124224,16.1243306468484));
#51165=CARTESIAN_POINT('Ctrl Pts',(-3.98722085768104,4.48182546278563,16.0779394943744));
#51166=CARTESIAN_POINT('Ctrl Pts',(-3.1729830009323,5.09086127512771,16.0315483419005));
#51167=CARTESIAN_POINT('Ctrl Pts',(-2.26261250213904,5.46759298808392,15.9851571894265));
#51168=CARTESIAN_POINT('Ctrl Pts',(-1.35224200334581,5.84432470104011,15.9387660369525));
#51169=CARTESIAN_POINT('Ctrl Pts',(-0.345738862508056,5.98875231461044,
15.8923748844785));
#51170=CARTESIAN_POINT('Ctrl Pts',(0.633834274466793,5.88321702223295,15.8459837320045));
#51171=CARTESIAN_POINT('Ctrl Pts',(1.61340741144164,5.77768172985545,15.7995925795305));
#51172=CARTESIAN_POINT('Ctrl Pts',(2.56605054455358,5.42218353153013,15.7532014270566));
#51173=CARTESIAN_POINT('Ctrl Pts',(3.37528635762781,4.86018831139205,15.7068102745826));
#51174=CARTESIAN_POINT('Ctrl Pts',(4.18452217070204,4.29819309125397,15.6604191221086));
#51175=CARTESIAN_POINT('Ctrl Pts',(4.85035066373854,3.52970084930314,15.6140279696346));
#51176=CARTESIAN_POINT('Ctrl Pts',(5.29136263616055,2.64867322839651,15.5676368171606));
#51177=CARTESIAN_POINT('Ctrl Pts',(5.73237460858256,1.76764560748987,15.5212456646866));
#51178=CARTESIAN_POINT('Ctrl Pts',(5.94857006039006,0.774082607627441,15.4748545122126));
#51179=CARTESIAN_POINT('Ctrl Pts',(5.91351530920981,-0.2105352842675,15.4284633597387));
#51180=CARTESIAN_POINT('Ctrl Pts',(5.87846055802955,-1.19515317616244,15.3820722072647));
#51181=CARTESIAN_POINT('Ctrl Pts',(5.59215560386154,-2.17082596008989,15.3356810547907));
#51182=CARTESIAN_POINT('Ctrl Pts',(5.0896062442704,-3.01826054151461,15.2892899023167));
#51183=CARTESIAN_POINT('Ctrl Pts',(4.58705688467926,-3.86569512293933,15.2428987498427));
#51184=CARTESIAN_POINT('Ctrl Pts',(3.86826311966498,-4.58489150186131,15.1965075973688));
#51185=CARTESIAN_POINT('Ctrl Pts',(3.02111008241334,-5.08791531848957,15.1501164448948));
#51186=CARTESIAN_POINT('Ctrl Pts',(2.1739570451617,-5.59093913511783,15.1037252924208));
#51187=CARTESIAN_POINT('Ctrl Pts',(1.19844473567268,-5.87779038945237,15.0573341399468));
#51188=CARTESIAN_POINT('Ctrl Pts',(0.213846627669457,-5.91339648916041,
15.0109429874728));
#51189=CARTESIAN_POINT('Ctrl Pts',(-0.770751480333769,-5.94900258886845,
14.9645518349988));
#51190=CARTESIAN_POINT('Ctrl Pts',(-1.7644353868512,-5.73336353394999,14.9181606825248));
#51191=CARTESIAN_POINT('Ctrl Pts',(-2.64570982200234,-5.29284497750885,
14.8717695300509));
#51192=CARTESIAN_POINT('Ctrl Pts',(-3.52698425715349,-4.85232642106771,
14.8253783775769));
#51193=CARTESIAN_POINT('Ctrl Pts',(-4.29584922093833,-4.18692836310389,
14.7789872251029));
#51194=CARTESIAN_POINT('Ctrl Pts',(-4.85829749872451,-3.37800737596404,
14.7325960726289));
#51195=CARTESIAN_POINT('Ctrl Pts',(-5.4207457765107,-2.56908638882419,14.6862049201549));
#51196=CARTESIAN_POINT('Ctrl Pts',(-5.77677736829822,-1.61664247250831,
14.6398137676809));
#51197=CARTESIAN_POINT('Ctrl Pts',(-5.88286117325461,-0.637128585447021,
14.593422615207));
#51198=CARTESIAN_POINT('Ctrl Pts',(-5.90576457035516,-0.425652427233307,
14.5834068075396));
#51199=CARTESIAN_POINT('Ctrl Pts',(-5.91701729682273,-0.212914472237162,
14.5733909998723));
#51200=CARTESIAN_POINT('Ctrl Pts',(-5.91679636992553,-0.000153270388958127,
14.5633751922049));
#51201=CARTESIAN_POINT('Ctrl Pts',(-5.91694833112707,-0.000138697138948813,
14.3116248077952));
#51202=CARTESIAN_POINT('Ctrl Pts',(-5.91711255763421,-0.164694649446748,
14.3193719100171));
#51203=CARTESIAN_POINT('Ctrl Pts',(-5.91038591951096,-0.329237215769999,
14.3271190122391));
#51204=CARTESIAN_POINT('Ctrl Pts',(-5.89667251930381,-0.493195412011086,
14.3348661144611));
#51205=CARTESIAN_POINT('Ctrl Pts',(-5.81455401593065,-1.4750089292788,14.3812572669351));
#51206=CARTESIAN_POINT('Ctrl Pts',(-5.48190091681204,-2.43586782972369,
14.427648419409));
#51207=CARTESIAN_POINT('Ctrl Pts',(-4.93938589239068,-3.25829027564972,
14.474039571883));
#51208=CARTESIAN_POINT('Ctrl Pts',(-4.39687086796933,-4.08071272157575,
14.520430724357));
#51209=CARTESIAN_POINT('Ctrl Pts',(-3.64449391824523,-4.76469871298291,
14.566821876831));
#51210=CARTESIAN_POINT('Ctrl Pts',(-2.7742463092126,-5.22661897694503,14.613213029305));
#51211=CARTESIAN_POINT('Ctrl Pts',(-1.90399870017996,-5.68853924090715,
14.659604181779));
#51212=CARTESIAN_POINT('Ctrl Pts',(-0.91588043183879,-5.92839377742422,
14.7059953342529));
#51213=CARTESIAN_POINT('Ctrl Pts',(0.0692937227240556,-5.91685616643946,
14.7523864867269));
#51214=CARTESIAN_POINT('Ctrl Pts',(1.0544678772869,-5.90531855545469,14.7987776392009));
#51215=CARTESIAN_POINT('Ctrl Pts',(2.03669791807142,-5.64238879696809,14.8451687916749));
#51216=CARTESIAN_POINT('Ctrl Pts',(2.89588901098887,-5.160214661269,14.8915599441489));
#51217=CARTESIAN_POINT('Ctrl Pts',(3.75508010390632,-4.67804052556991,14.9379510966229));
#51218=CARTESIAN_POINT('Ctrl Pts',(4.49123224895671,-3.97662201265833,14.9843422490968));
#51219=CARTESIAN_POINT('Ctrl Pts',(5.01433794682421,-3.14171982668418,15.0307334015708));
#51220=CARTESIAN_POINT('Ctrl Pts',(5.5374436446917,-2.30681764071002,15.0771245540448));
#51221=CARTESIAN_POINT('Ctrl Pts',(5.84750289537631,-1.33843178167331,15.1235157065188));
#51222=CARTESIAN_POINT('Ctrl Pts',(5.90660552231805,-0.354964389852698,
15.1699068589928));
#51223=CARTESIAN_POINT('Ctrl Pts',(5.9657081492598,0.628503001967902,15.2162980114668));
#51224=CARTESIAN_POINT('Ctrl Pts',(5.77385415245868,1.62705192657243,15.2626891639407));
#51225=CARTESIAN_POINT('Ctrl Pts',(5.35450104487847,2.51859228036953,15.3090803164147));
#51226=CARTESIAN_POINT('Ctrl Pts',(4.93514793729825,3.41013263416665,15.3554714688887));
#51227=CARTESIAN_POINT('Ctrl Pts',(4.28829571893895,4.19466441715633,15.4018626213627));
#51228=CARTESIAN_POINT('Ctrl Pts',(3.49303340827702,4.77626487152903,15.4482537738367));
#51229=CARTESIAN_POINT('Ctrl Pts',(2.69777109761512,5.35786532590172,15.4946449263107));
#51230=CARTESIAN_POINT('Ctrl Pts',(1.75409869465059,5.73653445165742,15.5410360787846));
#51231=CARTESIAN_POINT('Ctrl Pts',(0.777396686603823,5.86597331275885,15.5874272312586));
#51232=CARTESIAN_POINT('Ctrl Pts',(-0.199305321442962,5.99541217386027,
15.6338183837326));
#51233=CARTESIAN_POINT('Ctrl Pts',(-1.20903693457202,5.87562077030744,15.6802095362066));
#51234=CARTESIAN_POINT('Ctrl Pts',(-2.12834076956585,5.52124570028771,15.7266006886806));
#51235=CARTESIAN_POINT('Ctrl Pts',(-3.04764460455968,5.16687063026797,15.7729918411546));
#51236=CARTESIAN_POINT('Ctrl Pts',(-3.87652066141828,4.57791189378134,15.8193829936286));
#51237=CARTESIAN_POINT('Ctrl Pts',(-4.51362431780749,3.82638001667875,15.8657741461025));
#51238=CARTESIAN_POINT('Ctrl Pts',(-5.15072797419671,3.07484813957616,15.9121652985765));
#51239=CARTESIAN_POINT('Ctrl Pts',(-5.59605923011654,2.1607431218576,15.9585564510505));
#51240=CARTESIAN_POINT('Ctrl Pts',(-5.79516853599763,1.19583031978821,16.0049476035245));
#51241=CARTESIAN_POINT('Ctrl Pts',(-5.87625410368171,0.802877805714503,
16.0238400049481));
#51242=CARTESIAN_POINT('Ctrl Pts',(-5.91650483938724,0.401499043140845,
16.0427324063716));
#51243=CARTESIAN_POINT('Ctrl Pts',(-5.91630979238255,8.1702894319434E-5,
16.0616248077952));
#51244=CARTESIAN_POINT('Origin',(0.,0.,0.));
#51245=CARTESIAN_POINT('',(-5.91719822611734,-6.82369026905327E-5,18.0633751922049));
#51246=CARTESIAN_POINT('',(-5.91725660741841,-1.9475412519191E-5,17.8116248077952));
#51247=CARTESIAN_POINT('',(-5.91675,-7.2459289488551E-16,0.));
#51248=CARTESIAN_POINT('Ctrl Pts',(-5.91719822611734,-6.82369026905327E-5,
18.0633751922049));
#51249=CARTESIAN_POINT('Ctrl Pts',(-5.91666274279714,0.918771692973182,
18.0201119925812));
#51250=CARTESIAN_POINT('Ctrl Pts',(-5.69916543753697,1.83785627542067,17.9768487929575));
#51251=CARTESIAN_POINT('Ctrl Pts',(-5.28633221943619,2.65869894571221,17.9335855933338));
#51252=CARTESIAN_POINT('Ctrl Pts',(-4.84365093525427,3.53888898726857,17.8871944408598));
#51253=CARTESIAN_POINT('Ctrl Pts',(-4.17636686005132,4.3061176826772,17.8408032883858));
#51254=CARTESIAN_POINT('Ctrl Pts',(-3.36606716483014,4.86657787978705,17.7944121359119));
#51255=CARTESIAN_POINT('Ctrl Pts',(-2.55576746960896,5.4270380768969,17.7480209834379));
#51256=CARTESIAN_POINT('Ctrl Pts',(-1.60245215436954,5.78072977570796,17.7016298309639));
#51257=CARTESIAN_POINT('Ctrl Pts',(-0.622680721330418,5.88440796830605,
17.6552386784899));
#51258=CARTESIAN_POINT('Ctrl Pts',(0.35709071170871,5.98808616090414,17.6088475260159));
#51259=CARTESIAN_POINT('Ctrl Pts',(1.36331826254754,5.84175084728925,17.5624563735419));
#51260=CARTESIAN_POINT('Ctrl Pts',(2.27297298098518,5.46329408378239,17.516065221068));
#51261=CARTESIAN_POINT('Ctrl Pts',(3.18262769942285,5.08483732027552,17.469674068594));
#51262=CARTESIAN_POINT('Ctrl Pts',(3.99570958545932,4.47425910687667,17.42328291612));
#51263=CARTESIAN_POINT('Ctrl Pts',(4.61280513090447,3.70621332932708,17.376891763646));
#51264=CARTESIAN_POINT('Ctrl Pts',(5.2299006763496,2.93816755177751,17.330500611172));
#51265=CARTESIAN_POINT('Ctrl Pts',(5.65100988120343,2.01265421007721,17.284109458698));
#51266=CARTESIAN_POINT('Ctrl Pts',(5.82464476608204,1.04283352800596,17.237718306224));
#51267=CARTESIAN_POINT('Ctrl Pts',(5.99827965096066,0.0730128459347218,
17.1913271537501));
#51268=CARTESIAN_POINT('Ctrl Pts',(5.92444021586407,-0.941115176507489,
17.1449360012761));
#51269=CARTESIAN_POINT('Ctrl Pts',(5.61215462562019,-1.87555561802635,17.0985448488021));
#51270=CARTESIAN_POINT('Ctrl Pts',(5.29986903537631,-2.80999605954522,17.0521536963281));
#51271=CARTESIAN_POINT('Ctrl Pts',(4.74913728998514,-3.66474892014077,17.0057625438541));
#51272=CARTESIAN_POINT('Ctrl Pts',(4.02729599578517,-4.33530568478315,16.9593713913801));
#51273=CARTESIAN_POINT('Ctrl Pts',(3.30545470158519,-5.00586244942553,16.9129802389062));
#51274=CARTESIAN_POINT('Ctrl Pts',(2.41250385857643,-5.49222311811475,16.8665890864322));
#51275=CARTESIAN_POINT('Ctrl Pts',(1.45762235448143,-5.73492157661256,16.8201979339582));
#51276=CARTESIAN_POINT('Ctrl Pts',(0.502740850386421,-5.97762003511037,
16.7738067814842));
#51277=CARTESIAN_POINT('Ctrl Pts',(-0.514071314794815,-5.97665628341679,
16.7274156290102));
#51278=CARTESIAN_POINT('Ctrl Pts',(-1.46849103628399,-5.73214815706415,
16.6810244765362));
#51279=CARTESIAN_POINT('Ctrl Pts',(-2.42291075777316,-5.4876400307115,16.6346333240623));
#51280=CARTESIAN_POINT('Ctrl Pts',(-3.31493803557027,-4.99958752969981,
16.5882421715883));
#51281=CARTESIAN_POINT('Ctrl Pts',(-4.03550690398349,-4.32766362441467,
16.5418510191143));
#51282=CARTESIAN_POINT('Ctrl Pts',(-4.7560757723967,-3.65573971912954,16.4954598666403));
#51283=CARTESIAN_POINT('Ctrl Pts',(-5.30518623142603,-2.799944409571,16.4490687141663));
#51284=CARTESIAN_POINT('Ctrl Pts',(-5.61569990540051,-1.8649136684214,16.4026775616923));
#51285=CARTESIAN_POINT('Ctrl Pts',(-5.81494484303325,-1.26493963404005,
16.3729101051965));
#51286=CARTESIAN_POINT('Ctrl Pts',(-5.9159521861902,-0.632341948862379,
16.3431426487007));
#51287=CARTESIAN_POINT('Ctrl Pts',(-5.91639886804204,0.000116455658438486,
16.3133751922049));
#51288=CARTESIAN_POINT('Ctrl Pts',(-5.91630979238255,8.1702894319434E-5,
16.0616248077952));
#51289=CARTESIAN_POINT('Ctrl Pts',(-5.91602589258047,-0.584199525271585,
16.0891235588456));
#51290=CARTESIAN_POINT('Ctrl Pts',(-5.83005303644549,-1.16856248459223,
16.116622309896));
#51291=CARTESIAN_POINT('Ctrl Pts',(-5.65959094982708,-1.72714179932542,
16.1441210609464));
#51292=CARTESIAN_POINT('Ctrl Pts',(-5.37201670193311,-2.66948052994944,
16.1905122134204));
#51293=CARTESIAN_POINT('Ctrl Pts',(-4.84398085030286,-3.53843740477723,
16.2369033658944));
#51294=CARTESIAN_POINT('Ctrl Pts',(-4.14004503056272,-4.22776721914234,
16.2832945183684));
#51295=CARTESIAN_POINT('Ctrl Pts',(-3.43610921082259,-4.91709703350743,
16.3296856708424));
#51296=CARTESIAN_POINT('Ctrl Pts',(-2.55627342297255,-5.42679978740986,
16.3760768233164));
#51297=CARTESIAN_POINT('Ctrl Pts',(-1.60811300942713,-5.694555387671,16.4224679757903));
#51298=CARTESIAN_POINT('Ctrl Pts',(-0.659952595881694,-5.96231098793215,
16.4688591282643));
#51299=CARTESIAN_POINT('Ctrl Pts',(0.356532443359141,-5.98811943455204,
16.5152502807383));
#51300=CARTESIAN_POINT('Ctrl Pts',(1.31705900039552,-5.76882519269035,16.5616414332123));
#51301=CARTESIAN_POINT('Ctrl Pts',(2.2775855574319,-5.54953095082865,16.6080325856863));
#51302=CARTESIAN_POINT('Ctrl Pts',(3.18215363226381,-5.08513402048537,16.6544237381603));
#51303=CARTESIAN_POINT('Ctrl Pts',(3.92016392700974,-4.43241506401568,16.7008148906342));
#51304=CARTESIAN_POINT('Ctrl Pts',(4.65817422175568,-3.77969610754599,16.7472060431082));
#51305=CARTESIAN_POINT('Ctrl Pts',(5.22962673641563,-2.93865512494991,16.7935971955822));
#51306=CARTESIAN_POINT('Ctrl Pts',(5.56465138751824,-2.01212411389878,16.8399883480562));
#51307=CARTESIAN_POINT('Ctrl Pts',(5.89967603862086,-1.08559310284766,16.8863795005302));
#51308=CARTESIAN_POINT('Ctrl Pts',(5.99827282616614,-0.0735720633414831,
16.9327706530042));
#51309=CARTESIAN_POINT('Ctrl Pts',(5.8483865651666,0.900201698910001,16.9791618054781));
#51310=CARTESIAN_POINT('Ctrl Pts',(5.69850030416705,1.8739754611615,17.0255529579521));
#51311=CARTESIAN_POINT('Ctrl Pts',(5.30013099462269,2.80950194615832,17.0719441104261));
#51312=CARTESIAN_POINT('Ctrl Pts',(4.70198626524495,3.59239664789253,17.1183352629001));
#51313=CARTESIAN_POINT('Ctrl Pts',(4.1038415358672,4.37529134962675,17.1647264153741));
#51314=CARTESIAN_POINT('Ctrl Pts',(3.30592138665607,5.00555426809834,17.2111175678481));
#51315=CARTESIAN_POINT('Ctrl Pts',(2.40578553779589,5.40612471743612,17.2575087203221));
#51316=CARTESIAN_POINT('Ctrl Pts',(1.50564968893573,5.80669516677389,17.303899872796));
#51317=CARTESIAN_POINT('Ctrl Pts',(0.50329814042653,5.97757314697785,17.35029102527));
#51318=CARTESIAN_POINT('Ctrl Pts',(-0.478714066734747,5.8978658306757,17.396682177744));
#51319=CARTESIAN_POINT('Ctrl Pts',(-1.46072627389601,5.81815851437354,17.443073330218));
#51320=CARTESIAN_POINT('Ctrl Pts',(-2.42239913970938,5.48786590156526,17.489464482692));
#51321=CARTESIAN_POINT('Ctrl Pts',(-3.24615130494937,4.94737205187937,17.535855635166));
#51322=CARTESIAN_POINT('Ctrl Pts',(-4.06990347018936,4.40687820219348,17.5822467876399));
#51323=CARTESIAN_POINT('Ctrl Pts',(-4.755734934856,3.65618311562998,17.6286379401139));
#51324=CARTESIAN_POINT('Ctrl Pts',(-5.21979078457892,2.7870724209404,17.6750290925879));
#51325=CARTESIAN_POINT('Ctrl Pts',(-5.67525148709518,1.93405921616332,17.720560997657));
#51326=CARTESIAN_POINT('Ctrl Pts',(-5.91707585786333,0.966976319151631,
17.7660929027261));
#51327=CARTESIAN_POINT('Ctrl Pts',(-5.91725660741841,-1.9475412519191E-5,
17.8116248077952));
#51328=CARTESIAN_POINT('Origin',(0.,0.,0.));
#51329=CARTESIAN_POINT('',(-5.9162403766418,-6.30554099573244E-6,19.8133751922049));
#51330=CARTESIAN_POINT('',(-5.91626547054495,-5.06783466652393E-5,19.5616248077952));
#51331=CARTESIAN_POINT('',(-5.91675,-7.2459289488551E-16,0.));
#51332=CARTESIAN_POINT('Ctrl Pts',(-5.9162403766418,-6.30554099573244E-6,
19.8133751922049));
#51333=CARTESIAN_POINT('Ctrl Pts',(-5.91622190953983,0.499573431236169,
19.7898636414097));
#51334=CARTESIAN_POINT('Ctrl Pts',(-5.85363170713743,0.999157711713498,
19.7663520906144));
#51335=CARTESIAN_POINT('Ctrl Pts',(-5.72852485080488,1.48256246137935,19.7428405398192));
#51336=CARTESIAN_POINT('Ctrl Pts',(-5.48167379031089,2.4363788915969,19.6964493873452));
#51337=CARTESIAN_POINT('Ctrl Pts',(-4.99143230021176,3.32720501911184,19.6500582348712));
#51338=CARTESIAN_POINT('Ctrl Pts',(-4.31774099316667,4.04612173990211,19.6036670823972));
#51339=CARTESIAN_POINT('Ctrl Pts',(-3.64404968612158,4.76503846069237,19.5572759299233));
#51340=CARTESIAN_POINT('Ctrl Pts',(-2.78690856213052,5.31204577475796,19.5108847774493));
#51341=CARTESIAN_POINT('Ctrl Pts',(-1.85111814327297,5.62026245275307,19.4644936249753));
#51342=CARTESIAN_POINT('Ctrl Pts',(-0.915327724415407,5.92847913074819,
19.4181024725013));
#51343=CARTESIAN_POINT('Ctrl Pts',(0.0991119893086599,5.99790517267283,
19.3717113200273));
#51344=CARTESIAN_POINT('Ctrl Pts',(1.068167966884,5.82005202835019,19.3253201675533));
#51345=CARTESIAN_POINT('Ctrl Pts',(2.03722394445934,5.64219888402755,19.2789290150793));
#51346=CARTESIAN_POINT('Ctrl Pts',(2.96089618588596,5.21706655345763,19.2325378626054));
#51347=CARTESIAN_POINT('Ctrl Pts',(3.72624957415409,4.59663491364028,19.1861467101314));
#51348=CARTESIAN_POINT('Ctrl Pts',(4.49160296242219,3.97620327382295,19.1397555576574));
#51349=CARTESIAN_POINT('Ctrl Pts',(5.09863749753183,3.16047232475821,19.0933644051834));
#51350=CARTESIAN_POINT('Ctrl Pts',(5.47313257050844,2.24917946901088,19.0469732527094));
#51351=CARTESIAN_POINT('Ctrl Pts',(5.84762764348506,1.33788661326349,19.0005821002354));
#51352=CARTESIAN_POINT('Ctrl Pts',(5.98958325432864,0.331031850833484,18.9541909477615));
#51353=CARTESIAN_POINT('Ctrl Pts',(5.88164284212742,-0.648279180470583,
18.9077997952875));
#51354=CARTESIAN_POINT('Ctrl Pts',(5.7737024299262,-1.62759021177459,18.8614086428135));
#51355=CARTESIAN_POINT('Ctrl Pts',(5.41586599468022,-2.57935751195267,18.8150174903395));
#51356=CARTESIAN_POINT('Ctrl Pts',(4.85188531096097,-3.38721085075339,18.7686263378655));
#51357=CARTESIAN_POINT('Ctrl Pts',(4.28790462724169,-4.19506418955415,18.7222351853915));
#51358=CARTESIAN_POINT('Ctrl Pts',(3.51777969504913,-4.85900356697753,18.6758440329176));
#51359=CARTESIAN_POINT('Ctrl Pts',(2.6356717822319,-5.29785075993339,18.6294528804436));
#51360=CARTESIAN_POINT('Ctrl Pts',(1.7535638694147,-5.73669795288924,18.5830617279696));
#51361=CARTESIAN_POINT('Ctrl Pts',(0.759472975972835,-5.95045296137758,
18.5366705754956));
#51362=CARTESIAN_POINT('Ctrl Pts',(-0.225055866930035,-5.91298048998478,
18.4902794230216));
#51363=CARTESIAN_POINT('Ctrl Pts',(-1.20958470983288,-5.87550801859199,
18.4438882705476));
#51364=CARTESIAN_POINT('Ctrl Pts',(-2.18455150219673,-5.58680806731807,
18.3974971180736));
#51365=CARTESIAN_POINT('Ctrl Pts',(-3.03074946932609,-5.08217926409134,
18.3511059655997));
#51366=CARTESIAN_POINT('Ctrl Pts',(-3.87694743645549,-4.57755046086458,
18.3047148131257));
#51367=CARTESIAN_POINT('Ctrl Pts',(-4.59437657835038,-3.85699280568499,
18.2583236606517));
#51368=CARTESIAN_POINT('Ctrl Pts',(-5.0953186109136,-3.00860709821967,18.2119325081777));
#51369=CARTESIAN_POINT('Ctrl Pts',(-5.59626064347681,-2.16022139075437,
18.1655413557037));
#51370=CARTESIAN_POINT('Ctrl Pts',(-5.88071556670836,-1.18400763100336,
18.1191502032297));
#51371=CARTESIAN_POINT('Ctrl Pts',(-5.91390378174369,-0.199325057275803,
18.0727590507558));
#51372=CARTESIAN_POINT('Ctrl Pts',(-5.91614151817142,-0.132932210819952,
18.0696310979055));
#51373=CARTESIAN_POINT('Ctrl Pts',(-5.91723694185247,-0.0665008633059073,
18.0665031450552));
#51374=CARTESIAN_POINT('Ctrl Pts',(-5.91719822611734,-6.82369026905327E-5,
18.0633751922049));
#51375=CARTESIAN_POINT('Ctrl Pts',(-5.91725660741841,-1.9475412519191E-5,
17.8116248077952));
#51376=CARTESIAN_POINT('Ctrl Pts',(-5.91726001840211,-0.0182679678874798,
17.8124840552001));
#51377=CARTESIAN_POINT('Ctrl Pts',(-5.91717737358503,-0.0365164293429135,
17.813343302605));
#51378=CARTESIAN_POINT('Ctrl Pts',(-5.91700848474174,-0.0547640925781233,
17.8142025500099));
#51379=CARTESIAN_POINT('Ctrl Pts',(-5.90789010040242,-1.03996360859147,
17.8605937024839));
#51380=CARTESIAN_POINT('Ctrl Pts',(-5.64737309694456,-2.02283633780253,
17.9069848549578));
#51381=CARTESIAN_POINT('Ctrl Pts',(-5.16731024307657,-2.88320886620057,
17.9533760074318));
#51382=CARTESIAN_POINT('Ctrl Pts',(-4.6872473892086,-3.74358139459857,17.9997671599058));
#51383=CARTESIAN_POINT('Ctrl Pts',(-3.98763868493051,-4.48145372218359,
18.0461583123798));
#51384=CARTESIAN_POINT('Ctrl Pts',(-3.15402355357354,-5.00660802718217,
18.0925494648538));
#51385=CARTESIAN_POINT('Ctrl Pts',(-2.32040842221657,-5.53176233218075,
18.1389406173278));
#51386=CARTESIAN_POINT('Ctrl Pts',(-1.35278686378078,-5.84419861459291,
18.1853317698017));
#51387=CARTESIAN_POINT('Ctrl Pts',(-0.369467569403431,-5.90571606407731,
18.2317229222757));
#51388=CARTESIAN_POINT('Ctrl Pts',(0.613851724973923,-5.96723351356171,
18.2781140747497));
#51389=CARTESIAN_POINT('Ctrl Pts',(1.6128687552928,-5.77783213011833,18.3245052272237));
#51390=CARTESIAN_POINT('Ctrl Pts',(2.50543618383567,-5.36066955175085,18.3708963796977));
#51391=CARTESIAN_POINT('Ctrl Pts',(3.39800361237853,-4.94350697338336,18.4172875321717));
#51392=CARTESIAN_POINT('Ctrl Pts',(4.18412143914543,-4.29858320009175,18.4636786846456));
#51393=CARTESIAN_POINT('Ctrl Pts',(4.76767298468275,-3.5047514641509,18.5100698371196));
#51394=CARTESIAN_POINT('Ctrl Pts',(5.35122453022008,-2.71091972821004,18.5564609895936));
#51395=CARTESIAN_POINT('Ctrl Pts',(5.73220979452784,-1.7681800296199,18.6028521420676));
#51396=CARTESIAN_POINT('Ctrl Pts',(5.86404665304509,-0.791798816147322,
18.6492432945416));
#51397=CARTESIAN_POINT('Ctrl Pts',(5.99588351156234,0.184582397325205,18.6956344470156));
#51398=CARTESIAN_POINT('Ctrl Pts',(5.87857196428913,1.19460512568014,18.7420255994895));
#51399=CARTESIAN_POINT('Ctrl Pts',(5.52645540352815,2.11477639176251,18.7884167519635));
#51400=CARTESIAN_POINT('Ctrl Pts',(5.17433884276716,3.03494765784494,18.8348079044375));
#51401=CARTESIAN_POINT('Ctrl Pts',(4.58741726851836,3.86526746165476,18.8811990569115));
#51402=CARTESIAN_POINT('Ctrl Pts',(3.83745212785197,4.50421465749424,18.9275902093855));
#51403=CARTESIAN_POINT('Ctrl Pts',(3.08748698718558,5.14316185333373,18.9739813618595));
#51404=CARTESIAN_POINT('Ctrl Pts',(2.17447828010157,5.5907364412029,19.0203725143335));
#51405=CARTESIAN_POINT('Ctrl Pts',(1.2100573196794,5.79221458489168,19.0667636668074));
#51406=CARTESIAN_POINT('Ctrl Pts',(0.245636359257291,5.99369272858046,19.1131548192814));
#51407=CARTESIAN_POINT('Ctrl Pts',(-0.77019685450301,5.94907442808888,19.1595459717554));
#51408=CARTESIAN_POINT('Ctrl Pts',(-1.71323891078853,5.6638150524979,19.2059371242294));
#51409=CARTESIAN_POINT('Ctrl Pts',(-2.65628096707413,5.37855567690688,19.2523282767034));
#51410=CARTESIAN_POINT('Ctrl Pts',(-3.52653186588491,4.85265522621645,19.2987194291774));
#51411=CARTESIAN_POINT('Ctrl Pts',(-4.21758818544739,4.15041424586946,19.3451105816513));
#51412=CARTESIAN_POINT('Ctrl Pts',(-4.90864450500983,3.44817326552251,19.3915017341253));
#51413=CARTESIAN_POINT('Ctrl Pts',(-5.42050624532396,2.56959175551903,19.4378928865993));
#51414=CARTESIAN_POINT('Ctrl Pts',(-5.69058933929046,1.6220917008281,19.4842840390733));
#51415=CARTESIAN_POINT('Ctrl Pts',(-5.84067854805978,1.09555177036103,19.5100642953139));
#51416=CARTESIAN_POINT('Ctrl Pts',(-5.91610189576638,0.547728477777345,
19.5358445515546));
#51417=CARTESIAN_POINT('Ctrl Pts',(-5.91626547054495,-5.06783466652393E-5,
19.5616248077952));
#51418=CARTESIAN_POINT('Origin',(0.,0.,0.));
#51419=CARTESIAN_POINT('',(-5.917172481729,8.05799595049797E-5,21.5633751922049));
#51420=CARTESIAN_POINT('',(-5.91705519232424,0.000118322035579633,21.3116248077952));
#51421=CARTESIAN_POINT('',(-5.91675,-7.2459289488551E-16,0.));
#51422=CARTESIAN_POINT('Ctrl Pts',(-5.917172481729,8.05799595049797E-5,
21.5633751922049));
#51423=CARTESIAN_POINT('Ctrl Pts',(-5.91722591425258,0.0799357853801551,
21.5596152902381));
#51424=CARTESIAN_POINT('Ctrl Pts',(-5.91564301057614,0.159788870386215,
21.5558553882713));
#51425=CARTESIAN_POINT('Ctrl Pts',(-5.9124100156559,0.239575092512105,21.5520954863046));
#51426=CARTESIAN_POINT('Ctrl Pts',(-5.87252005000849,1.22400894974203,21.5057043338306));
#51427=CARTESIAN_POINT('Ctrl Pts',(-5.5814268424811,2.19826387152037,21.4593131813566));
#51428=CARTESIAN_POINT('Ctrl Pts',(-5.07472163851603,3.04322012180477,21.4129220288826));
#51429=CARTESIAN_POINT('Ctrl Pts',(-4.56801643455097,3.88817637208916,21.3665308764086));
#51430=CARTESIAN_POINT('Ctrl Pts',(-3.84569923414823,4.60383395087964,21.3201397239346));
#51431=CARTESIAN_POINT('Ctrl Pts',(-2.99608597221093,5.10269117871161,21.2737485714607));
#51432=CARTESIAN_POINT('Ctrl Pts',(-2.14647271027362,5.60154840654358,21.2273574189867));
#51433=CARTESIAN_POINT('Ctrl Pts',(-1.16956338680175,5.88360528341705,21.1809662665127));
#51434=CARTESIAN_POINT('Ctrl Pts',(-0.18480228495773,5.91437541365567,21.1345751140387));
#51435=CARTESIAN_POINT('Ctrl Pts',(0.799958816886288,5.94514554389429,21.0881839615647));
#51436=CARTESIAN_POINT('Ctrl Pts',(1.79257169710246,5.72462892749805,21.0417928090907));
#51437=CARTESIAN_POINT('Ctrl Pts',(2.67167203754318,5.27978758493088,20.9954016566168));
#51438=CARTESIAN_POINT('Ctrl Pts',(3.55077237798389,4.83494624236371,20.9490105041428));
#51439=CARTESIAN_POINT('Ctrl Pts',(4.31636017864916,4.16578017362559,20.9026193516688));
#51440=CARTESIAN_POINT('Ctrl Pts',(4.87482891552365,3.35410665640716,20.8562281991948));
#51441=CARTESIAN_POINT('Ctrl Pts',(5.43329765239815,2.54243313918872,20.8098370467208));
#51442=CARTESIAN_POINT('Ctrl Pts',(5.78464732548189,1.58825217348994,20.7634458942468));
#51443=CARTESIAN_POINT('Ctrl Pts',(5.88591928054512,0.60822910246681,20.7170547417728));
#51444=CARTESIAN_POINT('Ctrl Pts',(5.98719123560835,-0.37179396855635,20.6706635892989));
#51445=CARTESIAN_POINT('Ctrl Pts',(5.83838547265108,-1.37765914490381,20.6242724368249));
#51446=CARTESIAN_POINT('Ctrl Pts',(5.45769610371606,-2.28638178300624,20.5778812843509));
#51447=CARTESIAN_POINT('Ctrl Pts',(5.07700673478105,-3.19510442110866,20.5314901318769));
#51448=CARTESIAN_POINT('Ctrl Pts',(4.4644337598683,-4.00668452096599,20.4850989794029));
#51449=CARTESIAN_POINT('Ctrl Pts',(3.6948749592683,-4.62189219406429,20.438707826929));
#51450=CARTESIAN_POINT('Ctrl Pts',(2.92531615866827,-5.23709986716261,20.392316674455));
#51451=CARTESIAN_POINT('Ctrl Pts',(1.99877153238097,-5.6559351135019,20.345925521981));
#51452=CARTESIAN_POINT('Ctrl Pts',(1.02852739679816,-5.82718798497319,20.299534369507));
#51453=CARTESIAN_POINT('Ctrl Pts',(0.0582832612154045,-5.99844085644447,
20.253143217033));
#51454=CARTESIAN_POINT('Ctrl Pts',(-0.955660383662874,-5.92211135304779,
20.206752064559));
#51455=CARTESIAN_POINT('Ctrl Pts',(-1.88933115993044,-5.60753209409417,
20.160360912085));
#51456=CARTESIAN_POINT('Ctrl Pts',(-2.82300193619803,-5.29295283514055,
20.1139697596111));
#51457=CARTESIAN_POINT('Ctrl Pts',(-3.67639984385493,-4.74012382062998,
20.0675786071371));
#51458=CARTESIAN_POINT('Ctrl Pts',(-4.34518203461083,-4.01663808480122,
20.0211874546631));
#51459=CARTESIAN_POINT('Ctrl Pts',(-5.01396422536674,-3.29315234897246,
19.9747963021891));
#51460=CARTESIAN_POINT('Ctrl Pts',(-5.49813069922166,-2.39900989182551,
19.9284051497151));
#51461=CARTESIAN_POINT('Ctrl Pts',(-5.7384836207047,-1.44353529679196,19.8820139972411));
#51462=CARTESIAN_POINT('Ctrl Pts',(-5.85702301480442,-0.972305827750752,
19.8591343955624));
#51463=CARTESIAN_POINT('Ctrl Pts',(-5.91625834738056,-0.486158218010563,
19.8362547938837));
#51464=CARTESIAN_POINT('Ctrl Pts',(-5.9162403766418,-6.30554099573244E-6,
19.8133751922049));
#51465=CARTESIAN_POINT('Ctrl Pts',(-5.91626547054495,-5.06783466652393E-5,
19.5616248077952));
#51466=CARTESIAN_POINT('Ctrl Pts',(-5.91639624592421,-0.437991218591476,
19.5822357040285));
#51467=CARTESIAN_POINT('Ctrl Pts',(-5.86842290975251,-0.875903547946226,
19.6028466002619));
#51468=CARTESIAN_POINT('Ctrl Pts',(-5.77204196744726,-1.30288911284467,
19.6234574964952));
#51469=CARTESIAN_POINT('Ctrl Pts',(-5.55510705401869,-2.26395127244807,
19.6698486489692));
#51470=CARTESIAN_POINT('Ctrl Pts',(-5.09293277954264,-3.16965699227654,
19.7162398014432));
#51471=CARTESIAN_POINT('Ctrl Pts',(-4.442028047747,-3.90926787741268,19.7626309539172));
#51472=CARTESIAN_POINT('Ctrl Pts',(-3.79112331595134,-4.64887876254883,
19.8090221063912));
#51473=CARTESIAN_POINT('Ctrl Pts',(-2.95148812683609,-5.2223948129927,19.8554132588652));
#51474=CARTESIAN_POINT('Ctrl Pts',(-2.02578259518584,-5.55969364186407,
19.9018044113391));
#51475=CARTESIAN_POINT('Ctrl Pts',(-1.10007706353559,-5.89699247073543,
19.9481955638131));
#51476=CARTESIAN_POINT('Ctrl Pts',(-0.0883011893503864,-5.99807407803428,
19.9945867162871));
#51477=CARTESIAN_POINT('Ctrl Pts',(0.885837697416628,-5.85057946601678,
20.0409778687611));
#51478=CARTESIAN_POINT('Ctrl Pts',(1.85997658418364,-5.70308485399929,20.0873690212351));
#51479=CARTESIAN_POINT('Ctrl Pts',(2.79647848353242,-5.30701402266545,20.1337601737091));
#51480=CARTESIAN_POINT('Ctrl Pts',(3.58083962795835,-4.71079357148928,20.1801513261831));
#51481=CARTESIAN_POINT('Ctrl Pts',(4.36520077238426,-4.11457312031313,20.2265424786571));
#51482=CARTESIAN_POINT('Ctrl Pts',(4.99742116188733,-3.31820304929461,20.272933631131));
#51483=CARTESIAN_POINT('Ctrl Pts',(5.400200775462,-2.4190535543971,20.319324783605));
#51484=CARTESIAN_POINT('Ctrl Pts',(5.80298038903667,-1.51990405949956,20.365715936079));
#51485=CARTESIAN_POINT('Ctrl Pts',(5.97631922668297,-0.517975140722991,
20.412107088553));
#51486=CARTESIAN_POINT('Ctrl Pts',(5.89902357808467,0.464229834826226,20.458498241027));
#51487=CARTESIAN_POINT('Ctrl Pts',(5.82172792948637,1.44643481037541,20.5048893935009));
#51488=CARTESIAN_POINT('Ctrl Pts',(5.49379779464347,2.40891584269728,20.5512805459749));
#51489=CARTESIAN_POINT('Ctrl Pts',(4.95532837885557,3.23399276004914,20.5976716984489));
#51490=CARTESIAN_POINT('Ctrl Pts',(4.41685896306763,4.05906967740105,20.6440628509229));
#51491=CARTESIAN_POINT('Ctrl Pts',(3.66785026633468,4.74674247978297,20.6904540033969));
#51492=CARTESIAN_POINT('Ctrl Pts',(2.79988172670085,5.21293111702315,20.7368451558709));
#51493=CARTESIAN_POINT('Ctrl Pts',(1.93191318706708,5.67911975426331,20.7832363083449));
#51494=CARTESIAN_POINT('Ctrl Pts',(0.944984804532506,5.92382422636172,20.8296274608188));
#51495=CARTESIAN_POINT('Ctrl Pts',(-0.0402341322062733,5.91712512365145,
20.8760186132928));
#51496=CARTESIAN_POINT('Ctrl Pts',(-1.02545306894505,5.91042602094118,20.9224097657668));
#51497=CARTESIAN_POINT('Ctrl Pts',(-2.00896255988798,5.65232334342222,20.9688009182408));
#51498=CARTESIAN_POINT('Ctrl Pts',(-2.87051133574473,5.17437466615075,21.0151920707148));
#51499=CARTESIAN_POINT('Ctrl Pts',(-3.7320601116015,4.69642598887926,21.0615832231888));
#51500=CARTESIAN_POINT('Ctrl Pts',(-4.4716481723721,3.99863131185519,21.1079743756627));
#51501=CARTESIAN_POINT('Ctrl Pts',(-4.99884791783631,3.16630826179089,21.1543655281367));
#51502=CARTESIAN_POINT('Ctrl Pts',(-5.52604766330052,2.33398521172659,21.2007566806107));
#51503=CARTESIAN_POINT('Ctrl Pts',(-5.84085909345838,1.36713378862203,21.2471478330847));
#51504=CARTESIAN_POINT('Ctrl Pts',(-5.90479099453697,0.383968521075246,
21.2935389855587));
#51505=CARTESIAN_POINT('Ctrl Pts',(-5.91309905140046,0.256204559560241,
21.2995675929709));
#51506=CARTESIAN_POINT('Ctrl Pts',(-5.91717039659536,0.128165099062277,
21.305596200383));
#51507=CARTESIAN_POINT('Ctrl Pts',(-5.91705519232424,0.000118322035579633,
21.3116248077952));
#51508=CARTESIAN_POINT('Origin',(0.,0.,0.));
#51509=CARTESIAN_POINT('',(-5.91642923825227,-0.000124498022167352,23.3133751922049));
#51510=CARTESIAN_POINT('',(-5.91655481024517,-0.00014617215624503,23.0616248077952));
#51511=CARTESIAN_POINT('',(-5.91675,-7.2459289488551E-16,0.));
#51512=CARTESIAN_POINT('Ctrl Pts',(-5.91642923825227,-0.000124498022167352,
23.3133751922049));
#51513=CARTESIAN_POINT('Ctrl Pts',(-5.9159381515581,0.645751202424775,23.2829757865926));
#51514=CARTESIAN_POINT('Ctrl Pts',(-5.81051644106084,1.29178331094863,23.2525763809803));
#51515=CARTESIAN_POINT('Ctrl Pts',(-5.60287574930939,1.90309530922156,23.222176975368));
#51516=CARTESIAN_POINT('Ctrl Pts',(-5.28600471854996,2.83599079022973,23.175785822894));
#51517=CARTESIAN_POINT('Ctrl Pts',(-4.73108176846316,3.6880285989829,23.12939467042));
#51518=CARTESIAN_POINT('Ctrl Pts',(-4.00595595360395,4.35503218311477,23.0830035179461));
#51519=CARTESIAN_POINT('Ctrl Pts',(-3.28083013874475,5.02203576724663,23.0366123654721));
#51520=CARTESIAN_POINT('Ctrl Pts',(-2.38550145911315,5.50400512675718,22.9902212129981));
#51521=CARTESIAN_POINT('Ctrl Pts',(-1.42943953462563,5.74201106190414,22.9438300605241));
#51522=CARTESIAN_POINT('Ctrl Pts',(-0.473377610138116,5.98001699705111,
22.8974389080501));
#51523=CARTESIAN_POINT('Ctrl Pts',(0.543417559205304,5.97405950783449,22.8510477555761));
#51524=CARTESIAN_POINT('Ctrl Pts',(1.49662494666533,5.724867001704,22.8046566031021));
#51525=CARTESIAN_POINT('Ctrl Pts',(2.44983233412535,5.47567449557351,22.7582654506282));
#51526=CARTESIAN_POINT('Ctrl Pts',(3.33945193970195,4.98324697252917,22.7118742981541));
#51527=CARTESIAN_POINT('Ctrl Pts',(4.05671217782192,4.30779232606351,22.6654831456802));
#51528=CARTESIAN_POINT('Ctrl Pts',(4.77397241594188,3.63233767959784,22.6190919932062));
#51529=CARTESIAN_POINT('Ctrl Pts',(5.31887328660519,2.77385590971089,22.5727008407322));
#51530=CARTESIAN_POINT('Ctrl Pts',(5.62479111008316,1.83731145593495,22.5263096882582));
#51531=CARTESIAN_POINT('Ctrl Pts',(5.93070893356112,0.900767002159047,22.4799185357843));
#51532=CARTESIAN_POINT('Ctrl Pts',(5.99764370985374,-0.11384013550589,22.4335273833102));
#51533=CARTESIAN_POINT('Ctrl Pts',(5.81741148966215,-1.08245645553395,22.3871362308363));
#51534=CARTESIAN_POINT('Ctrl Pts',(5.63717926947054,-2.05107277556205,22.3407450783623));
#51535=CARTESIAN_POINT('Ctrl Pts',(5.20978005279472,-2.97369827795332,22.2943539258883));
#51536=CARTESIAN_POINT('Ctrl Pts',(4.58747088318358,-3.73752582788711,22.2479627734143));
#51537=CARTESIAN_POINT('Ctrl Pts',(3.96516171357244,-4.5013533778209,22.2015716209404));
#51538=CARTESIAN_POINT('Ctrl Pts',(3.147942591026,-5.10638297529717,22.1551804684663));
#51539=CARTESIAN_POINT('Ctrl Pts',(2.23573287339444,-5.47863915009957,22.1087893159924));
#51540=CARTESIAN_POINT('Ctrl Pts',(1.32352315576289,-5.85089532490197,22.0623981635184));
#51541=CARTESIAN_POINT('Ctrl Pts',(0.316322843046232,-5.99037807703048,
22.0160070110444));
#51542=CARTESIAN_POINT('Ctrl Pts',(-0.662720177369385,-5.88003319588315,
21.9696158585704));
#51543=CARTESIAN_POINT('Ctrl Pts',(-1.641763197785,-5.76968831473581,21.9232247060964));
#51544=CARTESIAN_POINT('Ctrl Pts',(-2.59264892589957,-5.40951580031264,
21.8768335536224));
#51545=CARTESIAN_POINT('Ctrl Pts',(-3.39911491909419,-4.84355305379962,
21.8304424011485));
#51546=CARTESIAN_POINT('Ctrl Pts',(-4.20558091228882,-4.2775903072866,21.7840512486745));
#51547=CARTESIAN_POINT('Ctrl Pts',(-4.86762717056349,-3.50583732868374,
21.7376600962005));
#51548=CARTESIAN_POINT('Ctrl Pts',(-5.30430693781711,-2.62265444304155,
21.6912689437265));
#51549=CARTESIAN_POINT('Ctrl Pts',(-5.70559476009434,-1.81105160858726,
21.6486376932193));
#51550=CARTESIAN_POINT('Ctrl Pts',(-5.91656664271564,-0.905349214931068,
21.6060064427121));
#51551=CARTESIAN_POINT('Ctrl Pts',(-5.917172481729,8.05799595049797E-5,
21.5633751922049));
#51552=CARTESIAN_POINT('Ctrl Pts',(-5.91705519232424,0.000118322035579633,
21.3116248077952));
#51553=CARTESIAN_POINT('Ctrl Pts',(-5.91628388026723,-0.857176481624185,
21.351987352857));
#51554=CARTESIAN_POINT('Ctrl Pts',(-5.72784928662205,-1.71479925078451,
21.3923498979188));
#51555=CARTESIAN_POINT('Ctrl Pts',(-5.36680573393853,-2.49226497959308,
21.4327124429806));
#51556=CARTESIAN_POINT('Ctrl Pts',(-4.95183620026223,-3.38585410072555,
21.4791035954546));
#51557=CARTESIAN_POINT('Ctrl Pts',(-4.30884476091035,-4.17355323100148,
21.5254947479286));
#51558=CARTESIAN_POINT('Ctrl Pts',(-3.51644838647332,-4.75905234890422,
21.5718859004026));
#51559=CARTESIAN_POINT('Ctrl Pts',(-2.7240520120363,-5.34455146680696,21.6182770528766));
#51560=CARTESIAN_POINT('Ctrl Pts',(-1.78225070251412,-5.72785057233648,
21.6646682053505));
#51561=CARTESIAN_POINT('Ctrl Pts',(-0.806196171166689,-5.86208463329708,
21.7110593578245));
#51562=CARTESIAN_POINT('Ctrl Pts',(0.169858360180775,-5.99631869425769,
21.7574505102985));
#51563=CARTESIAN_POINT('Ctrl Pts',(1.18016611335355,-5.88148771064937,21.8038416627725));
#51564=CARTESIAN_POINT('Ctrl Pts',(2.10119926191803,-5.53163178239991,21.8502328152465));
#51565=CARTESIAN_POINT('Ctrl Pts',(3.02223241048248,-5.18177585415046,21.8966239677205));
#51566=CARTESIAN_POINT('Ctrl Pts',(3.85399095443862,-4.59689498125992,21.9430151201944));
#51567=CARTESIAN_POINT('Ctrl Pts',(4.49477783689496,-3.8485010992982,21.9894062726684));
#51568=CARTESIAN_POINT('Ctrl Pts',(5.13556471935129,-3.10010721733648,22.0357974251424));
#51569=CARTESIAN_POINT('Ctrl Pts',(5.58537994030777,-2.18820032630358,22.0821885776164));
#51570=CARTESIAN_POINT('Ctrl Pts',(5.78922570689681,-1.22427702295961,22.1285797300904));
#51571=CARTESIAN_POINT('Ctrl Pts',(5.99307147348585,-0.260353719615633,
22.1749708825644));
#51572=CARTESIAN_POINT('Ctrl Pts',(5.95094778570745,0.755585996039466,22.2213620350384));
#51573=CARTESIAN_POINT('Ctrl Pts',(5.66800500252533,1.69932569146983,22.2677531875123));
#51574=CARTESIAN_POINT('Ctrl Pts',(5.3850622193432,2.64306538690021,22.3141443399863));
#51575=CARTESIAN_POINT('Ctrl Pts',(4.8613003407573,3.51460506210591,22.3605354924603));
#51576=CARTESIAN_POINT('Ctrl Pts',(4.16075843429663,4.20738371981581,22.4069266449343));
#51577=CARTESIAN_POINT('Ctrl Pts',(3.46021652783598,4.90016237752569,22.4533177974083));
#51578=CARTESIAN_POINT('Ctrl Pts',(2.58289459350059,5.41418001773979,22.4997089498823));
#51579=CARTESIAN_POINT('Ctrl Pts',(1.63606061106249,5.6865889768183,22.5461001023563));
#51580=CARTESIAN_POINT('Ctrl Pts',(0.689226628624362,5.95899793589682,22.5924912548302));
#51581=CARTESIAN_POINT('Ctrl Pts',(-0.327119401916475,5.98979821383971,
22.6388824073042));
#51582=CARTESIAN_POINT('Ctrl Pts',(-1.28871136890952,5.77522393695561,22.6852735597782));
#51583=CARTESIAN_POINT('Ctrl Pts',(-2.25030333590257,5.5606496600715,22.7316647122522));
#51584=CARTESIAN_POINT('Ctrl Pts',(-3.1571412393478,5.10070082836044,22.7780558647262));
#51585=CARTESIAN_POINT('Ctrl Pts',(-3.89834825504163,4.45161424617581,22.8244470172002));
#51586=CARTESIAN_POINT('Ctrl Pts',(-4.63955527073545,3.8025276639912,22.8708381696741));
#51587=CARTESIAN_POINT('Ctrl Pts',(-5.21513139867784,2.96430333133301,22.9172293221481));
#51588=CARTESIAN_POINT('Ctrl Pts',(-5.55470237141563,2.03942886106165,22.9636204746221));
#51589=CARTESIAN_POINT('Ctrl Pts',(-5.79382430863389,1.3881429951588,22.9962885856798));
#51590=CARTESIAN_POINT('Ctrl Pts',(-5.91591570474866,0.693888947129682,
23.0289566967375));
#51591=CARTESIAN_POINT('Ctrl Pts',(-5.91655481024517,-0.00014617215624503,
23.0616248077952));
#51592=CARTESIAN_POINT('Origin',(0.,0.,0.));
#51593=CARTESIAN_POINT('',(-5.91675358287475,0.000154743843751581,25.0633751922049));
#51594=CARTESIAN_POINT('',(-5.91660456592006,0.00015087079125364,24.8116248077952));
#51595=CARTESIAN_POINT('',(-5.91675,-7.2459289488551E-16,0.));
#51596=CARTESIAN_POINT('Ctrl Pts',(-5.91675358287475,0.000154743843751581,
25.0633751922049));
#51597=CARTESIAN_POINT('Ctrl Pts',(-5.91698729620724,0.226344858207055,
25.0527274354211));
#51598=CARTESIAN_POINT('Ctrl Pts',(-5.90426631585309,0.452508838225063,
25.0420796786372));
#51599=CARTESIAN_POINT('Ctrl Pts',(-5.87838809320626,0.677157178084404,
25.0314319218534));
#51600=CARTESIAN_POINT('Ctrl Pts',(-5.7656394084893,1.65592628401005,24.9850407693794));
#51601=CARTESIAN_POINT('Ctrl Pts',(-5.40313298671896,2.60592470624721,24.9386496169054));
#51602=CARTESIAN_POINT('Ctrl Pts',(-4.83519159015146,3.41099849086875,24.8922584644314));
#51603=CARTESIAN_POINT('Ctrl Pts',(-4.26725019358391,4.21607227549036,24.8458673119574));
#51604=CARTESIAN_POINT('Ctrl Pts',(-3.49387382221916,4.87622142249632,24.7994761594835));
#51605=CARTESIAN_POINT('Ctrl Pts',(-2.60962128931955,5.31073113088118,24.7530850070095));
#51606=CARTESIAN_POINT('Ctrl Pts',(-1.72536875642002,5.74524083926599,24.7066938545355));
#51607=CARTESIAN_POINT('Ctrl Pts',(-0.730240061985659,5.95411110902974,
24.6603027020615));
#51608=CARTESIAN_POINT('Ctrl Pts',(0.254092873463193,5.91180388966308,24.6139115495875));
#51609=CARTESIAN_POINT('Ctrl Pts',(1.23842580891207,5.86949667029642,24.5675203971135));
#51610=CARTESIAN_POINT('Ctrl Pts',(2.21196298537544,5.57601196179933,24.5211292446396));
#51611=CARTESIAN_POINT('Ctrl Pts',(3.05567242375276,5.0672334125139,24.4747380921656));
#51612=CARTESIAN_POINT('Ctrl Pts',(3.89938186213007,4.55845486322847,24.4283469396916));
#51613=CARTESIAN_POINT('Ctrl Pts',(4.61326356242133,3.8343824731547,24.3819557872176));
#51614=CARTESIAN_POINT('Ctrl Pts',(5.1100329774272,2.98354677988914,24.3355646347436));
#51615=CARTESIAN_POINT('Ctrl Pts',(5.60680239243305,2.13271108662361,24.2891734822696));
#51616=CARTESIAN_POINT('Ctrl Pts',(5.88645952215352,1.1551120901663,24.2427823297956));
#51617=CARTESIAN_POINT('Ctrl Pts',(5.91481138205244,0.17027839828723,24.1963911773217));
#51618=CARTESIAN_POINT('Ctrl Pts',(5.94316324195136,-0.8145552935919,24.1500000248477));
#51619=CARTESIAN_POINT('Ctrl Pts',(5.72020983202869,-1.8066236808928,24.1036088723737));
#51620=CARTESIAN_POINT('Ctrl Pts',(5.27321111345687,-2.68462901926789,24.0572177198997));
#51621=CARTESIAN_POINT('Ctrl Pts',(4.82621239488508,-3.56263435764293,24.0108265674257));
#51622=CARTESIAN_POINT('Ctrl Pts',(4.15516836766416,-4.32657664709217,23.9644354149517));
#51623=CARTESIAN_POINT('Ctrl Pts',(3.34212592281667,-4.88305055618075,23.9180442624778));
#51624=CARTESIAN_POINT('Ctrl Pts',(2.52908347796912,-5.43952446526937,23.8716531100038));
#51625=CARTESIAN_POINT('Ctrl Pts',(1.57404261549497,-5.78852999399728,23.8252619575298));
#51626=CARTESIAN_POINT('Ctrl Pts',(0.593773815998961,-5.88739510085864,
23.7788708050558));
#51627=CARTESIAN_POINT('Ctrl Pts',(-0.386494983496995,-5.98626020772,23.7324796525818));
#51628=CARTESIAN_POINT('Ctrl Pts',(-1.39199172001481,-5.83498489271484,
23.6860885001078));
#51629=CARTESIAN_POINT('Ctrl Pts',(-2.29977679821038,-5.45206521389771,
23.6396973476339));
#51630=CARTESIAN_POINT('Ctrl Pts',(-3.20756187640595,-5.06914553508058,
23.5933061951599));
#51631=CARTESIAN_POINT('Ctrl Pts',(-4.01763529627927,-4.45458149245148,
23.5469150426859));
#51632=CARTESIAN_POINT('Ctrl Pts',(-4.63095138734598,-3.68351430921866,
23.5005238902119));
#51633=CARTESIAN_POINT('Ctrl Pts',(-5.2442674784127,-2.91244712598584,23.4541327377379));
#51634=CARTESIAN_POINT('Ctrl Pts',(-5.66082624067281,-1.9848768021493,23.4077415852639));
#51635=CARTESIAN_POINT('Ctrl Pts',(-5.82969606608683,-1.01421506359947,
23.36135043279));
#51636=CARTESIAN_POINT('Ctrl Pts',(-5.88790810343836,-0.679612968514472,
23.3453586859283));
#51637=CARTESIAN_POINT('Ctrl Pts',(-5.91668757666193,-0.339890374940268,
23.3293669390666));
#51638=CARTESIAN_POINT('Ctrl Pts',(-5.91642923825227,-0.000124498022167352,
23.3133751922049));
#51639=CARTESIAN_POINT('Ctrl Pts',(-5.91655481024517,-0.00014617215624503,
23.0616248077952));
#51640=CARTESIAN_POINT('Ctrl Pts',(-5.91682328218658,-0.291692649070739,
23.0753478492115));
#51641=CARTESIAN_POINT('Ctrl Pts',(-5.89565996578793,-0.583200493247537,
23.0890708906278));
#51642=CARTESIAN_POINT('Ctrl Pts',(-5.85273708803951,-0.871468354347098,
23.102793932044));
#51643=CARTESIAN_POINT('Ctrl Pts',(-5.70763501439238,-1.84596649159989,
23.149185084518));
#51644=CARTESIAN_POINT('Ctrl Pts',(-5.3138650495649,-2.78343815822088,23.195576236992));
#51645=CARTESIAN_POINT('Ctrl Pts',(-4.71957247178265,-3.56926101566318,
23.241967389466));
#51646=CARTESIAN_POINT('Ctrl Pts',(-4.1252798940004,-4.35508387310549,23.28835854194));
#51647=CARTESIAN_POINT('Ctrl Pts',(-3.33046470326339,-4.98925792136908,
23.334749694414));
#51648=CARTESIAN_POINT('Ctrl Pts',(-2.43230698417431,-5.39424427043108,
23.381140846888));
#51649=CARTESIAN_POINT('Ctrl Pts',(-1.53414926508527,-5.79923061949304,
23.4275319993619));
#51650=CARTESIAN_POINT('Ctrl Pts',(-0.53264901764413,-5.97502926935343,
23.4739231518359));
#51651=CARTESIAN_POINT('Ctrl Pts',(0.449742803624946,-5.90014575454956,
23.5203143043099));
#51652=CARTESIAN_POINT('Ctrl Pts',(1.43213462489411,-5.82526223974569,23.5667054567839));
#51653=CARTESIAN_POINT('Ctrl Pts',(2.39541801999124,-5.49969656027755,23.6130966092579));
#51654=CARTESIAN_POINT('Ctrl Pts',(3.22181471426473,-4.96325482534283,23.6594877617319));
#51655=CARTESIAN_POINT('Ctrl Pts',(4.04821140853817,-4.42681309040814,23.7058789142058));
#51656=CARTESIAN_POINT('Ctrl Pts',(4.73772140198794,-3.6794953000069,23.7522700666798));
#51657=CARTESIAN_POINT('Ctrl Pts',(5.20604001564117,-2.8126741492545,23.7986612191538));
#51658=CARTESIAN_POINT('Ctrl Pts',(5.67435862929443,-1.94585299850204,23.8450523716278));
#51659=CARTESIAN_POINT('Ctrl Pts',(5.92148586315112,-0.959528487398357,
23.8914435241018));
#51660=CARTESIAN_POINT('Ctrl Pts',(5.91720608246528,0.0257039292238365,
23.9378346765758));
#51661=CARTESIAN_POINT('Ctrl Pts',(5.91292630177943,1.010936345846,23.9842258290497));
#51662=CARTESIAN_POINT('Ctrl Pts',(5.6572395065511,1.99507666798671,24.0306169815237));
#51663=CARTESIAN_POINT('Ctrl Pts',(5.18140788789295,2.85779649618763,24.0770081339977));
#51664=CARTESIAN_POINT('Ctrl Pts',(4.70557626923483,3.72051632438851,24.1233992864717));
#51665=CARTESIAN_POINT('Ctrl Pts',(4.00959982714694,4.46181565864958,24.1697904389457));
#51666=CARTESIAN_POINT('Ctrl Pts',(3.17857387725964,4.99105766557993,24.2161815914197));
#51667=CARTESIAN_POINT('Ctrl Pts',(2.34754792737227,5.52029967251033,24.2625727438937));
#51668=CARTESIAN_POINT('Ctrl Pts',(1.38147246968551,5.83748435210995,24.3089638963677));
#51669=CARTESIAN_POINT('Ctrl Pts',(0.398467157427821,5.90383031927519,24.3553550488416));
#51670=CARTESIAN_POINT('Ctrl Pts',(-0.584538154829837,5.97017628644043,
24.4017462013156));
#51671=CARTESIAN_POINT('Ctrl Pts',(-1.58447332165837,5.78568354117129,24.4481373537896));
#51672=CARTESIAN_POINT('Ctrl Pts',(-2.47907874706353,5.37290955444064,24.4945285062636));
#51673=CARTESIAN_POINT('Ctrl Pts',(-3.37368417246867,4.96013556771,24.5409196587376));
#51674=CARTESIAN_POINT('Ctrl Pts',(-4.16295985645046,4.31908033951782,24.5873108112116));
#51675=CARTESIAN_POINT('Ctrl Pts',(-4.75040301617563,3.52812410471217,24.6337019636855));
#51676=CARTESIAN_POINT('Ctrl Pts',(-5.33784617590082,2.73716786990651,24.6800931161595));
#51677=CARTESIAN_POINT('Ctrl Pts',(-5.72345681136941,1.79631062848735,24.7264842686335));
#51678=CARTESIAN_POINT('Ctrl Pts',(-5.86008726534579,0.820588664846031,
24.7728754211075));
#51679=CARTESIAN_POINT('Ctrl Pts',(-5.8981286159921,0.548923159302109,24.7857918833367));
#51680=CARTESIAN_POINT('Ctrl Pts',(-5.91686888656188,0.27455492139041,24.798708345566));
#51681=CARTESIAN_POINT('Ctrl Pts',(-5.91660456592006,0.00015087079125364,
24.8116248077952));
#51682=CARTESIAN_POINT('Origin',(0.,0.,0.));
#51683=CARTESIAN_POINT('',(-5.91685813319025,-0.000149150696060474,26.8133751922049));
#51684=CARTESIAN_POINT('',(-5.91700643196177,-0.000128843304525861,26.5616248077952));
#51685=CARTESIAN_POINT('',(-5.91675,-7.2459289488551E-16,0.));
#51686=CARTESIAN_POINT('Ctrl Pts',(-5.91685813319025,-0.000149150696060474,
26.8133751922049));
#51687=CARTESIAN_POINT('Ctrl Pts',(-5.91603947382885,0.791903180632938,
26.7760879317755));
#51688=CARTESIAN_POINT('Ctrl Pts',(-5.7559669811698,1.5842763881686,26.7388006713462));
#51689=CARTESIAN_POINT('Ctrl Pts',(-5.44640144828155,2.3131579458258,26.7015134109168));
#51690=CARTESIAN_POINT('Ctrl Pts',(-5.06125376857705,3.21999999019643,26.6551222584428));
#51691=CARTESIAN_POINT('Ctrl Pts',(-4.44470236403523,4.02856184536616,26.6087311059688));
#51692=CARTESIAN_POINT('Ctrl Pts',(-3.67213144768269,4.63998265612277,26.5623399534948));
#51693=CARTESIAN_POINT('Ctrl Pts',(-2.89956053133025,5.2514034668793,26.5159488010208));
#51694=CARTESIAN_POINT('Ctrl Pts',(-1.97097010316713,5.66568323322276,26.4695576485469));
#51695=CARTESIAN_POINT('Ctrl Pts',(-0.999896614712929,5.83216899429929,
26.4231664960729));
#51696=CARTESIAN_POINT('Ctrl Pts',(-0.0288231262586201,5.99865475537583,
26.3767753435989));
#51697=CARTESIAN_POINT('Ctrl Pts',(0.984733422486779,5.91734651118538,26.3303841911249));
#51698=CARTESIAN_POINT('Ctrl Pts',(1.91684798290235,5.59818561934342,26.2839930386509));
#51699=CARTESIAN_POINT('Ctrl Pts',(2.84896254331783,5.27902472750149,26.2376018861769));
#51700=CARTESIAN_POINT('Ctrl Pts',(3.6996351154035,4.72201118800808,26.191210733703));
#51701=CARTESIAN_POINT('Ctrl Pts',(4.36485607089869,3.99524966660648,26.144819581229));
#51702=CARTESIAN_POINT('Ctrl Pts',(5.0300770263939,3.26848814520484,26.098428428755));
#51703=CARTESIAN_POINT('Ctrl Pts',(5.50984636529861,2.37197864189498,26.052037276281));
#51704=CARTESIAN_POINT('Ctrl Pts',(5.74550387894051,1.41533515297964,26.005646123807));
#51705=CARTESIAN_POINT('Ctrl Pts',(5.9811613925824,0.458691664064318,25.9592549713331));
#51706=CARTESIAN_POINT('Ctrl Pts',(5.97270708096148,-0.558085810456485,
25.9128638188591));
#51707=CARTESIAN_POINT('Ctrl Pts',(5.7211746318182,-1.51067840734559,25.8664726663851));
#51708=CARTESIAN_POINT('Ctrl Pts',(5.46964218267493,-2.46327100423464,25.8200815139111));
#51709=CARTESIAN_POINT('Ctrl Pts',(4.97503159600933,-3.35167872349201,25.7736903614371));
#51710=CARTESIAN_POINT('Ctrl Pts',(4.29781768309543,-4.06727815388284,25.7272992089631));
#51711=CARTESIAN_POINT('Ctrl Pts',(3.62060377018146,-4.78287758427373,25.6809080564892));
#51712=CARTESIAN_POINT('Ctrl Pts',(2.76078653101917,-5.32566872579805,25.6345169040152));
#51713=CARTESIAN_POINT('Ctrl Pts',(1.82349368966122,-5.62928585008312,25.5881257515412));
#51714=CARTESIAN_POINT('Ctrl Pts',(0.886200848303285,-5.93290297436818,
25.5417345990672));
#51715=CARTESIAN_POINT('Ctrl Pts',(-0.128567595250301,-5.997346081414,25.4953434465932));
#51716=CARTESIAN_POINT('Ctrl Pts',(-1.09673841700233,-5.81473587214859,
25.4489522941192));
#51717=CARTESIAN_POINT('Ctrl Pts',(-2.06490923875435,-5.63212566288317,
25.4025611416452));
#51718=CARTESIAN_POINT('Ctrl Pts',(-2.98648243870481,-5.20246213730653,
25.3561699891713));
#51719=CARTESIAN_POINT('Ctrl Pts',(-3.74877954444589,-4.57827919040816,
25.3097788366973));
#51720=CARTESIAN_POINT('Ctrl Pts',(-4.51107665018696,-3.95409624350979,
25.2633876842233));
#51721=CARTESIAN_POINT('Ctrl Pts',(-5.11409766171865,-3.1353938752897,25.2169965317493));
#51722=CARTESIAN_POINT('Ctrl Pts',(-5.48411269365271,-2.22227279637257,
25.1706053792753));
#51723=CARTESIAN_POINT('Ctrl Pts',(-5.76920140114136,-1.5187324380027,25.1348619835852));
#51724=CARTESIAN_POINT('Ctrl Pts',(-5.91596903188523,-0.759141596503511,
25.0991185878951));
#51725=CARTESIAN_POINT('Ctrl Pts',(-5.91675358287475,0.000154743843751581,
25.0633751922049));
#51726=CARTESIAN_POINT('Ctrl Pts',(-5.91660456592006,0.00015087079125364,
24.8116248077952));
#51727=CARTESIAN_POINT('Ctrl Pts',(-5.91591954463069,-0.711002882665989,
24.8450994980399));
#51728=CARTESIAN_POINT('Ctrl Pts',(-5.7875893169904,-1.42239717367699,24.8785741882847));
#51729=CARTESIAN_POINT('Ctrl Pts',(-5.53677480568972,-2.08760946190163,
24.9120488785294));
#51730=CARTESIAN_POINT('Ctrl Pts',(-5.18918161957311,-3.00949893914454,
24.9584400310034));
#51731=CARTESIAN_POINT('Ctrl Pts',(-4.60634497485573,-3.84269120776689,
25.0048311834774));
#51732=CARTESIAN_POINT('Ctrl Pts',(-3.85952686439241,-4.48531391291345,
25.0512223359514));
#51733=CARTESIAN_POINT('Ctrl Pts',(-3.11270875392911,-5.12793661806,25.0976134884254));
#51734=CARTESIAN_POINT('Ctrl Pts',(-2.20190917771993,-5.57998975973076,
25.1440046408994));
#51735=CARTESIAN_POINT('Ctrl Pts',(-1.23848934388416,-5.78620192003589,
25.1903957933733));
#51736=CARTESIAN_POINT('Ctrl Pts',(-0.275069510048367,-5.99241408034102,
25.2367869458473));
#51737=CARTESIAN_POINT('Ctrl Pts',(0.740970581413977,-5.95278525928045,
25.2831780983213));
#51738=CARTESIAN_POINT('Ctrl Pts',(1.6854022252657,-5.67216077464409,25.3295692507953));
#51739=CARTESIAN_POINT('Ctrl Pts',(2.6298338691174,-5.39153629000774,25.3759604032693));
#51740=CARTESIAN_POINT('Ctrl Pts',(3.50265706535853,-4.86991614179561,25.4223515557433));
#51741=CARTESIAN_POINT('Ctrl Pts',(4.19715388378028,-4.17107753346899,25.4687427082172));
#51742=CARTESIAN_POINT('Ctrl Pts',(4.89165070220204,-3.47223892514236,25.5151338606912));
#51743=CARTESIAN_POINT('Ctrl Pts',(5.40782114280446,-2.59618185670121,25.5615250131652));
#51744=CARTESIAN_POINT('Ctrl Pts',(5.6825543243767,-1.65001965589786,25.6079161656392));
#51745=CARTESIAN_POINT('Ctrl Pts',(5.95728750594894,-0.703857455094489,
25.6543073181132));
#51746=CARTESIAN_POINT('Ctrl Pts',(5.99058342849101,0.31240987807104,25.7006984705872));
#51747=CARTESIAN_POINT('Ctrl Pts',(5.77837108202817,1.27452585408153,25.7470896230612));
#51748=CARTESIAN_POINT('Ctrl Pts',(5.56615873556533,2.236641830092,25.7934807755351));
#51749=CARTESIAN_POINT('Ctrl Pts',(5.10843812009756,3.14460644894739,25.8398719280091));
#51750=CARTESIAN_POINT('Ctrl Pts',(4.46117360149757,3.88740512574169,25.8862630804831));
#51751=CARTESIAN_POINT('Ctrl Pts',(3.81390908289758,4.63020380253599,25.9326542329571));
#51752=CARTESIAN_POINT('Ctrl Pts',(2.97710066116534,5.20783653726923,25.9790453854311));
#51753=CARTESIAN_POINT('Ctrl Pts',(2.05306282923954,5.54967760627017,26.0254365379051));
#51754=CARTESIAN_POINT('Ctrl Pts',(1.12902499731371,5.89151867527112,26.071827690379));
#51755=CARTESIAN_POINT('Ctrl Pts',(0.117757755194285,5.99756807853976,26.118218842853));
#51756=CARTESIAN_POINT('Ctrl Pts',(-0.857093756348307,5.85485941822435,
26.164609995327));
#51757=CARTESIAN_POINT('Ctrl Pts',(-1.83194526789087,5.71215075790894,26.211001147801));
#51758=CARTESIAN_POINT('Ctrl Pts',(-2.77038104885656,5.32068403400952,26.257392300275));
#51759=CARTESIAN_POINT('Ctrl Pts',(-3.5576608808258,4.72832291318851,26.303783452749));
#51760=CARTESIAN_POINT('Ctrl Pts',(-4.34494071279503,4.13596179236749,26.350174605223));
#51761=CARTESIAN_POINT('Ctrl Pts',(-4.98106459576776,3.34270627462487,26.3965657576969));
#51762=CARTESIAN_POINT('Ctrl Pts',(-5.38825523826091,2.44554574720971,26.4429569101709));
#51763=CARTESIAN_POINT('Ctrl Pts',(-5.7354511646396,1.6805711924923,26.4825128760457));
#51764=CARTESIAN_POINT('Ctrl Pts',(-5.91620524671528,0.840054346904411,
26.5220688419204));
#51765=CARTESIAN_POINT('Ctrl Pts',(-5.91700643196177,-0.000128843304525861,
26.5616248077952));
#51766=CARTESIAN_POINT('Origin',(0.,0.,0.));
#51767=CARTESIAN_POINT('',(-5.91635914490505,0.000103511046959798,28.5633751922049));
#51768=CARTESIAN_POINT('',(-5.9162836429884,6.56326992744338E-5,28.3116248077952));
#51769=CARTESIAN_POINT('',(-5.91675,-7.2459289488551E-16,0.));
#51770=CARTESIAN_POINT('Ctrl Pts',(-5.91635914490505,0.000103511046959798,
28.5633751922049));
#51771=CARTESIAN_POINT('Ctrl Pts',(-5.91659096314501,0.372683485960868,
28.545839580604));
#51772=CARTESIAN_POINT('Ctrl Pts',(-5.88194934158775,0.745220890230166,
28.5283039690031));
#51773=CARTESIAN_POINT('Ctrl Pts',(-5.8120251919434,1.11101376516929,28.5107683574022));
#51774=CARTESIAN_POINT('Ctrl Pts',(-5.62703809473853,2.07873325060279,28.4643772049282));
#51775=CARTESIAN_POINT('Ctrl Pts',(-5.1951128511199,2.9992485910523,28.4179860524542));
#51776=CARTESIAN_POINT('Ctrl Pts',(-4.56905989073968,3.76001065597083,28.3715948999802));
#51777=CARTESIAN_POINT('Ctrl Pts',(-3.94300693035947,4.52077272088937,28.3252037475062));
#51778=CARTESIAN_POINT('Ctrl Pts',(-3.12282625321767,5.12178151027694,28.2788125950323));
#51779=CARTESIAN_POINT('Ctrl Pts',(-2.20879931910905,5.48955316816257,28.2324214425583));
#51780=CARTESIAN_POINT('Ctrl Pts',(-1.2947723850004,5.85732482604821,28.1860302900843));
#51781=CARTESIAN_POINT('Ctrl Pts',(-0.286899193924923,5.99185935243189,
28.1396391376103));
#51782=CARTESIAN_POINT('Ctrl Pts',(0.691590095561016,5.87670754401665,28.0932479851363));
#51783=CARTESIAN_POINT('Ctrl Pts',(1.6700793850469,5.76155573560141,28.0468568326623));
#51784=CARTESIAN_POINT('Ctrl Pts',(2.61918477294326,5.39671759238728,28.0004656801884));
#51785=CARTESIAN_POINT('Ctrl Pts',(3.42286149441974,4.8268009704357,27.9540745277144));
#51786=CARTESIAN_POINT('Ctrl Pts',(4.22653821589624,4.2568843484841,27.9076833752404));
#51787=CARTESIAN_POINT('Ctrl Pts',(4.88478627095287,3.48188924779502,27.8612922227664));
#51788=CARTESIAN_POINT('Ctrl Pts',(5.31712330038777,2.5965723996557,27.8149010702924));
#51789=CARTESIAN_POINT('Ctrl Pts',(5.74946032982268,1.71125555151635,27.7685099178184));
#51790=CARTESIAN_POINT('Ctrl Pts',(5.95588633363586,0.715616955926808,27.7221187653445));
#51791=CARTESIAN_POINT('Ctrl Pts',(5.91116211566127,-0.268609122241495,
27.6757276128705));
#51792=CARTESIAN_POINT('Ctrl Pts',(5.86643789768668,-1.25283520040977,27.6293364603965));
#51793=CARTESIAN_POINT('Ctrl Pts',(5.57056345792431,-2.22564876115675,27.5829453079225));
#51794=CARTESIAN_POINT('Ctrl Pts',(5.05971463123867,-3.0681063000831,27.5365541554485));
#51795=CARTESIAN_POINT('Ctrl Pts',(4.54886580455303,-3.91056383900945,27.4901630029745));
#51796=CARTESIAN_POINT('Ctrl Pts',(3.8230425909441,-4.6226653561152,27.4437718505005));
#51797=CARTESIAN_POINT('Ctrl Pts',(2.97098959686529,-5.11734396278954,27.3973806980266));
#51798=CARTESIAN_POINT('Ctrl Pts',(2.11893660278645,-5.61202256946389,27.3509895455526));
#51799=CARTESIAN_POINT('Ctrl Pts',(1.1406538282377,-5.88927826570684,27.3045983930786));
#51800=CARTESIAN_POINT('Ctrl Pts',(0.155753484842588,-5.91521168430511,
27.2582072406046));
#51801=CARTESIAN_POINT('Ctrl Pts',(-0.829146858552467,-5.94114510290338,
27.2118160881306));
#51802=CARTESIAN_POINT('Ctrl Pts',(-1.8206647707939,-5.71575624385699,27.1654249356566));
#51803=CARTESIAN_POINT('Ctrl Pts',(-2.69756981275611,-5.26660284467011,
27.1190337831827));
#51804=CARTESIAN_POINT('Ctrl Pts',(-3.57447485471833,-4.81744944548322,
27.0726426307087));
#51805=CARTESIAN_POINT('Ctrl Pts',(-4.33676702640134,-4.14453150615582,
27.0262514782347));
#51806=CARTESIAN_POINT('Ctrl Pts',(-4.89124275218217,-3.33012503630204,
26.9798603257607));
#51807=CARTESIAN_POINT('Ctrl Pts',(-5.44571847796304,-2.51571856644821,
26.9334691732867));
#51808=CARTESIAN_POINT('Ctrl Pts',(-5.79237775784171,-1.55982356606796,
26.8870780208127));
#51809=CARTESIAN_POINT('Ctrl Pts',(-5.88883542034745,-0.579314949092088,
26.8406868683387));
#51810=CARTESIAN_POINT('Ctrl Pts',(-5.90776446391498,-0.386897987630189,
26.8315829762941));
#51811=CARTESIAN_POINT('Ctrl Pts',(-5.91705801342714,-0.193533133189506,
26.8224790842495));
#51812=CARTESIAN_POINT('Ctrl Pts',(-5.91685813319025,-0.000149150696060474,
26.8133751922049));
#51813=CARTESIAN_POINT('Ctrl Pts',(-5.91700643196177,-0.000128843304525861,
26.5616248077952));
#51814=CARTESIAN_POINT('Ctrl Pts',(-5.91714487506483,-0.145310707926279,
26.5684599943944));
#51815=CARTESIAN_POINT('Ctrl Pts',(-5.91191008600676,-0.290482609897553,
26.5752951809936));
#51816=CARTESIAN_POINT('Ctrl Pts',(-5.90123235330366,-0.435253060487541,
26.5821303675929));
#51817=CARTESIAN_POINT('Ctrl Pts',(-5.82876142383966,-1.41782580368188,
26.6285215200669));
#51818=CARTESIAN_POINT('Ctrl Pts',(-5.50556216289807,-2.38190575298281,
26.6749126725408));
#51819=CARTESIAN_POINT('Ctrl Pts',(-4.97115134354497,-3.20961724102932,
26.7213038250148));
#51820=CARTESIAN_POINT('Ctrl Pts',(-4.43674052419186,-4.03732872907586,
26.7676949774888));
#51821=CARTESIAN_POINT('Ctrl Pts',(-3.69111814642719,-4.72867175586796,
26.8140861299628));
#51822=CARTESIAN_POINT('Ctrl Pts',(-2.82544961146294,-5.19911752198635,
26.8604772824368));
#51823=CARTESIAN_POINT('Ctrl Pts',(-1.95978107649869,-5.66956328810475,
26.9068684349107));
#51824=CARTESIAN_POINT('Ctrl Pts',(-0.974066384334856,-5.91911179354946,
26.9532595873847));
#51825=CARTESIAN_POINT('Ctrl Pts',(0.0111735712472701,-5.91725136069503,
26.9996507398587));
#51826=CARTESIAN_POINT('Ctrl Pts',(0.996413526829369,-5.9153909278406,27.0460418923327));
#51827=CARTESIAN_POINT('Ctrl Pts',(1.98117874582977,-5.66212155668702,27.0924330448067));
#51828=CARTESIAN_POINT('Ctrl Pts',(2.84506442419887,-5.18840986589336,27.1388241972807));
#51829=CARTESIAN_POINT('Ctrl Pts',(3.70895010256799,-4.7146981750997,27.1852153497547));
#51830=CARTESIAN_POINT('Ctrl Pts',(4.45195624030583,-4.02054416466596,27.2316065022287));
#51831=CARTESIAN_POINT('Ctrl Pts',(4.98323731738814,-3.19082032601835,27.2779976547026));
#51832=CARTESIAN_POINT('Ctrl Pts',(5.51451839447044,-2.36109648737076,27.3243888071766));
#51833=CARTESIAN_POINT('Ctrl Pts',(5.83407441089722,-1.39580282050927,27.3707799596506));
#51834=CARTESIAN_POINT('Ctrl Pts',(5.90283404408481,-0.412963391034791,
27.4171711121246));
#51835=CARTESIAN_POINT('Ctrl Pts',(5.9715936772724,0.569876038439717,27.4635622645986));
#51836=CARTESIAN_POINT('Ctrl Pts',(5.78955692722082,1.57026123052724,27.5099534170725));
#51837=CARTESIAN_POINT('Ctrl Pts',(5.3789809764512,2.46587756575986,27.5563445695465));
#51838=CARTESIAN_POINT('Ctrl Pts',(4.96840502568157,3.36149390099247,27.6027357220205));
#51839=CARTESIAN_POINT('Ctrl Pts',(4.32928987419394,4.15234137937011,27.6491268744945));
#51840=CARTESIAN_POINT('Ctrl Pts',(3.5397785484632,4.74172503865222,27.6955180269685));
#51841=CARTESIAN_POINT('Ctrl Pts',(2.75026722273249,5.3311086979343,27.7419091794425));
#51842=CARTESIAN_POINT('Ctrl Pts',(1.81035972275864,5.71902853812085,27.7883003319165));
#51843=CARTESIAN_POINT('Ctrl Pts',(0.834976210399108,5.85805456123526,27.8346914843904));
#51844=CARTESIAN_POINT('Ctrl Pts',(-0.140407301960424,5.99708058434966,
27.8810826368644));
#51845=CARTESIAN_POINT('Ctrl Pts',(-1.15126682670565,5.88721279039195,27.9274737893384));
#51846=CARTESIAN_POINT('Ctrl Pts',(-2.07400707365966,5.54188444238522,27.9738649418124));
#51847=CARTESIAN_POINT('Ctrl Pts',(-2.99674732061373,5.19655609437846,28.0202560942864));
#51848=CARTESIAN_POINT('Ctrl Pts',(-3.83136828977652,4.61576719232268,28.0666472467603));
#51849=CARTESIAN_POINT('Ctrl Pts',(-4.47582294261673,3.87052935664972,28.1130383992343));
#51850=CARTESIAN_POINT('Ctrl Pts',(-5.12027759545691,3.12529152097679,28.1594295517083));
#51851=CARTESIAN_POINT('Ctrl Pts',(-5.57456593197452,2.21560475168666,28.2058207041823));
#51852=CARTESIAN_POINT('Ctrl Pts',(-5.78314324254227,1.25269419675327,28.2522118566563));
#51853=CARTESIAN_POINT('Ctrl Pts',(-5.87218459993183,0.841629049625724,
28.2720161737026));
#51854=CARTESIAN_POINT('Ctrl Pts',(-5.9164469911479,0.420864272260875,28.2918204907489));
#51855=CARTESIAN_POINT('Ctrl Pts',(-5.9162836429884,6.56326992744338E-5,
28.3116248077952));
#51856=CARTESIAN_POINT('Origin',(0.,0.,0.));
#51857=CARTESIAN_POINT('',(-5.91722862746563,-4.93335032009101E-5,30.3133751922049));
#51858=CARTESIAN_POINT('',(-5.91726189923285,1.1977277558789E-6,30.0616248077952));
#51859=CARTESIAN_POINT('',(-5.91675,-7.2459289488551E-16,0.));
#51860=CARTESIAN_POINT('Ctrl Pts',(-5.91722862746563,-4.93335032009101E-5,
30.3133751922049));
#51861=CARTESIAN_POINT('Ctrl Pts',(-5.91681565401081,0.938144190620326,
30.2692000769585));
#51862=CARTESIAN_POINT('Ctrl Pts',(-5.68970999499436,1.87653053611386,30.225024961712));
#51863=CARTESIAN_POINT('Ctrl Pts',(-5.25996281841822,2.7104943399753,30.1808498464656));
#51864=CARTESIAN_POINT('Ctrl Pts',(-4.80865744699841,3.5862937978123,30.1344586939916));
#51865=CARTESIAN_POINT('Ctrl Pts',(-4.13386965324051,4.34693125512901,30.0880675415176));
#51866=CARTESIAN_POINT('Ctrl Pts',(-3.31810406922818,4.89940545412927,30.0416763890437));
#51867=CARTESIAN_POINT('Ctrl Pts',(-2.50233848521586,5.45187965312954,29.9952852365697));
#51868=CARTESIAN_POINT('Ctrl Pts',(-1.54559511094913,5.79619059381336,29.9488940840957));
#51869=CARTESIAN_POINT('Ctrl Pts',(-0.564852588932413,5.89024023032649,
29.9025029316217));
#51870=CARTESIAN_POINT('Ctrl Pts',(0.4158899330843,5.98428986683962,29.8561117791477));
#51871=CARTESIAN_POINT('Ctrl Pts',(1.42063160285098,5.82807819918207,29.8097206266737));
#51872=CARTESIAN_POINT('Ctrl Pts',(2.32652514516487,5.44070484101977,29.7633294741997));
#51873=CARTESIAN_POINT('Ctrl Pts',(3.23241868747876,5.05333148285746,29.7169383217258));
#51874=CARTESIAN_POINT('Ctrl Pts',(4.03946410233985,4.43479643419041,29.6705471692518));
#51875=CARTESIAN_POINT('Ctrl Pts',(4.64898594593624,3.66072644329887,29.6241560167778));
#51876=CARTESIAN_POINT('Ctrl Pts',(5.25850778953263,2.88665645240734,29.5777648643038));
#51877=CARTESIAN_POINT('Ctrl Pts',(5.6705060618643,1.95705151929134,29.5313737118298));
#51878=CARTESIAN_POINT('Ctrl Pts',(5.83460675469892,0.985572136478123,29.4849825593558));
#51879=CARTESIAN_POINT('Ctrl Pts',(5.99870744753355,0.0140927536648758,
29.4385914068819));
#51880=CARTESIAN_POINT('Ctrl Pts',(5.91491056087111,-0.999261078845656,
29.3922002544079));
#51881=CARTESIAN_POINT('Ctrl Pts',(5.59346173247772,-1.93058909804433,29.3458091019339));
#51882=CARTESIAN_POINT('Ctrl Pts',(5.27201290408436,-2.86191711724293,29.2994179494599));
#51883=CARTESIAN_POINT('Ctrl Pts',(4.71291213396012,-3.71121932312976,29.2530267969859));
#51884=CARTESIAN_POINT('Ctrl Pts',(3.98451928836737,-4.37465363872486,29.2066356445119));
#51885=CARTESIAN_POINT('Ctrl Pts',(3.25612644277459,-5.03808795432001,29.160244492038));
#51886=CARTESIAN_POINT('Ctrl Pts',(2.3584415217133,-5.51565437962341,29.113853339564));
#51887=CARTESIAN_POINT('Ctrl Pts',(1.40122223690316,-5.74896205075215,29.06746218709));
#51888=CARTESIAN_POINT('Ctrl Pts',(0.444002952092992,-5.9822697218809,29.021071034616));
#51889=CARTESIAN_POINT('Ctrl Pts',(-0.572750696465934,-5.97131863883498,
28.974679882142));
#51890=CARTESIAN_POINT('Ctrl Pts',(-1.52472275867795,-5.71744776341243,
28.928288729668));
#51891=CARTESIAN_POINT('Ctrl Pts',(-2.4766948208899,-5.46357688798989,28.8818975771941));
#51892=CARTESIAN_POINT('Ctrl Pts',(-3.36388529675494,-4.96678622019069,
28.8355064247201));
#51893=CARTESIAN_POINT('Ctrl Pts',(-4.0778196043725,-4.28781712440906,28.7891152722461));
#51894=CARTESIAN_POINT('Ctrl Pts',(-4.79175391199009,-3.60884802862741,
28.7427241197721));
#51895=CARTESIAN_POINT('Ctrl Pts',(-5.33243205136026,-2.74770050486329,
28.6963329672981));
#51896=CARTESIAN_POINT('Ctrl Pts',(-5.63374664564981,-1.80966492777249,
28.6499418148241));
#51897=CARTESIAN_POINT('Ctrl Pts',(-5.82116590832173,-1.22620186441537,
28.6210862739511));
#51898=CARTESIAN_POINT('Ctrl Pts',(-5.91597767884327,-0.612991540285919,
28.592230733078));
#51899=CARTESIAN_POINT('Ctrl Pts',(-5.91635914490505,0.000103511046959798,
28.5633751922049));
#51900=CARTESIAN_POINT('Ctrl Pts',(-5.9162836429884,6.56326992744338E-5,
28.3116248077952));
#51901=CARTESIAN_POINT('Ctrl Pts',(-5.9160643518801,-0.564846762515274,
28.3382116432229));
#51902=CARTESIAN_POINT('Ctrl Pts',(-5.83577904487672,-1.1298201856659,28.3647984786505));
#51903=CARTESIAN_POINT('Ctrl Pts',(-5.67628234379502,-1.67146859613411,
28.3913853140782));
#51904=CARTESIAN_POINT('Ctrl Pts',(-5.3979778498621,-2.61658649351127,28.4377764665522));
#51905=CARTESIAN_POINT('Ctrl Pts',(-4.87850257737835,-3.49068794768887,
28.4841676190262));
#51906=CARTESIAN_POINT('Ctrl Pts',(-4.18137148116261,-4.18689873902649,
28.5305587715002));
#51907=CARTESIAN_POINT('Ctrl Pts',(-3.48424038494692,-4.88310953036406,
28.5769499239742));
#51908=CARTESIAN_POINT('Ctrl Pts',(-2.60945346499925,-5.4014296588617,28.6233410764482));
#51909=CARTESIAN_POINT('Ctrl Pts',(-1.6639687511618,-5.67848540629442,28.6697322289221));
#51910=CARTESIAN_POINT('Ctrl Pts',(-0.718484037324299,-5.95554115372715,
28.7161233813961));
#51911=CARTESIAN_POINT('Ctrl Pts',(0.297698470402942,-5.99133252009495,
28.7625145338701));
#51912=CARTESIAN_POINT('Ctrl Pts',(1.26033265389896,-5.78148338368776,28.8089056863441));
#51913=CARTESIAN_POINT('Ctrl Pts',(2.22296683739498,-5.57163424728057,28.8552968388181));
#51914=CARTESIAN_POINT('Ctrl Pts',(3.13205269665974,-5.11614460809836,28.9016879912921));
#51915=CARTESIAN_POINT('Ctrl Pts',(3.87643855549968,-4.47070605606958,28.9480791437661));
#51916=CARTESIAN_POINT('Ctrl Pts',(4.62082441433958,-3.82526750404082,28.99447029624));
#51917=CARTESIAN_POINT('Ctrl Pts',(5.20051027275471,-2.98988003916548,29.040861448714));
#51918=CARTESIAN_POINT('Ctrl Pts',(5.54461937672687,-2.06668441750707,29.087252601188));
#51919=CARTESIAN_POINT('Ctrl Pts',(5.88872848069905,-1.14348879584861,29.133643753662));
#51920=CARTESIAN_POINT('Ctrl Pts',(5.99726083022826,-0.132485017407117,
29.180034906136));
#51921=CARTESIAN_POINT('Ctrl Pts',(5.85694644377375,0.842713990098421,29.22642605861));
#51922=CARTESIAN_POINT('Ctrl Pts',(5.71663205731926,1.8179129976039,29.2728172110839));
#51923=CARTESIAN_POINT('Ctrl Pts',(5.32747093488102,2.75730723417347,29.3192083635579));
#51924=CARTESIAN_POINT('Ctrl Pts',(4.73704484294192,3.54603929339467,29.3655995160319));
#51925=CARTESIAN_POINT('Ctrl Pts',(4.1466187510028,4.33477135261589,29.4119906685059));
#51926=CARTESIAN_POINT('Ctrl Pts',(3.35492768956284,4.97284123448879,29.4583818209799));
#51927=CARTESIAN_POINT('Ctrl Pts',(2.45876976367401,5.38223371506516,29.5047729734539));
#51928=CARTESIAN_POINT('Ctrl Pts',(1.56261183778516,5.79162619564153,29.5511641259278));
#51929=CARTESIAN_POINT('Ctrl Pts',(0.561987047447457,5.97234127492132,29.5975552784018));
#51930=CARTESIAN_POINT('Ctrl Pts',(-0.420760692786501,5.90228336779483,
29.6439464308758));
#51931=CARTESIAN_POINT('Ctrl Pts',(-1.40350843302046,5.83222546066834,29.6903375833498));
#51932=CARTESIAN_POINT('Ctrl Pts',(-2.36837912315064,5.51139456713559,29.7367287358238));
#51933=CARTESIAN_POINT('Ctrl Pts',(-3.19740041389354,4.97901788584606,29.7831198882978));
#51934=CARTESIAN_POINT('Ctrl Pts',(-4.02642170463643,4.44664120455655,29.8295110407718));
#51935=CARTESIAN_POINT('Ctrl Pts',(-4.71959359599201,3.70271873551026,29.8759021932458));
#51936=CARTESIAN_POINT('Ctrl Pts',(-5.19216367780099,2.83820803629081,29.9222933457197));
#51937=CARTESIAN_POINT('Ctrl Pts',(-5.66527027191213,1.97271585169314,29.9687371664116));
#51938=CARTESIAN_POINT('Ctrl Pts',(-5.91727379117156,0.986361472032727,
30.0151809871034));
#51939=CARTESIAN_POINT('Ctrl Pts',(-5.91726188962992,1.19770528722231E-6,
30.0616248077952));
#51940=CARTESIAN_POINT('Origin',(0.,0.,0.));
#51941=CARTESIAN_POINT('',(-5.91624577020395,-2.44117356945628E-5,32.0633751922049));
#51942=CARTESIAN_POINT('',(-5.91628636364003,-6.75382191168991E-5,31.8116248077952));
#51943=CARTESIAN_POINT('',(-5.91675,-7.2459289488551E-16,0.));
#51944=CARTESIAN_POINT('Ctrl Pts',(-5.91624577020395,-2.44117356945628E-5,
32.0633751922049));
#51945=CARTESIAN_POINT('Ctrl Pts',(-5.91617142152926,0.518930599746724,
32.038951725787));
#51946=CARTESIAN_POINT('Ctrl Pts',(-5.84857166224644,1.03790461430612,32.014528259369));
#51947=CARTESIAN_POINT('Ctrl Pts',(-5.71368641895957,1.53875791597551,31.990104792951));
#51948=CARTESIAN_POINT('Ctrl Pts',(-5.4574786480919,2.49010370314597,31.943713640477));
#51949=CARTESIAN_POINT('Ctrl Pts',(-4.95851089479277,3.37607158588524,31.897322488003));
#51950=CARTESIAN_POINT('Ctrl Pts',(-4.27779071030773,4.08833646572602,31.850931335529));
#51951=CARTESIAN_POINT('Ctrl Pts',(-3.59707052582268,4.80060134556683,31.804540183055));
#51952=CARTESIAN_POINT('Ctrl Pts',(-2.73459791015171,5.33916322250914,31.7581490305811));
#51953=CARTESIAN_POINT('Ctrl Pts',(-1.79582525365581,5.63817346988476,31.7117578781071));
#51954=CARTESIAN_POINT('Ctrl Pts',(-0.857052597159934,5.93718371726037,
31.6653667256331));
#51955=CARTESIAN_POINT('Ctrl Pts',(0.158020100160874,5.9966423350693,31.6189755731591));
#51956=CARTESIAN_POINT('Ctrl Pts',(1.12528241395491,5.80927946539191,31.5725844206851));
#51957=CARTESIAN_POINT('Ctrl Pts',(2.09254472774896,5.62191659571452,31.5261932682111));
#51958=CARTESIAN_POINT('Ctrl Pts',(3.01199665801623,5.1877322385508,31.4798021157372));
#51959=CARTESIAN_POINT('Ctrl Pts',(3.77121909473866,4.55981303977025,31.4334109632632));
#51960=CARTESIAN_POINT('Ctrl Pts',(4.53044153146111,3.93189384098969,31.3870198107892));
#51961=CARTESIAN_POINT('Ctrl Pts',(5.12943447463871,3.11023980059227,31.3406286583152));
#51962=CARTESIAN_POINT('Ctrl Pts',(5.49496054082328,2.1953125228485,31.2942375058412));
#51963=CARTESIAN_POINT('Ctrl Pts',(5.86048660700783,1.28038524510478,31.2478463533672));
#51964=CARTESIAN_POINT('Ctrl Pts',(5.99254579619939,0.272184730014703,31.2014552008933));
#51965=CARTESIAN_POINT('Ctrl Pts',(5.87499155844803,-0.706018842768892,
31.1550640484193));
#51966=CARTESIAN_POINT('Ctrl Pts',(5.75743732069666,-1.68422241555252,31.1086728959453));
#51967=CARTESIAN_POINT('Ctrl Pts',(5.39026965600235,-2.63242904602966,31.0622817434713));
#51968=CARTESIAN_POINT('Ctrl Pts',(4.81838124524767,-3.43470385821338,31.0158905909973));
#51969=CARTESIAN_POINT('Ctrl Pts',(4.246492834493,-4.23697867039708,30.9694994385233));
#51970=CARTESIAN_POINT('Ctrl Pts',(3.46988367767797,-4.89332166428738,30.9231082860494));
#51971=CARTESIAN_POINT('Ctrl Pts',(2.58350785273426,-5.32348340779237,30.8767171335754));
#51972=CARTESIAN_POINT('Ctrl Pts',(1.6971320277905,-5.75364515129739,30.8303259811014));
#51973=CARTESIAN_POINT('Ctrl Pts',(0.700989534718055,-5.95762564441709,
30.7839348286274));
#51974=CARTESIAN_POINT('Ctrl Pts',(-0.283123751314443,-5.91048469752033,
30.7375436761534));
#51975=CARTESIAN_POINT('Ctrl Pts',(-1.26723703734694,-5.86334375062357,
30.6911525236794));
#51976=CARTESIAN_POINT('Ctrl Pts',(-2.23932111633949,-5.56508136371036,
30.6447613712054));
#51977=CARTESIAN_POINT('Ctrl Pts',(-3.08052167581995,-5.05216534002835,
30.5983702187315));
#51978=CARTESIAN_POINT('Ctrl Pts',(-3.92172223530036,-4.53924931634636,
30.5519790662575));
#51979=CARTESIAN_POINT('Ctrl Pts',(-4.6320392752687,-3.8116796558956,30.5055879137835));
#51980=CARTESIAN_POINT('Ctrl Pts',(-5.1246240907136,-2.95841449885882,30.4591967613095));
#51981=CARTESIAN_POINT('Ctrl Pts',(-5.61720890615852,-2.10514934182202,
30.4128056088355));
#51982=CARTESIAN_POINT('Ctrl Pts',(-5.89206149707999,-1.12618868819918,
30.3664144563616));
#51983=CARTESIAN_POINT('Ctrl Pts',(-5.91557631799987,-0.141227632209123,
30.3200233038876));
#51984=CARTESIAN_POINT('Ctrl Pts',(-5.91669958646333,-0.0941774889952961,
30.31780726666));
#51985=CARTESIAN_POINT('Ctrl Pts',(-5.91724934420955,-0.047113653867736,
30.3155912294325));
#51986=CARTESIAN_POINT('Ctrl Pts',(-5.91722862746563,-4.93335032009101E-5,
30.3133751922049));
#51987=CARTESIAN_POINT('Ctrl Pts',(-5.91726188962992,1.19770528722231E-6,
30.0616248077952));
#51988=CARTESIAN_POINT('Ctrl Pts',(-5.91725001508146,-0.984121972222739,
30.1079632920513));
#51989=CARTESIAN_POINT('Ctrl Pts',(-5.66643406602473,-1.96825097069318,
30.1543017763075));
#51990=CARTESIAN_POINT('Ctrl Pts',(-5.19538055793008,-2.83231519655277,
30.2006402605636));
#51991=CARTESIAN_POINT('Ctrl Pts',(-4.72379165146888,-3.69736151588404,
30.2470314130376));
#51992=CARTESIAN_POINT('Ctrl Pts',(-4.03146425841823,-4.44206997679278,
30.2934225655116));
#51993=CARTESIAN_POINT('Ctrl Pts',(-3.20304753422148,-4.97538692041728,
30.3398137179856));
#51994=CARTESIAN_POINT('Ctrl Pts',(-2.3746308100247,-5.50870386404179,30.3862048704596));
#51995=CARTESIAN_POINT('Ctrl Pts',(-1.41012475468182,-5.83062929038205,
30.4325960229335));
#51996=CARTESIAN_POINT('Ctrl Pts',(-0.427457134484195,-5.90180217497335,
30.4789871754075));
#51997=CARTESIAN_POINT('Ctrl Pts',(0.555210485713345,-5.97297505956465,
30.5253783278815));
#51998=CARTESIAN_POINT('Ctrl Pts',(1.55603967076562,-5.79339540240703,30.5717694803555));
#51999=CARTESIAN_POINT('Ctrl Pts',(2.45266151528465,-5.38501996335977,30.6181606328295));
#52000=CARTESIAN_POINT('Ctrl Pts',(3.34928335980375,-4.97664452431247,30.6645517853035));
#52001=CARTESIAN_POINT('Ctrl Pts',(4.14169786378957,-4.33947330337547,30.7109429377774));
#52002=CARTESIAN_POINT('Ctrl Pts',(4.73301846866193,-3.55141164745045,30.7573340902514));
#52003=CARTESIAN_POINT('Ctrl Pts',(5.32433907353427,-2.76334999152544,30.8037252427254));
#52004=CARTESIAN_POINT('Ctrl Pts',(5.71456577929316,-1.82439790061242,30.8501163951994));
#52005=CARTESIAN_POINT('Ctrl Pts',(5.85598653322264,-0.849358721069426,
30.8965075476734));
#52006=CARTESIAN_POINT('Ctrl Pts',(5.99740728715212,0.125680458473537,30.9428987001474));
#52007=CARTESIAN_POINT('Ctrl Pts',(5.89002208925218,1.13680672664654,30.9892898526213));
#52008=CARTESIAN_POINT('Ctrl Pts',(5.54696066167538,2.06039217921429,31.0356810050953));
#52009=CARTESIAN_POINT('Ctrl Pts',(5.20389923409858,2.98397763178207,31.0820721575693));
#52010=CARTESIAN_POINT('Ctrl Pts',(4.62516157684496,3.82002226874459,31.1284633100433));
#52011=CARTESIAN_POINT('Ctrl Pts',(3.8815085097253,4.46630498323522,31.1748544625173));
#52012=CARTESIAN_POINT('Ctrl Pts',(3.13785544260559,5.11258769772589,31.2212456149913));
#52013=CARTESIAN_POINT('Ctrl Pts',(2.2292869656198,5.56910848974459,31.2676367674653));
#52014=CARTESIAN_POINT('Ctrl Pts',(1.26689149591189,5.78004969285972,31.3140279199392));
#52015=CARTESIAN_POINT('Ctrl Pts',(0.304496026204034,5.99099089597484,31.3604190724132));
#52016=CARTESIAN_POINT('Ctrl Pts',(-0.711726436225908,5.95635251018647,
31.4068102248872));
#52017=CARTESIAN_POINT('Ctrl Pts',(-1.6575248880945,5.68036968512516,31.4532013773612));
#52018=CARTESIAN_POINT('Ctrl Pts',(-2.6033233399631,5.40438686006385,31.4995925298352));
#52019=CARTESIAN_POINT('Ctrl Pts',(-3.47869778127026,4.88705959572961,31.5459836823092));
#52020=CARTESIAN_POINT('Ctrl Pts',(-4.17661834739248,4.19164021530547,31.5923748347831));
#52021=CARTESIAN_POINT('Ctrl Pts',(-4.87453891351471,3.49622083488134,31.6387659872571));
#52022=CARTESIAN_POINT('Ctrl Pts',(-5.39500560445199,2.62270933836731,31.6851571397311));
#52023=CARTESIAN_POINT('Ctrl Pts',(-5.67438224710694,1.67790781274158,31.7315482922051));
#52024=CARTESIAN_POINT('Ctrl Pts',(-5.83512775487457,1.13429543508152,31.7582404640685));
#52025=CARTESIAN_POINT('Ctrl Pts',(-5.9160596836837,0.567082280831977,31.7849326359318));
#52026=CARTESIAN_POINT('Ctrl Pts',(-5.91628636364003,-6.75382191168991E-5,
31.8116248077952));
#52027=CARTESIAN_POINT('Origin',(0.,0.,0.));
#52028=CARTESIAN_POINT('',(-5.91712951644955,9.70841563171718E-5,33.8133751922049));
#52029=CARTESIAN_POINT('',(-5.91699986415359,0.000130094215637797,33.5616248077952));
#52030=CARTESIAN_POINT('',(-5.91675,-7.2459289488551E-16,0.));
#52031=CARTESIAN_POINT('Ctrl Pts',(-5.91712951644955,9.70841563171718E-5,
33.8133751922049));
#52032=CARTESIAN_POINT('Ctrl Pts',(-5.91720654989048,0.0993222265836009,
33.8087033746154));
#52033=CARTESIAN_POINT('Ctrl Pts',(-5.91476231278835,0.198543573571387,
33.8040315570259));
#52034=CARTESIAN_POINT('Ctrl Pts',(-5.90977163932508,0.297636673159239,
33.7993597394364));
#52035=CARTESIAN_POINT('Ctrl Pts',(-5.86021424776472,1.28163123288083,33.7529685869624));
#52036=CARTESIAN_POINT('Ctrl Pts',(-5.55956571221439,2.2529799684796,33.7065774344884));
#52037=CARTESIAN_POINT('Ctrl Pts',(-5.04458558440507,3.09291847609872,33.6601862820144));
#52038=CARTESIAN_POINT('Ctrl Pts',(-4.52960545659575,3.93285698371785,33.6137951295404));
#52039=CARTESIAN_POINT('Ctrl Pts',(-3.80029373652743,4.64138526335733,33.5674039770665));
#52040=CARTESIAN_POINT('Ctrl Pts',(-2.94582156169723,5.13187331730042,33.5210128245925));
#52041=CARTESIAN_POINT('Ctrl Pts',(-2.09134938686702,5.62236137124351,33.4746216721185));
#52042=CARTESIAN_POINT('Ctrl Pts',(-1.11171675727491,5.89480919949021,33.4282305196445));
#52043=CARTESIAN_POINT('Ctrl Pts',(-0.126700927976976,5.915905280938,33.3818393671705));
#52044=CARTESIAN_POINT('Ctrl Pts',(0.858314901320957,5.93700136238578,33.3354482146965));
#52045=CARTESIAN_POINT('Ctrl Pts',(1.84871393032473,5.70674569703466,33.2890570622226));
#52046=CARTESIAN_POINT('Ctrl Pts',(2.72340252299071,5.25329107474049,33.2426659097486));
#52047=CARTESIAN_POINT('Ctrl Pts',(3.5980911156567,4.79983645244633,33.1962747572746));
#52048=CARTESIAN_POINT('Ctrl Pts',(4.35706927198491,4.12318287320913,33.1498836048006));
#52049=CARTESIAN_POINT('Ctrl Pts',(4.90753861280094,3.30606309408155,33.1034924523266));
#52050=CARTESIAN_POINT('Ctrl Pts',(5.45800795361698,2.48894331495397,33.0571012998526));
#52051=CARTESIAN_POINT('Ctrl Pts',(5.79996847892084,1.53135733593599,33.0107101473786));
#52052=CARTESIAN_POINT('Ctrl Pts',(5.89160952232476,0.550386822727887,32.9643189949047));
#52053=CARTESIAN_POINT('Ctrl Pts',(5.98325056572869,-0.430583690480249,
32.9179278424307));
#52054=CARTESIAN_POINT('Ctrl Pts',(5.8245721272327,-1.43493873787846,32.8715366899567));
#52055=CARTESIAN_POINT('Ctrl Pts',(5.43497542646289,-2.33987831562345,32.8251455374827));
#52056=CARTESIAN_POINT('Ctrl Pts',(5.04537872569309,-3.24481789336841,32.7787543850087));
#52057=CARTESIAN_POINT('Ctrl Pts',(4.42486376264948,-4.05034200146009,32.7323632325347));
#52058=CARTESIAN_POINT('Ctrl Pts',(3.6492993648389,-4.65796120249694,32.6859720800608));
#52059=CARTESIAN_POINT('Ctrl Pts',(2.87373496702833,-5.26558040353378,32.6395809275868));
#52060=CARTESIAN_POINT('Ctrl Pts',(1.94312113445076,-5.67529469751581,32.5931897751128));
#52061=CARTESIAN_POINT('Ctrl Pts',(0.971241715271586,-5.83700933258605,
32.5467986226388));
#52062=CARTESIAN_POINT('Ctrl Pts',(-0.000637703907585968,-5.99872396765628,
32.5004074701648));
#52063=CARTESIAN_POINT('Ctrl Pts',(-1.01378270968838,-5.91243894381474,
32.4540163176908));
#52064=CARTESIAN_POINT('Ctrl Pts',(-1.94431857178876,-5.58870411719726,
32.4076251652168));
#52065=CARTESIAN_POINT('Ctrl Pts',(-2.87485443388914,-5.26496929057979,
32.3612340127429));
#52066=CARTESIAN_POINT('Ctrl Pts',(-3.72278115230912,-4.70378466118638,
32.3148428602689));
#52067=CARTESIAN_POINT('Ctrl Pts',(-4.38442482751419,-3.97376488359055,
32.2684517077949));
#52068=CARTESIAN_POINT('Ctrl Pts',(-5.04606850271927,-3.24374510599472,
32.2220605553209));
#52069=CARTESIAN_POINT('Ctrl Pts',(-5.52142913470946,-2.34489018019647,
32.1756694028469));
#52070=CARTESIAN_POINT('Ctrl Pts',(-5.75238555648645,-1.38710087149652,
32.1292782503729));
#52071=CARTESIAN_POINT('Ctrl Pts',(-5.86175076721409,-0.93355717363047,
32.1073105643169));
#52072=CARTESIAN_POINT('Ctrl Pts',(-5.91631264311692,-0.466798479525038,
32.0853428782609));
#52073=CARTESIAN_POINT('Ctrl Pts',(-5.91624577020395,-2.44117356945628E-5,
32.0633751922049));
#52074=CARTESIAN_POINT('Ctrl Pts',(-5.91628636364003,-6.75382191168991E-5,
31.8116248077952));
#52075=CARTESIAN_POINT('Ctrl Pts',(-5.91645365478769,-0.418627457059442,
31.8313237884058));
#52076=CARTESIAN_POINT('Ctrl Pts',(-5.87266461226124,-0.837152880211372,
31.8510227690164));
#52077=CARTESIAN_POINT('Ctrl Pts',(-5.78456082316728,-1.2461318539464,31.870721749627));
#52078=CARTESIAN_POINT('Ctrl Pts',(-5.57707616220006,-2.20927844027123,
31.917112902101));
#52079=CARTESIAN_POINT('Ctrl Pts',(-5.12382024589301,-3.11948005818347,
31.963504054575));
#52080=CARTESIAN_POINT('Ctrl Pts',(-4.48021155241156,-3.86544861044351,
32.009895207049));
#52081=CARTESIAN_POINT('Ctrl Pts',(-3.83660285893011,-4.61141716270354,
32.056286359523));
#52082=CARTESIAN_POINT('Ctrl Pts',(-3.00264138827423,-5.1931526493114,32.102677511997));
#52083=CARTESIAN_POINT('Ctrl Pts',(-2.08029354372645,-5.53952771328672,
32.1490686644709));
#52084=CARTESIAN_POINT('Ctrl Pts',(-1.15794569917867,-5.88590277726204,
32.1954598169449));
#52085=CARTESIAN_POINT('Ctrl Pts',(-0.147211480738965,-5.99691741860484,
32.2418509694189));
#52086=CARTESIAN_POINT('Ctrl Pts',(0.828329142307269,-5.85899815210298,
32.2882421218929));
#52087=CARTESIAN_POINT('Ctrl Pts',(1.8038697653535,-5.72107888560113,32.3346332743669));
#52088=CARTESIAN_POINT('Ctrl Pts',(2.74421679300629,-5.33422571125461,32.3810244268409));
#52089=CARTESIAN_POINT('Ctrl Pts',(3.53439632344765,-4.74573820844991,32.4274155793149));
#52090=CARTESIAN_POINT('Ctrl Pts',(4.32457585388903,-4.15725070564519,32.4738067317888));
#52091=CARTESIAN_POINT('Ctrl Pts',(4.96458788711896,-3.36712887438234,32.5201978842628));
#52092=CARTESIAN_POINT('Ctrl Pts',(5.37617973715353,-2.47197895382655,32.5665890367368));
#52093=CARTESIAN_POINT('Ctrl Pts',(5.78777158718809,-1.57682903327079,32.6129801892108));
#52094=CARTESIAN_POINT('Ctrl Pts',(5.97094325402726,-0.576651023422171,
32.6593713416848));
#52095=CARTESIAN_POINT('Ctrl Pts',(5.90329879168547,0.406265787910474,32.7057624941588));
#52096=CARTESIAN_POINT('Ctrl Pts',(5.83565432934368,1.38918259924312,32.7521536466327));
#52097=CARTESIAN_POINT('Ctrl Pts',(5.51719373782093,2.3548382120598,32.7985447991067));
#52098=CARTESIAN_POINT('Ctrl Pts',(4.98685440481123,3.18516430652431,32.8449359515807));
#52099=CARTESIAN_POINT('Ctrl Pts',(4.45651507180153,4.01549040098881,32.8913271040547));
#52100=CARTESIAN_POINT('Ctrl Pts',(3.71429699730487,4.71048697710115,32.9377182565287));
#52101=CARTESIAN_POINT('Ctrl Pts',(2.8509493468051,5.18517852501659,32.9841094090027));
#52102=CARTESIAN_POINT('Ctrl Pts',(1.98760169630535,5.65987007293202,33.0305005614767));
#52103=CARTESIAN_POINT('Ctrl Pts',(1.00312446980238,5.9142565926506,33.0768917139506));
#52104=CARTESIAN_POINT('Ctrl Pts',(0.0178872592165909,5.91723487452538,
33.1232828664246));
#52105=CARTESIAN_POINT('Ctrl Pts',(-0.967349951369257,5.92021315640015,
33.1696740188986));
#52106=CARTESIAN_POINT('Ctrl Pts',(-1.95334714603794,5.67178320043115,33.2160651713726));
#52107=CARTESIAN_POINT('Ctrl Pts',(-2.81954889012674,5.20231992197007,33.2624563238466));
#52108=CARTESIAN_POINT('Ctrl Pts',(-3.68575063421552,4.73285664350901,33.3088474763206));
#52109=CARTESIAN_POINT('Ctrl Pts',(-4.43215692772435,4.0423600425559,33.3552386287945));
#52110=CARTESIAN_POINT('Ctrl Pts',(-4.96750652200506,3.21525542813924,33.4016297812685));
#52111=CARTESIAN_POINT('Ctrl Pts',(-5.50285611628576,2.38815081372258,33.4480209337425));
#52112=CARTESIAN_POINT('Ctrl Pts',(-5.82714901133836,1.42443818584236,33.4944120862165));
#52113=CARTESIAN_POINT('Ctrl Pts',(-5.90073471816293,0.441948300379427,
33.5408032386905));
#52114=CARTESIAN_POINT('Ctrl Pts',(-5.91174378489267,0.294959201855924,
33.5477437617254));
#52115=CARTESIAN_POINT('Ctrl Pts',(-5.91714132713061,0.147549816058014,
33.5546842847603));
#52116=CARTESIAN_POINT('Ctrl Pts',(-5.91699986415359,0.000130094215637797,
33.5616248077952));
#52117=CARTESIAN_POINT('Origin',(0.,0.,0.));
#52118=CARTESIAN_POINT('',(-5.91647681799755,-0.000134629570711919,35.5633751922049));
#52119=CARTESIAN_POINT('',(-5.91661122068025,-0.000151359735457047,35.3116248077952));
#52120=CARTESIAN_POINT('',(-5.91675,-7.2459289488551E-16,0.));
#52121=CARTESIAN_POINT('Ctrl Pts',(-5.91647681799755,-0.000134629570711919,
35.5633751922049));
#52122=CARTESIAN_POINT('Ctrl Pts',(-5.91592360889482,0.665100593798877,
35.5320638709699));
#52123=CARTESIAN_POINT('Ctrl Pts',(-5.80395651976011,1.33051735339803,35.5007525497348));
#52124=CARTESIAN_POINT('Ctrl Pts',(-5.58391280219011,1.95803632134791,35.4694412284998));
#52125=CARTESIAN_POINT('Ctrl Pts',(-5.25789392946026,2.88777441524527,35.4230500760258));
#52126=CARTESIAN_POINT('Ctrl Pts',(-4.69462882472502,3.73432053322438,35.3766589235518));
#52127=CARTESIAN_POINT('Ctrl Pts',(-3.96298651712459,4.39416957834686,35.3302677710778));
#52128=CARTESIAN_POINT('Ctrl Pts',(-3.23134420952415,5.05401862346935,35.2838766186039));
#52129=CARTESIAN_POINT('Ctrl Pts',(-2.33132469905851,5.52717059573522,35.2374854661299));
#52130=CARTESIAN_POINT('Ctrl Pts',(-1.37297114191099,5.75577437549979,35.1910943136559));
#52131=CARTESIAN_POINT('Ctrl Pts',(-0.414617584763474,5.98437815526435,
35.1447031611819));
#52132=CARTESIAN_POINT('Ctrl Pts',(0.602070019065926,5.96843374252761,35.0983120087079));
#52133=CARTESIAN_POINT('Ctrl Pts',(1.55278379460685,5.70989062114036,35.0519208562339));
#52134=CARTESIAN_POINT('Ctrl Pts',(2.50349757014778,5.4513474997531,35.0055297037599));
#52135=CARTESIAN_POINT('Ctrl Pts',(3.38823751740023,4.95020566971533,34.959138551286));
#52136=CARTESIAN_POINT('Ctrl Pts',(4.09882867452727,4.2677385012502,34.912747398812));
#52137=CARTESIAN_POINT('Ctrl Pts',(4.80941983165431,3.58527133278508,34.866356246338));
#52138=CARTESIAN_POINT('Ctrl Pts',(5.34586219865593,2.72147882589261,34.819965093864));
#52139=CARTESIAN_POINT('Ctrl Pts',(5.64256629609434,1.78197475076402,34.77357394139));
#52140=CARTESIAN_POINT('Ctrl Pts',(5.93927039353275,0.842470675635441,34.7271827889161));
#52141=CARTESIAN_POINT('Ctrl Pts',(5.99623622140793,-0.172744967729249,
34.6807916364421));
#52142=CARTESIAN_POINT('Ctrl Pts',(5.80649870905078,-1.13954427731964,34.6344004839681));
#52143=CARTESIAN_POINT('Ctrl Pts',(5.61676119669363,-2.10634358691004,34.5880093314941));
#52144=CARTESIAN_POINT('Ctrl Pts',(5.18032034410413,-3.02472656272614,34.5416181790201));
#52145=CARTESIAN_POINT('Ctrl Pts',(4.55053869325812,-3.7824047931628,34.4952270265461));
#52146=CARTESIAN_POINT('Ctrl Pts',(3.92075704241212,-4.54008302359946,34.4488358740721));
#52147=CARTESIAN_POINT('Ctrl Pts',(3.0976345933096,-5.13705650865668,34.4024447215982));
#52148=CARTESIAN_POINT('Ctrl Pts',(2.18181248891615,-5.50033477902844,34.3560535691242));
#52149=CARTESIAN_POINT('Ctrl Pts',(1.2659903845227,-5.86361304940021,34.3096624166502));
#52150=CARTESIAN_POINT('Ctrl Pts',(0.257468624838311,-5.99319610508651,
34.2632712641762));
#52151=CARTESIAN_POINT('Ctrl Pts',(-0.720443332703347,-5.8732401468477,
34.2168801117022));
#52152=CARTESIAN_POINT('Ctrl Pts',(-1.69835529024501,-5.75328418860889,
34.1704889592282));
#52153=CARTESIAN_POINT('Ctrl Pts',(-2.64565744564394,-5.38378921644496,
34.1240978067543));
#52154=CARTESIAN_POINT('Ctrl Pts',(-3.44652551084063,-4.80993246535802,
34.0777066542803));
#52155=CARTESIAN_POINT('Ctrl Pts',(-4.24739357603731,-4.23607571427107,
34.0313155018063));
#52156=CARTESIAN_POINT('Ctrl Pts',(-4.90182755103176,-3.45785718426112,
33.9849243493323));
#52157=CARTESIAN_POINT('Ctrl Pts',(-5.32981141474379,-2.57042772733394,
33.9385331968583));
#52158=CARTESIAN_POINT('Ctrl Pts',(-5.71469519501551,-1.77236678843735,
33.8968138619738));
#52159=CARTESIAN_POINT('Ctrl Pts',(-5.91644160775919,-0.88598351864123,
33.8550945270894));
#52160=CARTESIAN_POINT('Ctrl Pts',(-5.91712951644955,9.70841563171718E-5,
33.8133751922049));
#52161=CARTESIAN_POINT('Ctrl Pts',(-5.91699986415359,0.000130094215637797,
33.5616248077952));
#52162=CARTESIAN_POINT('Ctrl Pts',(-5.91619577439583,-0.837818398883012,
33.6010754372343));
#52163=CARTESIAN_POINT('Ctrl Pts',(-5.73643198268786,-1.67610083920967,
33.6405260666734));
#52164=CARTESIAN_POINT('Ctrl Pts',(-5.39102647875133,-2.43943067533054,
33.6799766961124));
#52165=CARTESIAN_POINT('Ctrl Pts',(-4.98485401391861,-3.33705262253189,
33.7263678485864));
#52166=CARTESIAN_POINT('Ctrl Pts',(-4.34963056565659,-4.13102937388896,
33.7727590010604));
#52167=CARTESIAN_POINT('Ctrl Pts',(-3.56302333152666,-4.72428335870514,
33.8191501535344));
#52168=CARTESIAN_POINT('Ctrl Pts',(-2.77641609739674,-5.31753734352131,
33.8655413060084));
#52169=CARTESIAN_POINT('Ctrl Pts',(-1.83842507739896,-5.71006856179661,
33.9119324584823));
#52170=CARTESIAN_POINT('Ctrl Pts',(-0.863736110131024,-5.85388319377807,
33.9583236109563));
#52171=CARTESIAN_POINT('Ctrl Pts',(0.110952857136989,-5.99769782575954,
34.0047147634303));
#52172=CARTESIAN_POINT('Ctrl Pts',(1.12233977167512,-5.89279587144709,34.0511059159043));
#52173=CARTESIAN_POINT('Ctrl Pts',(2.04676486066272,-5.55200343295085,34.0974970683783));
#52174=CARTESIAN_POINT('Ctrl Pts',(2.97118994965026,-5.21121099445462,34.1438882208523));
#52175=CARTESIAN_POINT('Ctrl Pts',(3.80865321308733,-4.63452807177462,34.1902793733263));
#52176=CARTESIAN_POINT('Ctrl Pts',(4.45676009216202,-3.89246425741503,34.2366705258002));
#52177=CARTESIAN_POINT('Ctrl Pts',(5.10486697123672,-3.15040044305545,34.2830616782742));
#52178=CARTESIAN_POINT('Ctrl Pts',(5.56361746594906,-2.24295573701623,34.3294528307482));
#52179=CARTESIAN_POINT('Ctrl Pts',(5.77692128964215,-1.28108115575122,34.3758439832222));
#52180=CARTESIAN_POINT('Ctrl Pts',(5.99022511333525,-0.319206574486185,
34.4222351356962));
#52181=CARTESIAN_POINT('Ctrl Pts',(5.9580822660091,0.697097882004619,34.4686262881702));
#52182=CARTESIAN_POINT('Ctrl Pts',(5.68442277398798,1.64357118522697,34.5150174406441));
#52183=CARTESIAN_POINT('Ctrl Pts',(5.41076328196687,2.5900444884493,34.5614085931181));
#52184=CARTESIAN_POINT('Ctrl Pts',(4.89558714525077,3.46668663840314,34.6077997455921));
#52185=CARTESIAN_POINT('Ctrl Pts',(4.20188367397727,4.16631277086886,34.6541908980661));
#52186=CARTESIAN_POINT('Ctrl Pts',(3.50818020270377,4.86593890333457,34.7005820505401));
#52187=CARTESIAN_POINT('Ctrl Pts',(2.63594939687283,5.38854901831218,34.7469732030141));
#52188=CARTESIAN_POINT('Ctrl Pts',(1.69183675658515,5.67024487155617,34.793364355488));
#52189=CARTESIAN_POINT('Ctrl Pts',(0.747724116297463,5.95194072480015,34.839755507962));
#52190=CARTESIAN_POINT('Ctrl Pts',(-0.268270358447003,5.99272231631053,
34.886146660436));
#52191=CARTESIAN_POINT('Ctrl Pts',(-1.23192353985419,5.78760338190989,34.93253781291));
#52192=CARTESIAN_POINT('Ctrl Pts',(-2.19557672126134,5.58248444750926,34.978928965384));
#52193=CARTESIAN_POINT('Ctrl Pts',(-3.10688860933118,5.13146498719767,35.025320117858));
#52194=CARTESIAN_POINT('Ctrl Pts',(-3.85443535684222,4.48969003320565,35.0717112703319));
#52195=CARTESIAN_POINT('Ctrl Pts',(-4.60198210435332,3.84791507921359,35.1181024228059));
#52196=CARTESIAN_POINT('Ctrl Pts',(-5.18576371130555,3.01538463154107,35.1644935752799));
#52197=CARTESIAN_POINT('Ctrl Pts',(-5.53440264665228,2.09389012583512,35.2108847277539));
#52198=CARTESIAN_POINT('Ctrl Pts',(-5.78676336904098,1.42687048012088,35.2444647544343));
#52199=CARTESIAN_POINT('Ctrl Pts',(-5.91592054800081,0.713237911653397,
35.2780447811148));
#52200=CARTESIAN_POINT('Ctrl Pts',(-5.91661122068025,-0.000151359735457047,
35.3116248077952));
#52201=CARTESIAN_POINT('Origin',(0.,0.,0.));
#52202=CARTESIAN_POINT('',(-5.91669249471401,0.000154889389280682,37.3133751922049));
#52203=CARTESIAN_POINT('',(-5.91654848309511,0.000145436179947218,37.0616248077952));
#52204=CARTESIAN_POINT('',(-5.91675,-7.2459289488551E-16,0.));
#52205=CARTESIAN_POINT('Ctrl Pts',(-5.91669249471401,0.000154889389280682,
37.3133751922049));
#52206=CARTESIAN_POINT('Ctrl Pts',(-5.91694160613561,0.245724103443592,
37.3018155197983));
#52207=CARTESIAN_POINT('Ctrl Pts',(-5.9019420281964,0.491263090650058,37.2902558473917));
#52208=CARTESIAN_POINT('Ctrl Pts',(-5.87145331977663,0.734863478385117,
37.2786961749852));
#52209=CARTESIAN_POINT('Ctrl Pts',(-5.74909636438138,1.71247792390357,37.2323050225112));
#52210=CARTESIAN_POINT('Ctrl Pts',(-5.37727631279197,2.65886989201929,37.1859138700372));
#52211=CARTESIAN_POINT('Ctrl Pts',(-4.80145468171261,3.45832638101732,37.1395227175632));
#52212=CARTESIAN_POINT('Ctrl Pts',(-4.22563305063326,4.25778287001535,37.0931315650893));
#52213=CARTESIAN_POINT('Ctrl Pts',(-3.44580984006395,4.91030387989569,37.0467404126153));
#52214=CARTESIAN_POINT('Ctrl Pts',(-2.55733210232766,5.33610728308424,37.0003492601413));
#52215=CARTESIAN_POINT('Ctrl Pts',(-1.66885436459137,5.76191068627279,36.9539581076673));
#52216=CARTESIAN_POINT('Ctrl Pts',(-0.671722099688089,5.96099648276954,
36.9075669551933));
#52217=CARTESIAN_POINT('Ctrl Pts',(0.31214780026346,5.90902294537523,36.8611758027193));
#52218=CARTESIAN_POINT('Ctrl Pts',(1.29601770021501,5.85704940798092,36.8147846502453));
#52219=CARTESIAN_POINT('Ctrl Pts',(2.26662523521483,5.55401653669555,36.7683934977713));
#52220=CARTESIAN_POINT('Ctrl Pts',(3.10529662616736,5.03697541007437,36.7220023452974));
#52221=CARTESIAN_POINT('Ctrl Pts',(3.9439680171199,4.5199342834532,36.6756111928234));
#52222=CARTESIAN_POINT('Ctrl Pts',(4.65070326402515,3.78888490149623,36.6292200403494));
#52223=CARTESIAN_POINT('Ctrl Pts',(5.13909159883741,2.93321086131548,36.5828288878754));
#52224=CARTESIAN_POINT('Ctrl Pts',(5.62747993364967,2.07753682113472,36.5364377354014));
#52225=CARTESIAN_POINT('Ctrl Pts',(5.89752135636894,1.09723812273018,36.4900465829274));
#52226=CARTESIAN_POINT('Ctrl Pts',(5.91619857113585,0.112173459741759,36.4436554304535));
#52227=CARTESIAN_POINT('Ctrl Pts',(5.93487578590275,-0.872891203246667,
36.3972642779795));
#52228=CARTESIAN_POINT('Ctrl Pts',(5.70218879271729,-1.86272183081898,36.3508731255055));
#52229=CARTESIAN_POINT('Ctrl Pts',(5.2465876538672,-2.73629428396665,36.3044819730315));
#52230=CARTESIAN_POINT('Ctrl Pts',(4.79098651501711,-3.60986673711433,36.2580908205575));
#52231=CARTESIAN_POINT('Ctrl Pts',(4.1124712305024,-4.36718101583737,36.2116996680835));
#52232=CARTESIAN_POINT('Ctrl Pts',(3.29400218346852,-4.91564217915472,36.1653085156096));
#52233=CARTESIAN_POINT('Ctrl Pts',(2.47553313643465,-5.46410334247206,36.1189173631356));
#52234=CARTESIAN_POINT('Ctrl Pts',(1.51711032688161,-5.8037113903837,36.0725262106616));
#52235=CARTESIAN_POINT('Ctrl Pts',(0.535917737706336,-5.89294328808551,
36.0261350581876));
#52236=CARTESIAN_POINT('Ctrl Pts',(-0.44527485146894,-5.98217518578732,
35.9797439057136));
#52237=CARTESIAN_POINT('Ctrl Pts',(-1.44923722026646,-5.82103093327931,
35.9333527532396));
#52238=CARTESIAN_POINT('Ctrl Pts',(-2.35321737668262,-5.42921323915899,
35.8869616007656));
#52239=CARTESIAN_POINT('Ctrl Pts',(-3.25719753309878,-5.03739554503867,
35.8405704482917));
#52240=CARTESIAN_POINT('Ctrl Pts',(-4.06119547713358,-4.41490440930605,
35.7941792958177));
#52241=CARTESIAN_POINT('Ctrl Pts',(-4.66690837168441,-3.63785028120762,
35.7477881433437));
#52242=CARTESIAN_POINT('Ctrl Pts',(-5.27262126623519,-2.86079615310923,
35.7013969908697));
#52243=CARTESIAN_POINT('Ctrl Pts',(-5.68004911130202,-1.92917903264505,
35.6550058383957));
#52244=CARTESIAN_POINT('Ctrl Pts',(-5.83937671347322,-0.956905437505181,
35.6086146859218));
#52245=CARTESIAN_POINT('Ctrl Pts',(-5.89116748012414,-0.640859791926311,
35.5935348546828));
#52246=CARTESIAN_POINT('Ctrl Pts',(-5.91674324878296,-0.320518264209038,
35.5784550234439));
#52247=CARTESIAN_POINT('Ctrl Pts',(-5.91647681799755,-0.000134629570711919,
35.5633751922049));
#52248=CARTESIAN_POINT('Ctrl Pts',(-5.91661122068025,-0.000151359735457047,
35.3116248077952));
#52249=CARTESIAN_POINT('Ctrl Pts',(-5.91687471941605,-0.272316709171056,
35.3244359335887));
#52250=CARTESIAN_POINT('Ctrl Pts',(-5.89843990491604,-0.544446646691766,
35.3372470593823));
#52251=CARTESIAN_POINT('Ctrl Pts',(-5.86101453084031,-0.81393929971491,
35.3500581851759));
#52252=CARTESIAN_POINT('Ctrl Pts',(-5.72549121594036,-1.78981565581969,
35.3964493376498));
#52253=CARTESIAN_POINT('Ctrl Pts',(-5.34094832239917,-2.73110980428999,
35.4428404901238));
#52254=CARTESIAN_POINT('Ctrl Pts',(-4.75440295729178,-3.52273204119144,
35.4892316425978));
#52255=CARTESIAN_POINT('Ctrl Pts',(-4.16785759218437,-4.31435427809291,
35.5356227950718));
#52256=CARTESIAN_POINT('Ctrl Pts',(-3.37930975551075,-4.95630460342556,
35.5820139475458));
#52257=CARTESIAN_POINT('Ctrl Pts',(-2.48517323801659,-5.37009334103121,
35.6284051000198));
#52258=CARTESIAN_POINT('Ctrl Pts',(-1.59103672052242,-5.78388207863687,
35.6747962524937));
#52259=CARTESIAN_POINT('Ctrl Pts',(-0.591311522207775,-5.96950922851551,
35.7211874049677));
#52260=CARTESIAN_POINT('Ctrl Pts',(0.391768433263235,-5.90427861885261,
35.7675785574417));
#52261=CARTESIAN_POINT('Ctrl Pts',(1.37484838873424,-5.83904800918971,35.8139697099157));
#52262=CARTESIAN_POINT('Ctrl Pts',(2.34128310136155,-5.52295963998528,35.8603608623897));
#52263=CARTESIAN_POINT('Ctrl Pts',(3.17290899270499,-4.99466085318647,35.9067520148637));
#52264=CARTESIAN_POINT('Ctrl Pts',(4.00453488404839,-4.46636206638769,35.9531431673376));
#52265=CARTESIAN_POINT('Ctrl Pts',(4.701351954108,-3.72585286199446,35.9995343198116));
#52266=CARTESIAN_POINT('Ctrl Pts',(5.17816210575339,-2.86367346617613,36.0459254722856));
#52267=CARTESIAN_POINT('Ctrl Pts',(5.65497225739884,-2.00149407035771,36.0923166247596));
#52268=CARTESIAN_POINT('Ctrl Pts',(5.91177549063012,-1.01764448311409,36.1387077772336));
#52269=CARTESIAN_POINT('Ctrl Pts',(5.91717311022538,-0.0324175564679062,
36.1850989297076));
#52270=CARTESIAN_POINT('Ctrl Pts',(5.92257072982063,0.952809370178166,36.2314900821816));
#52271=CARTESIAN_POINT('Ctrl Pts',(5.67656273577991,1.93941363622675,36.2778812346556));
#52272=CARTESIAN_POINT('Ctrl Pts',(5.20922791616921,2.80676558190117,36.3242723871295));
#52273=CARTESIAN_POINT('Ctrl Pts',(4.74189309655848,3.67411752757564,36.3706635396035));
#52274=CARTESIAN_POINT('Ctrl Pts',(4.05323145137778,4.42221715287586,36.4170546920775));
#52275=CARTESIAN_POINT('Ctrl Pts',(3.22744393415846,4.95959616967,36.4634458445515));
#52276=CARTESIAN_POINT('Ctrl Pts',(2.40165641693915,5.49697518646414,36.5098369970254));
#52277=CARTESIAN_POINT('Ctrl Pts',(1.43874302768128,5.82363359475216,36.5562281494994));
#52278=CARTESIAN_POINT('Ctrl Pts',(0.456436801339,5.8996316800903,36.6026193019734));
#52279=CARTESIAN_POINT('Ctrl Pts',(-0.525869425003222,5.97562976542843,
36.6490104544474));
#52280=CARTESIAN_POINT('Ctrl Pts',(-1.52756848842996,5.80096752781665,36.6954016069214));
#52281=CARTESIAN_POINT('Ctrl Pts',(-2.42618512567881,5.39700048640691,36.7417927593954));
#52282=CARTESIAN_POINT('Ctrl Pts',(-3.32480176292772,4.99303344499716,36.7881839118694));
#52283=CARTESIAN_POINT('Ctrl Pts',(-4.12033597399883,4.35976159978945,36.8345750643434));
#52284=CARTESIAN_POINT('Ctrl Pts',(-4.71551976145427,3.57461353067377,36.8809662168173));
#52285=CARTESIAN_POINT('Ctrl Pts',(-5.3107035489097,2.78946546155808,36.9273573692913));
#52286=CARTESIAN_POINT('Ctrl Pts',(-5.70553691274941,1.8524411685345,36.9737485217653));
#52287=CARTESIAN_POINT('Ctrl Pts',(-5.85174455558468,0.878108290888243,
37.0201396742393));
#52288=CARTESIAN_POINT('Ctrl Pts',(-5.89532645476485,0.587676980882504,
37.0339680520913));
#52289=CARTESIAN_POINT('Ctrl Pts',(-5.91681720987146,0.293930690774358,
37.0477964299432));
#52290=CARTESIAN_POINT('Ctrl Pts',(-5.91654848309511,0.000145436179947218,
37.0616248077952));
#52291=CARTESIAN_POINT('Origin',(0.,0.,0.));
#52292=CARTESIAN_POINT('',(-5.91691912648428,-0.000142687999947211,39.0633751922049));
#52293=CARTESIAN_POINT('',(-5.91706133753908,-0.000116827836684568,38.8116248077952));
#52294=CARTESIAN_POINT('',(-5.91675,-7.2459289488551E-16,0.));
#52295=CARTESIAN_POINT('Ctrl Pts',(-5.91691912648428,-0.000142687999947211,
39.0633751922049));
#52296=CARTESIAN_POINT('Ctrl Pts',(-5.9160967133036,0.811256349217919,39.0251760161528));
#52297=CARTESIAN_POINT('Ctrl Pts',(-5.74787377874497,1.62298581578632,38.9869768401007));
#52298=CARTESIAN_POINT('Ctrl Pts',(-5.42341831385396,2.36654224790806,38.9487776640486));
#52299=CARTESIAN_POINT('Ctrl Pts',(-5.02938198903266,3.26955753202083,38.9023865115746));
#52300=CARTESIAN_POINT('Ctrl Pts',(-4.40491843421483,4.07202446391407,38.8559953591006));
#52301=CARTESIAN_POINT('Ctrl Pts',(-3.62637926144279,4.67582739954737,38.8096042066266));
#52302=CARTESIAN_POINT('Ctrl Pts',(-2.84784008867076,5.27963033518068,38.7632130541527));
#52303=CARTESIAN_POINT('Ctrl Pts',(-1.91522529794454,5.68476927455403,38.7168219016787));
#52304=CARTESIAN_POINT('Ctrl Pts',(-0.942563389625921,5.84170888308526,
38.6704307492047));
#52305=CARTESIAN_POINT('Ctrl Pts',(0.0300985186927029,5.99864849161649,
38.6240395967307));
#52306=CARTESIAN_POINT('Ctrl Pts',(1.0428075446037,5.90738876930559,38.5776484442567));
#52307=CARTESIAN_POINT('Ctrl Pts',(1.97174226400384,5.57908781634788,38.5312572917827));
#52308=CARTESIAN_POINT('Ctrl Pts',(2.90067698340398,5.25078686339016,38.4848661393088));
#52309=CARTESIAN_POINT('Ctrl Pts',(3.74583739629323,4.68544467978563,38.4384749868348));
#52310=CARTESIAN_POINT('Ctrl Pts',(4.40388783246218,3.95218425396285,38.3920838343608));
#52311=CARTESIAN_POINT('Ctrl Pts',(5.06193826863114,3.21892382814006,38.3456926818868));
#52312=CARTESIAN_POINT('Ctrl Pts',(5.53287872807978,2.31774516009906,38.2993015294128));
#52313=CARTESIAN_POINT('Ctrl Pts',(5.75912848735764,1.3588331333486,38.2529103769389));
#52314=CARTESIAN_POINT('Ctrl Pts',(5.9853782466355,0.399921106598193,38.2065192244649));
#52315=CARTESIAN_POINT('Ctrl Pts',(5.96693730574259,-0.616724278861779,
38.1601280719908));
#52316=CARTESIAN_POINT('Ctrl Pts',(5.70606039284341,-1.56680030999616,38.1137369195169));
#52317=CARTESIAN_POINT('Ctrl Pts',(5.44518347994422,-2.51687634113059,38.0673457670429));
#52318=CARTESIAN_POINT('Ctrl Pts',(4.94187059503875,-3.40038301793954,38.0209546145689));
#52319=CARTESIAN_POINT('Ctrl Pts',(4.25766055785111,-4.10929616750841,37.9745634620949));
#52320=CARTESIAN_POINT('Ctrl Pts',(3.57345052066347,-4.81820931707727,37.928172309621));
#52321=CARTESIAN_POINT('Ctrl Pts',(2.70834333119368,-5.35252893940602,37.8817811571469));
#52322=CARTESIAN_POINT('Ctrl Pts',(1.76811350261519,-5.64692509778996,37.835390004673));
#52323=CARTESIAN_POINT('Ctrl Pts',(0.827883674036693,-5.9413212561739,37.788998852199));
#52324=CARTESIAN_POINT('Ctrl Pts',(-0.187468793650468,-5.99579395061301,
37.742607699725));
#52325=CARTESIAN_POINT('Ctrl Pts',(-1.15379926926493,-5.80368293968787,
37.696216547251));
#52326=CARTESIAN_POINT('Ctrl Pts',(-2.1201297448794,-5.61157192876273,37.6498253947771));
#52327=CARTESIAN_POINT('Ctrl Pts',(-3.03743822842114,-5.17287721247336,
37.6034342423031));
#52328=CARTESIAN_POINT('Ctrl Pts',(-3.79356768379389,-4.54123690712729,
37.5570430898291));
#52329=CARTESIAN_POINT('Ctrl Pts',(-4.54969713916663,-3.90959660178122,
37.5106519373551));
#52330=CARTESIAN_POINT('Ctrl Pts',(-5.14464756637036,-3.08501070737847,
37.4642607848811));
#52331=CARTESIAN_POINT('Ctrl Pts',(-5.50567585037168,-2.1682992987165,37.4178696324071));
#52332=CARTESIAN_POINT('Ctrl Pts',(-5.77674368997775,-1.48001255748339,
37.3830381523397));
#52333=CARTESIAN_POINT('Ctrl Pts',(-5.91594187486849,-0.739791614598744,
37.3482066722723));
#52334=CARTESIAN_POINT('Ctrl Pts',(-5.91669249471401,0.000154889389280682,
37.3133751922049));
#52335=CARTESIAN_POINT('Ctrl Pts',(-5.91654848309511,0.000145436179947218,
37.0616248077952));
#52336=CARTESIAN_POINT('Ctrl Pts',(-5.91591569090887,-0.691653929951799,
37.0941875824172));
#52337=CARTESIAN_POINT('Ctrl Pts',(-5.79462691049747,-1.38366935355313,
37.1267503570392));
#52338=CARTESIAN_POINT('Ctrl Pts',(-5.55701272580384,-2.03312520017727,
37.1593131316612));
#52339=CARTESIAN_POINT('Ctrl Pts',(-5.2184913313569,-2.95838435132766,37.2057042841352));
#52340=CARTESIAN_POINT('Ctrl Pts',(-4.64386662063219,-3.79726119135959,
37.2520954366092));
#52341=CARTESIAN_POINT('Ctrl Pts',(-3.90339653365634,-4.44718832695235,
37.2984865890832));
#52342=CARTESIAN_POINT('Ctrl Pts',(-3.16292644668049,-5.09711546254512,
37.3448777415572));
#52343=CARTESIAN_POINT('Ctrl Pts',(-2.25661098345347,-5.55809289369875,
37.3912688940312));
#52344=CARTESIAN_POINT('Ctrl Pts',(-1.29526309070761,-5.77375805175383,
37.4376600465051));
#52345=CARTESIAN_POINT('Ctrl Pts',(-0.333915197961686,-5.98942320980892,
37.4840511989791));
#52346=CARTESIAN_POINT('Ctrl Pts',(0.682465124303125,-5.95977609476543,
37.5304423514531));
#52347=CARTESIAN_POINT('Ctrl Pts',(1.62960757167219,-5.6884415859434,37.5768335039271));
#52348=CARTESIAN_POINT('Ctrl Pts',(2.57675001904114,-5.41710707712141,37.6232246564011));
#52349=CARTESIAN_POINT('Ctrl Pts',(3.45465459151441,-4.90408517452091,37.6696158088751));
#52350=CARTESIAN_POINT('Ctrl Pts',(4.15598207159793,-4.21210179541024,37.7160069613491));
#52351=CARTESIAN_POINT('Ctrl Pts',(4.85730955168154,-3.5201184162995,37.762398113823));
#52352=CARTESIAN_POINT('Ctrl Pts',(5.3820599393754,-2.6491735606785,37.808789266297));
#52353=CARTESIAN_POINT('Ctrl Pts',(5.66607330459045,-1.70575549870112,37.855180418771));
#52354=CARTESIAN_POINT('Ctrl Pts',(5.95008666980548,-0.762337436723782,
37.901571571245));
#52355=CARTESIAN_POINT('Ctrl Pts',(5.99336301254174,0.253553831609811,37.947962723719));
#52356=CARTESIAN_POINT('Ctrl Pts',(5.79061104156902,1.21770779729813,37.994353876193));
#52357=CARTESIAN_POINT('Ctrl Pts',(5.5878590705963,2.18186176298639,38.0407450286669));
#52358=CARTESIAN_POINT('Ctrl Pts',(5.13907878591457,3.09427842602926,38.0871361811409));
#52359=CARTESIAN_POINT('Ctrl Pts',(4.49914144129667,3.8433988611057,38.1335273336149));
#52360=CARTESIAN_POINT('Ctrl Pts',(3.85920409667869,4.59251929618222,38.1799184860889));
#52361=CARTESIAN_POINT('Ctrl Pts',(3.02810969212445,5.1783435032923,38.2263096385629));
#52362=CARTESIAN_POINT('Ctrl Pts',(2.107474081846,5.52924420772758,38.2727007910369));
#52363=CARTESIAN_POINT('Ctrl Pts',(1.1868384715676,5.88014491216284,38.3190919435108));
#52364=CARTESIAN_POINT('Ctrl Pts',(0.176661655564968,5.99612211392334,38.3654830959848));
#52365=CARTESIAN_POINT('Ctrl Pts',(-0.799544549091766,5.86299556782702,
38.4118742484588));
#52366=CARTESIAN_POINT('Ctrl Pts',(-1.7757507537485,5.7298690217307,38.4582654009328));
#52367=CARTESIAN_POINT('Ctrl Pts',(-2.71798634705937,5.34763872777755,38.5046565534068));
#52368=CARTESIAN_POINT('Ctrl Pts',(-3.5110465169614,4.76303903721929,38.5510477058807));
#52369=CARTESIAN_POINT('Ctrl Pts',(-4.30410668686342,4.17843934666103,38.5974388583547));
#52370=CARTESIAN_POINT('Ctrl Pts',(-4.94799143335662,3.39147025949764,38.6438300108287));
#52371=CARTESIAN_POINT('Ctrl Pts',(-5.36397456339906,2.49835253668281,38.6902211633027));
#52372=CARTESIAN_POINT('Ctrl Pts',(-5.72684453135159,1.71926902091001,38.7306890448002));
#52373=CARTESIAN_POINT('Ctrl Pts',(-5.91629496269227,0.859412724788655,
38.7711569262977));
#52374=CARTESIAN_POINT('Ctrl Pts',(-5.91706133753908,-0.000116827836684568,
38.8116248077952));
#52375=CARTESIAN_POINT('Origin',(0.,0.,0.));
#52376=CARTESIAN_POINT('',(-5.9163246276023,8.91563840094145E-5,40.8133751922049));
#52377=CARTESIAN_POINT('',(-5.91626344896283,4.86828180632854E-5,40.5616248077952));
#52378=CARTESIAN_POINT('',(-5.91675,-7.2459289488551E-16,0.));
#52379=CARTESIAN_POINT('Ctrl Pts',(-5.9163246276023,8.91563840094145E-5,
40.8133751922049));
#52380=CARTESIAN_POINT('Ctrl Pts',(-5.91653311395868,0.392051192521081,
40.7949276649813));
#52381=CARTESIAN_POINT('Ctrl Pts',(-5.87816883703071,0.783972960225323,
40.7764801377576));
#52382=CARTESIAN_POINT('Ctrl Pts',(-5.8008321742822,1.16804730383351,40.758032610534));
#52383=CARTESIAN_POINT('Ctrl Pts',(-5.60634882321301,2.1339031185268,40.71164145806));
#52384=CARTESIAN_POINT('Ctrl Pts',(-5.16540288854038,3.05013157845018,40.665250305586));
#52385=CARTESIAN_POINT('Ctrl Pts',(-4.5319077374673,3.80470769931993,40.618859153112));
#52386=CARTESIAN_POINT('Ctrl Pts',(-3.89841258639425,4.55928382018964,40.572468000638));
#52387=CARTESIAN_POINT('Ctrl Pts',(-3.07236821892077,5.15220760200574,40.5260768481641));
#52388=CARTESIAN_POINT('Ctrl Pts',(-2.15477303373402,5.51098372264635,40.4796856956901));
#52389=CARTESIAN_POINT('Ctrl Pts',(-1.23717784854716,5.869759843287,40.4332945432161));
#52390=CARTESIAN_POINT('Ctrl Pts',(-0.228031845647002,5.9943883027521,40.3869033907421));
#52391=CARTESIAN_POINT('Ctrl Pts',(0.749279192861052,5.86963108800935,40.3405122382681));
#52392=CARTESIAN_POINT('Ctrl Pts',(1.72659023136905,5.7448738732666,40.2941210857941));
#52393=CARTESIAN_POINT('Ctrl Pts',(2.67206630548495,5.37073098431603,40.2477299333201));
#52394=CARTESIAN_POINT('Ctrl Pts',(3.47010639758447,4.79294794543229,40.2013387808462));
#52395=CARTESIAN_POINT('Ctrl Pts',(4.268146489684,4.21516490654855,40.1549476283722));
#52396=CARTESIAN_POINT('Ctrl Pts',(4.91875059976714,3.43374171773163,40.1085564758982));
#52397=CARTESIAN_POINT('Ctrl Pts',(5.34237097484983,2.54422105668167,40.0621653234242));
#52398=CARTESIAN_POINT('Ctrl Pts',(5.76599134993251,1.65470039563171,40.0157741709502));
#52399=CARTESIAN_POINT('Ctrl Pts',(5.96262799001472,0.657082262348707,39.9693830184762));
#52400=CARTESIAN_POINT('Ctrl Pts',(5.9082386201854,-0.32665704512534,39.9229918660023));
#52401=CARTESIAN_POINT('Ctrl Pts',(5.85384925035609,-1.31039635259939,39.8766007135283));
#52402=CARTESIAN_POINT('Ctrl Pts',(5.54843387061524,-2.28025683426448,39.8302095610543));
#52403=CARTESIAN_POINT('Ctrl Pts',(5.02933486292548,-3.11765605138583,39.7838184085803));
#52404=CARTESIAN_POINT('Ctrl Pts',(4.51023585523571,-3.95505526850718,39.7374272561063));
#52405=CARTESIAN_POINT('Ctrl Pts',(3.77745321959704,-4.6599932210848,39.6910361036323));
#52406=CARTESIAN_POINT('Ctrl Pts',(2.92058247375582,-5.14627889179849,39.6446449511583));
#52407=CARTESIAN_POINT('Ctrl Pts',(2.0637117279146,-5.63256456251218,39.5982537986844));
#52408=CARTESIAN_POINT('Ctrl Pts',(1.08275287187084,-5.90019795136195,39.5518626462104));
#52409=CARTESIAN_POINT('Ctrl Pts',(0.0976453151037753,-5.9164561868249,
39.5054714937364));
#52410=CARTESIAN_POINT('Ctrl Pts',(-0.887462241663293,-5.93271442228785,
39.4590803412624));
#52411=CARTESIAN_POINT('Ctrl Pts',(-1.87671849915367,-5.69759750436398,
39.4126891887884));
#52412=CARTESIAN_POINT('Ctrl Pts',(-2.74916954516603,-5.23985259621985,
39.3662980363144));
#52413=CARTESIAN_POINT('Ctrl Pts',(-3.6216205911784,-4.78210768807572,39.3199068838405));
#52414=CARTESIAN_POINT('Ctrl Pts',(-4.37726642571275,-4.10173478971132,
39.2735157313665));
#52415=CARTESIAN_POINT('Ctrl Pts',(-4.92371610432621,-3.28192141011619,
39.2271245788925));
#52416=CARTESIAN_POINT('Ctrl Pts',(-5.47016578293967,-2.46210803052105,
39.1807334264185));
#52417=CARTESIAN_POINT('Ctrl Pts',(-5.80741930563224,-1.50285416969518,
39.1343422739445));
#52418=CARTESIAN_POINT('Ctrl Pts',(-5.89424151956614,-0.521445421116098,
39.0879511214705));
#52419=CARTESIAN_POINT('Ctrl Pts',(-5.90957301041108,-0.348143468053205,
39.0797591450487));
#52420=CARTESIAN_POINT('Ctrl Pts',(-5.91709549650274,-0.174150676354238,
39.0715671686268));
#52421=CARTESIAN_POINT('Ctrl Pts',(-5.91691912648428,-0.000142687999947211,
39.0633751922049));
#52422=CARTESIAN_POINT('Ctrl Pts',(-5.91706133753908,-0.000116827836684568,
38.8116248077952));
#52423=CARTESIAN_POINT('Ctrl Pts',(-5.91717351158228,-0.125925895771626,
38.8175480787717));
#52424=CARTESIAN_POINT('Ctrl Pts',(-5.91324330254416,-0.251727963526452,
38.8234713497482));
#52425=CARTESIAN_POINT('Ctrl Pts',(-5.90522284338791,-0.377268716263677,
38.8293946207247));
#52426=CARTESIAN_POINT('Ctrl Pts',(-5.84240647974259,-1.3605058879289,38.8757857731986));
#52427=CARTESIAN_POINT('Ctrl Pts',(-5.5286922388603,-2.32771387279308,38.9221769256726));
#52428=CARTESIAN_POINT('Ctrl Pts',(-5.002437183899,-3.160634546335,38.9685680781466));
#52429=CARTESIAN_POINT('Ctrl Pts',(-4.47618212893773,-3.99355521987688,
39.0149592306206));
#52430=CARTESIAN_POINT('Ctrl Pts',(-3.73738625989748,-4.69218858209652,
39.0613503830946));
#52431=CARTESIAN_POINT('Ctrl Pts',(-2.87638031767776,-5.17111446232025,
39.1077415355686));
#52432=CARTESIAN_POINT('Ctrl Pts',(-2.01537437545794,-5.65004034254403,
39.1541326880426));
#52433=CARTESIAN_POINT('Ctrl Pts',(-1.03215836005863,-5.90925874077186,
39.2005238405165));
#52434=CARTESIAN_POINT('Ctrl Pts',(-0.0469476582424495,-5.91707566554013,
39.2469149929905));
#52435=CARTESIAN_POINT('Ctrl Pts',(0.938263043573675,-5.92489259030839,
39.2933061454645));
#52436=CARTESIAN_POINT('Ctrl Pts',(1.92546843180667,-5.68130804161713,39.3396972979385));
#52437=CARTESIAN_POINT('Ctrl Pts',(2.79396534895927,-5.21610449887237,39.3860884504125));
#52438=CARTESIAN_POINT('Ctrl Pts',(3.66246226611187,-4.7509009561276,39.4324796028865));
#52439=CARTESIAN_POINT('Ctrl Pts',(4.41225071218408,-4.06407841932935,39.4788707553604));
#52440=CARTESIAN_POINT('Ctrl Pts',(4.95165591111146,-3.23961297878258,39.5252619078344));
#52441=CARTESIAN_POINT('Ctrl Pts',(5.49106111003884,-2.41514753823582,39.5716530603084));
#52442=CARTESIAN_POINT('Ctrl Pts',(5.82008306182138,-1.45303919394055,39.6180442127824));
#52443=CARTESIAN_POINT('Ctrl Pts',(5.89849306740675,-0.4709225499975,39.6644353652564));
#52444=CARTESIAN_POINT('Ctrl Pts',(5.97690307299213,0.511194093945548,39.7108265177304));
#52445=CARTESIAN_POINT('Ctrl Pts',(5.80470113238033,1.51331903753637,39.7572176702043));
#52446=CARTESIAN_POINT('Ctrl Pts',(5.40294195030329,2.41292494620007,39.8036088226783));
#52447=CARTESIAN_POINT('Ctrl Pts',(5.00118276822624,3.31253085486376,39.8499999751523));
#52448=CARTESIAN_POINT('Ctrl Pts',(4.36986634468393,4.10961772860033,39.8963911276263));
#52449=CARTESIAN_POINT('Ctrl Pts',(3.586182175003,4.70672772975369,39.9427822801003));
#52450=CARTESIAN_POINT('Ctrl Pts',(2.80249800532207,5.30383773090705,39.9891734325743));
#52451=CARTESIAN_POINT('Ctrl Pts',(1.86644608950252,5.7009708594772,40.0355645850482));
#52452=CARTESIAN_POINT('Ctrl Pts',(0.892475176677488,5.84957063153836,40.0819557375222));
#52453=CARTESIAN_POINT('Ctrl Pts',(-0.0814957361475431,5.99817040359952,
40.1283468899962));
#52454=CARTESIAN_POINT('Ctrl Pts',(-1.09338564597805,5.89823681915169,40.1747380424702));
#52455=CARTESIAN_POINT('Ctrl Pts',(-2.01947328000496,5.56198851002837,40.2211291949442));
#52456=CARTESIAN_POINT('Ctrl Pts',(-2.94556091403187,5.22574020090506,40.2675203474182));
#52457=CARTESIAN_POINT('Ctrl Pts',(-3.78584627225519,4.65317716710625,40.3139114998921));
#52458=CARTESIAN_POINT('Ctrl Pts',(-4.4375897453239,3.91430527252765,40.3603026523661));
#52459=CARTESIAN_POINT('Ctrl Pts',(-5.08933321839262,3.17543337794904,40.4066938048401));
#52460=CARTESIAN_POINT('Ctrl Pts',(-5.55253480630674,2.27025262259063,40.4530849573141));
#52461=CARTESIAN_POINT('Ctrl Pts',(-5.77055999826902,1.3094372152643,40.4994761097881));
#52462=CARTESIAN_POINT('Ctrl Pts',(-5.86792038626399,0.880379637069279,
40.5201923424572));
#52463=CARTESIAN_POINT('Ctrl Pts',(-5.91638966469366,0.440227842995804,
40.5409085751262));
#52464=CARTESIAN_POINT('Ctrl Pts',(-5.91626344896283,4.86828180632854E-5,
40.5616248077952));
#52465=CARTESIAN_POINT('Origin',(0.,0.,0.));
#52466=CARTESIAN_POINT('',(-5.9172499153618,-2.94340949030803E-5,42.5633751922049));
#52467=CARTESIAN_POINT('',(-5.91725525726564,2.18443538467081E-5,42.3116248077952));
#52468=CARTESIAN_POINT('',(-5.91675,-7.2459289488551E-16,0.));
#52469=CARTESIAN_POINT('Ctrl Pts',(-5.9172499153618,-2.94340949030803E-5,
42.5633751922049));
#52470=CARTESIAN_POINT('Ctrl Pts',(-5.91698609659766,0.957521378018406,
42.5182881613357));
#52471=CARTESIAN_POINT('Ctrl Pts',(-5.68004380919251,1.91519802461481,42.4732011304666));
#52472=CARTESIAN_POINT('Ctrl Pts',(-5.23308594241081,2.7620282289511,42.4281140995974));
#52473=CARTESIAN_POINT('Ctrl Pts',(-4.77320002516144,3.63335260697322,42.3817229471234));
#52474=CARTESIAN_POINT('Ctrl Pts',(-4.09097361557659,4.38732544079608,42.3353317946494));
#52475=CARTESIAN_POINT('Ctrl Pts',(-3.26982084687155,4.93176033962971,42.2889406421755));
#52476=CARTESIAN_POINT('Ctrl Pts',(-2.44866807816651,5.47619523846334,42.2425494897015));
#52477=CARTESIAN_POINT('Ctrl Pts',(-1.48858895034126,5.81109220230777,42.1961583372275));
#52478=CARTESIAN_POINT('Ctrl Pts',(-0.506969960225164,5.89550420893833,
42.1497671847535));
#52479=CARTESIAN_POINT('Ctrl Pts',(0.474649029890985,5.9799162155689,42.1033760322795));
#52480=CARTESIAN_POINT('Ctrl Pts',(1.47780788229784,5.81384326498563,42.0569848798055));
#52481=CARTESIAN_POINT('Ctrl Pts',(2.37985284895086,5.41759068549118,42.0105937273315));
#52482=CARTESIAN_POINT('Ctrl Pts',(3.28189781560384,5.02133810599675,41.9642025748575));
#52483=CARTESIAN_POINT('Ctrl Pts',(4.08282889650282,4.39490589759118,41.9178114223836));
#52484=CARTESIAN_POINT('Ctrl Pts',(4.68471823230415,3.61488637471462,41.8714202699096));
#52485=CARTESIAN_POINT('Ctrl Pts',(5.28660756810544,2.83486685183809,41.8250291174356));
#52486=CARTESIAN_POINT('Ctrl Pts',(5.68945515880915,1.90126001449041,41.7786379649616));
#52487=CARTESIAN_POINT('Ctrl Pts',(5.8440058273591,0.928215658116778,41.7322468124877));
#52488=CARTESIAN_POINT('Ctrl Pts',(5.99855649590908,-0.0448286982570238,
41.6858556600137));
#52489=CARTESIAN_POINT('Ctrl Pts',(5.90481024230533,-1.05731057365682,41.6394645075397));
#52490=CARTESIAN_POINT('Ctrl Pts',(5.57422918876514,-1.98543631710994,41.5930733550657));
#52491=CARTESIAN_POINT('Ctrl Pts',(5.24364813522496,-2.91356206056301,41.5466822025917));
#52492=CARTESIAN_POINT('Ctrl Pts',(4.67623228174835,-3.75733167206929,41.5002910501177));
#52493=CARTESIAN_POINT('Ctrl Pts',(3.94135815924267,-4.41357953125936,41.4538998976437));
#52494=CARTESIAN_POINT('Ctrl Pts',(3.20648403673703,-5.06982739044939,41.4075087451697));
#52495=CARTESIAN_POINT('Ctrl Pts',(2.30415164520231,-5.53855349732326,41.3611175926957));
#52496=CARTESIAN_POINT('Ctrl Pts',(1.34468693106113,-5.76244787183483,41.3147264402218));
#52497=CARTESIAN_POINT('Ctrl Pts',(0.385222216919947,-5.98634224634639,
41.2683352877478));
#52498=CARTESIAN_POINT('Ctrl Pts',(-0.63137481982772,-5.96540488849565,
41.2219441352738));
#52499=CARTESIAN_POINT('Ctrl Pts',(-1.58080737762424,-5.70219575716487,
41.1755529827998));
#52500=CARTESIAN_POINT('Ctrl Pts',(-2.5302399354207,-5.43898662583412,41.1291618303258));
#52501=CARTESIAN_POINT('Ctrl Pts',(-3.41250801426605,-4.93350572102335,
41.0827706778519));
#52502=CARTESIAN_POINT('Ctrl Pts',(-4.11973888155062,-4.24755694088029,
41.0363795253779));
#52503=CARTESIAN_POINT('Ctrl Pts',(-4.82696974883531,-3.56160816073712,
40.9899883729039));
#52504=CARTESIAN_POINT('Ctrl Pts',(-5.35916340455918,-2.69519150526158,
40.9435972204299));
#52505=CARTESIAN_POINT('Ctrl Pts',(-5.6512498486882,-1.75424159279215,40.8972060679559));
#52506=CARTESIAN_POINT('Ctrl Pts',(-5.82718758034986,-1.18746214604047,
40.8692624427056));
#52507=CARTESIAN_POINT('Ctrl Pts',(-5.91600882025632,-0.593640296750067,
40.8413188174552));
#52508=CARTESIAN_POINT('Ctrl Pts',(-5.9163246276023,8.91563840094145E-5,
40.8133751922049));
#52509=CARTESIAN_POINT('Ctrl Pts',(-5.91626344896283,4.86828180632854E-5,
40.5616248077952));
#52510=CARTESIAN_POINT('Ctrl Pts',(-5.91610702193196,-0.545492816832468,
40.5872997276001));
#52511=CARTESIAN_POINT('Ctrl Pts',(-5.84130698505393,-1.09107635134332,
40.6129746474051));
#52512=CARTESIAN_POINT('Ctrl Pts',(-5.69242609675824,-1.61563413162986,
40.63864956721));
#52513=CARTESIAN_POINT('Ctrl Pts',(-5.42341820727474,-2.56344001190361,
40.685040719684));
#52514=CARTESIAN_POINT('Ctrl Pts',(-4.91255363229728,-3.44260171315683,
40.731431872158));
#52515=CARTESIAN_POINT('Ctrl Pts',(-4.22229451798941,-4.14562631187354,
40.777823024632));
#52516=CARTESIAN_POINT('Ctrl Pts',(-3.53203540368151,-4.84865091059029,
40.824214177106));
#52517=CARTESIAN_POINT('Ctrl Pts',(-2.66238175004321,-5.37553840677047,
40.8706053295799));
#52518=CARTESIAN_POINT('Ctrl Pts',(-1.71966395516019,-5.6618675713641,40.9169964820539));
#52519=CARTESIAN_POINT('Ctrl Pts',(-0.776946160277282,-5.94819673595769,
40.9633876345279));
#52520=CARTESIAN_POINT('Ctrl Pts',(0.238835775850449,-5.99396756896476,
41.0097787870019));
#52521=CARTESIAN_POINT('Ctrl Pts',(1.20348471199892,-5.79358378400852,41.0561699394759));
#52522=CARTESIAN_POINT('Ctrl Pts',(2.16813364814744,-5.59319999905228,41.1025610919499));
#52523=CARTESIAN_POINT('Ctrl Pts',(3.08164958431682,-5.14666159613273,41.1489522444239));
#52524=CARTESIAN_POINT('Ctrl Pts',(3.83233918978381,-4.50856571969277,41.1953433968978));
#52525=CARTESIAN_POINT('Ctrl Pts',(4.58302879525085,-3.87046984325278,41.2417345493718));
#52526=CARTESIAN_POINT('Ctrl Pts',(5.17089207001545,-3.04081649329238,41.2881257018459));
#52527=CARTESIAN_POINT('Ctrl Pts',(5.52405242761798,-2.12104532984789,41.3345168543198));
#52528=CARTESIAN_POINT('Ctrl Pts',(5.87721278522047,-1.20127416640351,41.3809080067938));
#52529=CARTESIAN_POINT('Ctrl Pts',(5.99567022566093,-0.191385189475094,
41.4272991592678));
#52530=CARTESIAN_POINT('Ctrl Pts',(5.8649412511175,0.785144977237938,41.4736903117417));
#52531=CARTESIAN_POINT('Ctrl Pts',(5.73421227657406,1.76167514395103,41.5200814642157));
#52532=CARTESIAN_POINT('Ctrl Pts',(5.3542968870467,2.70484650044868,41.5664726166897));
#52533=CARTESIAN_POINT('Ctrl Pts',(4.77164639615703,3.49933982122104,41.6128637691637));
#52534=CARTESIAN_POINT('Ctrl Pts',(4.18899590526738,4.29383314199335,41.6592549216377));
#52535=CARTESIAN_POINT('Ctrl Pts',(3.40361031301533,4.93964842704044,41.7056460741117));
#52536=CARTESIAN_POINT('Ctrl Pts',(2.51151677035428,5.35782344115321,41.7520372265857));
#52537=CARTESIAN_POINT('Ctrl Pts',(1.61942322769312,5.77599845526603,41.7984283790596));
#52538=CARTESIAN_POINT('Ctrl Pts',(0.620621734623047,5.96653319844456,41.8448195315337));
#52539=CARTESIAN_POINT('Ctrl Pts',(-0.362766724344341,5.90613145959774,
41.8912106840076));
#52540=CARTESIAN_POINT('Ctrl Pts',(-1.34615518331167,5.84572972075092,41.9376018364816));
#52541=CARTESIAN_POINT('Ctrl Pts',(-2.31413060817627,5.53439149987867,41.9839929889556));
#52542=CARTESIAN_POINT('Ctrl Pts',(-3.14834104142876,5.01018335005785,42.0303841414296));
#52543=CARTESIAN_POINT('Ctrl Pts',(-3.9825514746812,4.48597520023706,42.0767752939036));
#52544=CARTESIAN_POINT('Ctrl Pts',(-4.68299691632168,3.74889712146773,42.1231664463775));
#52545=CARTESIAN_POINT('Ctrl Pts',(-5.16403563721432,2.88906982468789,42.1695575988515));
#52546=CARTESIAN_POINT('Ctrl Pts',(-5.64507435810699,2.029242527908,42.2159487513255));
#52547=CARTESIAN_POINT('Ctrl Pts',(-5.90670635825177,1.04666601311763,42.2623399037995));
#52548=CARTESIAN_POINT('Ctrl Pts',(-5.91694254105722,0.0614774769239503,
42.3087310562735));
#52549=CARTESIAN_POINT('Ctrl Pts',(-5.91715537596208,0.0409930334200531,
42.3096956401141));
#52550=CARTESIAN_POINT('Ctrl Pts',(-5.91725952634774,0.0205074606758483,
42.3106602239546));
#52551=CARTESIAN_POINT('Ctrl Pts',(-5.91725525726564,2.18443538467081E-5,
42.3116248077952));
#52552=CARTESIAN_POINT('Origin',(0.,0.,0.));
#52553=CARTESIAN_POINT('',(-5.91625748489978,-4.2193274442659E-5,44.3133751922049));
#52554=CARTESIAN_POINT('',(-5.91631318557293,-8.34923490093236E-5,44.0616248077952));
#52555=CARTESIAN_POINT('',(-5.91675,-7.2459289488551E-16,0.));
#52556=CARTESIAN_POINT('Ctrl Pts',(-5.91625748489978,-4.2193274442659E-5,
44.3133751922049));
#52557=CARTESIAN_POINT('Ctrl Pts',(-5.91612386542984,0.538286346723986,
44.2880398101642));
#52558=CARTESIAN_POINT('Ctrl Pts',(-5.84331471980756,1.07665031667677,44.2627044281235));
#52559=CARTESIAN_POINT('Ctrl Pts',(-5.69829673740849,1.59480491302855,44.2373690460828));
#52560=CARTESIAN_POINT('Ctrl Pts',(-5.43275697478975,2.54358827243592,44.1909778936088));
#52561=CARTESIAN_POINT('Ctrl Pts',(-4.92511109810911,3.42461243326639,44.1445867411348));
#52562=CARTESIAN_POINT('Ctrl Pts',(-4.23742771126215,4.13015675368477,44.0981955886608));
#52563=CARTESIAN_POINT('Ctrl Pts',(-3.54974432441519,4.83570107410316,44.0518044361868));
#52564=CARTESIAN_POINT('Ctrl Pts',(-2.68202342740191,5.36576555410946,44.0054132837129));
#52565=CARTESIAN_POINT('Ctrl Pts',(-1.74035910494293,5.65554052271067,43.9590221312389));
#52566=CARTESIAN_POINT('Ctrl Pts',(-0.798694782483963,5.94531549131189,
43.9126309787649));
#52567=CARTESIAN_POINT('Ctrl Pts',(0.216912965420696,5.99480094850802,43.8662398262909));
#52568=CARTESIAN_POINT('Ctrl Pts',(1.18228829510979,5.79794643002389,43.8198486738169));
#52569=CARTESIAN_POINT('Ctrl Pts',(2.14766362479889,5.60109191153975,43.7734575213429));
#52570=CARTESIAN_POINT('Ctrl Pts',(3.06280653627241,5.15789741737534,43.727066368869));
#52571=CARTESIAN_POINT('Ctrl Pts',(3.8158247725667,4.522551240533,43.680675216395));
#52572=CARTESIAN_POINT('Ctrl Pts',(4.568843008861,3.88720506369065,43.634284063921));
#52573=CARTESIAN_POINT('Ctrl Pts',(5.15973656997605,3.05970720417037,43.587892911447));
#52574=CARTESIAN_POINT('Ctrl Pts',(5.51625836384621,2.14123377553155,43.541501758973));
#52575=CARTESIAN_POINT('Ctrl Pts',(5.87278015771636,1.22276034689272,43.495110606499));
#52576=CARTESIAN_POINT('Ctrl Pts',(5.99493018434163,0.213311349135362,43.448719454025));
#52577=CARTESIAN_POINT('Ctrl Pts',(5.8677734625339,-0.763690389204473,43.4023283015511));
#52578=CARTESIAN_POINT('Ctrl Pts',(5.74061674072617,-1.74069212754431,43.3559371490771));
#52579=CARTESIAN_POINT('Ctrl Pts',(5.36415327048545,-2.68524660646662,43.3095459966031));
#52580=CARTESIAN_POINT('Ctrl Pts',(4.78441230781263,-3.48186548950865,43.2631548441291));
#52581=CARTESIAN_POINT('Ctrl Pts',(4.20467134513981,-4.27848437255069,43.2167636916552));
#52582=CARTESIAN_POINT('Ctrl Pts',(3.42165289003488,-4.92716765971245,43.1703725391812));
#52583=CARTESIAN_POINT('Ctrl Pts',(2.53109466945551,-5.34860245227052,43.1239813867072));
#52584=CARTESIAN_POINT('Ctrl Pts',(1.64053644887615,-5.77003724482859,43.0775902342332));
#52585=CARTESIAN_POINT('Ctrl Pts',(0.642438462822346,-5.96422354278298,
43.0311990817592));
#52586=CARTESIAN_POINT('Ctrl Pts',(-0.34116432025421,-5.90741866848506,
42.9848079292852));
#52587=CARTESIAN_POINT('Ctrl Pts',(-1.32476710333077,-5.85061379418714,
42.9384167768112));
#52588=CARTESIAN_POINT('Ctrl Pts',(-2.29387468343007,-5.54281774763692,
42.8920256243373));
#52589=CARTESIAN_POINT('Ctrl Pts',(-3.12999667722686,-5.02166398903084,
42.8456344718633));
#52590=CARTESIAN_POINT('Ctrl Pts',(-3.96611867102364,-4.50051023042476,
42.7992433193893));
#52591=CARTESIAN_POINT('Ctrl Pts',(-4.6692550785179,-3.76599875976282,42.7528521669153));
#52592=CARTESIAN_POINT('Ctrl Pts',(-5.15343515284433,-2.90793647516735,
42.7064610144413));
#52593=CARTESIAN_POINT('Ctrl Pts',(-5.63761522717078,-2.04987419057183,
42.6600698619673));
#52594=CARTESIAN_POINT('Ctrl Pts',(-5.90283896832939,-1.06826109204276,
42.6136787094933));
#52595=CARTESIAN_POINT('Ctrl Pts',(-5.91667812645172,-0.0831165816674949,
42.5672875570194));
#52596=CARTESIAN_POINT('Ctrl Pts',(-5.91706716496741,-0.0554227613734876,
42.5659834354146));
#52597=CARTESIAN_POINT('Ctrl Pts',(-5.91725754619806,-0.0277261503725831,
42.5646793138097));
#52598=CARTESIAN_POINT('Ctrl Pts',(-5.9172499153618,-2.94340949030803E-5,
42.5633751922049));
#52599=CARTESIAN_POINT('Ctrl Pts',(-5.91725525726564,2.18443538467081E-5,
42.3116248077952));
#52600=CARTESIAN_POINT('Ctrl Pts',(-5.9170542070895,-0.96473748158776,42.3570513764286));
#52601=CARTESIAN_POINT('Ctrl Pts',(-5.67639075946303,-1.92959345826523,
42.402477945062));
#52602=CARTESIAN_POINT('Ctrl Pts',(-5.22294962861403,-2.78114826848592,
42.4479045136954));
#52603=CARTESIAN_POINT('Ctrl Pts',(-4.75988016789937,-3.65078492010495,
42.4942956661694));
#52604=CARTESIAN_POINT('Ctrl Pts',(-4.07490088100393,-4.40225766574615,
42.5406868186434));
#52605=CARTESIAN_POINT('Ctrl Pts',(-3.25176248863289,-4.94368579420877,
42.5870779711174));
#52606=CARTESIAN_POINT('Ctrl Pts',(-2.42862409626176,-5.48511392267146,
42.6334691235913));
#52607=CARTESIAN_POINT('Ctrl Pts',(-1.46732659841493,-5.81649743395556,
42.6798602760653));
#52608=CARTESIAN_POINT('Ctrl Pts',(-0.485405459006441,-5.89731888697808,
42.7262514285393));
#52609=CARTESIAN_POINT('Ctrl Pts',(0.496515680401994,-5.97814034000059,
42.7726425810133));
#52610=CARTESIAN_POINT('Ctrl Pts',(1.49906046137198,-5.8083997347616,42.8190337334873));
#52611=CARTESIAN_POINT('Ctrl Pts',(2.3996502168525,-5.40885083461371,42.8654248859613));
#52612=CARTESIAN_POINT('Ctrl Pts',(3.30023997233296,-5.00930193446583,42.9118160384352));
#52613=CARTESIAN_POINT('Ctrl Pts',(4.09887470232382,-4.37994473940907,42.9582071909092));
#52614=CARTESIAN_POINT('Ctrl Pts',(4.69790731661882,-3.59772919475618,43.0045983433832));
#52615=CARTESIAN_POINT('Ctrl Pts',(5.2969399309139,-2.81551365010321,43.0509894958572));
#52616=CARTESIAN_POINT('Ctrl Pts',(5.69637042951309,-1.88043975585402,43.0973806483312));
#52617=CARTESIAN_POINT('Ctrl Pts',(5.84736143474778,-0.906836680867013,
43.1437718008052));
#52618=CARTESIAN_POINT('Ctrl Pts',(5.99835243998247,0.0667663941199431,
43.1901629532792));
#52619=CARTESIAN_POINT('Ctrl Pts',(5.90090395185268,1.07889864984477,43.2365541057531));
#52620=CARTESIAN_POINT('Ctrl Pts',(5.56693075562074,2.00580918246615,43.2829452582271));
#52621=CARTESIAN_POINT('Ctrl Pts',(5.2329575593888,2.93271971508754,43.3293364107011));
#52622=CARTESIAN_POINT('Ctrl Pts',(4.66245965505468,3.77440852460552,43.3757275631751));
#52623=CARTESIAN_POINT('Ctrl Pts',(3.92519040824982,4.42796440515563,43.4221187156491));
#52624=CARTESIAN_POINT('Ctrl Pts',(3.18792116144496,5.08152028570573,43.4685098681231));
#52625=CARTESIAN_POINT('Ctrl Pts',(2.28388057216931,5.546943237288,43.5149010205971));
#52626=CARTESIAN_POINT('Ctrl Pts',(1.32360344395206,5.7673271484718,43.561292173071));
#52627=CARTESIAN_POINT('Ctrl Pts',(0.363326315734754,5.98771105965562,43.607683325545));
#52628=CARTESIAN_POINT('Ctrl Pts',(-0.653187351424031,5.96305593044097,
43.654074478019));
#52629=CARTESIAN_POINT('Ctrl Pts',(-1.60165094936008,5.69637628240582,43.700465630493));
#52630=CARTESIAN_POINT('Ctrl Pts',(-2.55011454729602,5.4296966343707,43.746856782967));
#52631=CARTESIAN_POINT('Ctrl Pts',(-3.43052807600912,4.92099246751511,43.793247935441));
#52632=CARTESIAN_POINT('Ctrl Pts',(-4.13524555414061,4.23246178025295,43.839639087915));
#52633=CARTESIAN_POINT('Ctrl Pts',(-4.83996303227218,3.5439310929907,43.8860302403889));
#52634=CARTESIAN_POINT('Ctrl Pts',(-5.36898445982214,2.67557388532179,43.9324213928629));
#52635=CARTESIAN_POINT('Ctrl Pts',(-5.65762769723763,1.73356204209462,43.9788125453369));
#52636=CARTESIAN_POINT('Ctrl Pts',(-5.82937883410267,1.17303754665422,44.006416632823));
#52637=CARTESIAN_POINT('Ctrl Pts',(-5.91602174695989,0.58643491484543,44.0340207203091));
#52638=CARTESIAN_POINT('Ctrl Pts',(-5.91631318557293,-8.34923490093236E-5,
44.0616248077952));
#52639=CARTESIAN_POINT('Origin',(0.,0.,0.));
#52640=CARTESIAN_POINT('',(-5.91708074246689,0.000111828887577881,46.0633751922049));
#52641=CARTESIAN_POINT('',(-5.9169414605903,0.000139691133403882,45.8116248077952));
#52642=CARTESIAN_POINT('',(-5.91675,-7.2459289488551E-16,0.));
#52643=CARTESIAN_POINT('Ctrl Pts',(-5.91708074246689,0.000111828887577881,
46.0633751922049));
#52644=CARTESIAN_POINT('Ctrl Pts',(-5.91718319560474,0.118708057921104,
46.0577914589927));
#52645=CARTESIAN_POINT('Ctrl Pts',(-5.91369093890245,0.237298258279482,
46.0522077257804));
#52646=CARTESIAN_POINT('Ctrl Pts',(-5.90656309521846,0.355669538172284,
46.0466239925682));
#52647=CARTESIAN_POINT('Ctrl Pts',(-5.84734305898366,1.33912986575459,46.0002328400942));
#52648=CARTESIAN_POINT('Ctrl Pts',(-5.53716820162539,2.307478700597,45.9538416876202));
#52649=CARTESIAN_POINT('Ctrl Pts',(-5.01396283464526,3.14231842927739,45.9074505351462));
#52650=CARTESIAN_POINT('Ctrl Pts',(-4.49075746766513,3.97715815795778,45.8610593826722));
#52651=CARTESIAN_POINT('Ctrl Pts',(-3.75452159106314,4.67848878047613,45.8146682301982));
#52652=CARTESIAN_POINT('Ctrl Pts',(-2.89527294180451,5.1605603388232,45.7682770777242));
#52653=CARTESIAN_POINT('Ctrl Pts',(-2.03602429254593,5.64263189717024,45.7218859252502));
#52654=CARTESIAN_POINT('Ctrl Pts',(-1.05376287063074,5.90544439134602,45.6754947727763));
#52655=CARTESIAN_POINT('Ctrl Pts',(-0.06858734704076,5.91686438867803,45.6291036203023));
#52656=CARTESIAN_POINT('Ctrl Pts',(0.916588176549275,5.92828438601003,45.5827124678283));
#52657=CARTESIAN_POINT('Ctrl Pts',(1.90467780181407,5.68831188649823,45.5363213153544));
#52658=CARTESIAN_POINT('Ctrl Pts',(2.77487025778479,5.22628773324257,45.4899301628804));
#52659=CARTESIAN_POINT('Ctrl Pts',(3.64506271375556,4.76426357998688,45.4435390104064));
#52660=CARTESIAN_POINT('Ctrl Pts',(4.3973580004322,4.08018777298733,45.3971478579324));
#52661=CARTESIAN_POINT('Ctrl Pts',(4.93977483655907,3.25770056670009,45.3507567054584));
#52662=CARTESIAN_POINT('Ctrl Pts',(5.48219167268588,2.43521336041294,45.3043655529844));
#52663=CARTESIAN_POINT('Ctrl Pts',(5.81473005826294,1.47431475483818,45.2579744005104));
#52664=CARTESIAN_POINT('Ctrl Pts',(5.89673134858815,0.492491442319647,45.2115832480365));
#52665=CARTESIAN_POINT('Ctrl Pts',(5.97873263891336,-0.489331870198937,
45.1651920955625));
#52666=CARTESIAN_POINT('Ctrl Pts',(5.81019683398663,-1.4920798896614,45.1188009430885));
#52667=CARTESIAN_POINT('Ctrl Pts',(5.41173038921079,-2.39314909954912,45.0724097906145));
#52668=CARTESIAN_POINT('Ctrl Pts',(5.01326394443495,-3.29421830943683,45.0260186381405));
#52669=CARTESIAN_POINT('Ctrl Pts',(4.38486685980999,-4.09360870974991,44.9796274856665));
#52670=CARTESIAN_POINT('Ctrl Pts',(3.60337169032434,-4.69358081634368,44.9332363331926));
#52671=CARTESIAN_POINT('Ctrl Pts',(2.8218765208387,-5.29355292293745,44.8868451807186));
#52672=CARTESIAN_POINT('Ctrl Pts',(1.88728326649239,-5.69410673581187,44.8404540282446));
#52673=CARTESIAN_POINT('Ctrl Pts',(0.913862329493332,-5.84626753244438,
44.7940628757706));
#52674=CARTESIAN_POINT('Ctrl Pts',(-0.0595586075057249,-5.9984283290769,
44.7476717232966));
#52675=CARTESIAN_POINT('Ctrl Pts',(-1.07180722715749,-5.9021961094675,44.7012805708226));
#52676=CARTESIAN_POINT('Ctrl Pts',(-1.99911839809162,-5.56933694873922,
44.6548894183486));
#52677=CARTESIAN_POINT('Ctrl Pts',(-2.92642956902575,-5.23647778801094,
44.6084982658746));
#52678=CARTESIAN_POINT('Ctrl Pts',(-3.76880329124222,-4.66699168616381,
44.5621071134007));
#52679=CARTESIAN_POINT('Ctrl Pts',(-4.42324461629749,-3.93050829824535,
44.5157159609267));
#52680=CARTESIAN_POINT('Ctrl Pts',(-5.07768594135277,-3.19402491032689,
44.4693248084527));
#52681=CARTESIAN_POINT('Ctrl Pts',(-5.54419486924684,-2.29054423633713,
44.4229336559787));
#52682=CARTESIAN_POINT('Ctrl Pts',(-5.76573250891546,-1.33053262035011,
44.3765425035047));
#52683=CARTESIAN_POINT('Ctrl Pts',(-5.8662828387614,-0.8948076357027,44.3554867330715));
#52684=CARTESIAN_POINT('Ctrl Pts',(-5.91636853358576,-0.447437150164224,
44.3344309626382));
#52685=CARTESIAN_POINT('Ctrl Pts',(-5.91625748489978,-4.2193274442659E-5,
44.3133751922049));
#52686=CARTESIAN_POINT('Ctrl Pts',(-5.91631318557293,-8.34923490093236E-5,
44.0616248077952));
#52687=CARTESIAN_POINT('Ctrl Pts',(-5.91651153576893,-0.399262035675468,
44.0804118727831));
#52688=CARTESIAN_POINT('Ctrl Pts',(-5.87671164968556,-0.798401565932907,
44.099198937771));
#52689=CARTESIAN_POINT('Ctrl Pts',(-5.79652159130293,-1.18925436972102,
44.1179860027589));
#52690=CARTESIAN_POINT('Ctrl Pts',(-5.59850720067171,-2.15439245952413,
44.1643771552329));
#52691=CARTESIAN_POINT('Ctrl Pts',(-5.15421337212823,-3.06900216034495,
44.2107683077068));
#52692=CARTESIAN_POINT('Ctrl Pts',(-4.51796281156627,-3.82125640956555,
44.2571594601808));
#52693=CARTESIAN_POINT('Ctrl Pts',(-3.88171225100428,-4.57351065878619,
44.3035506126548));
#52694=CARTESIAN_POINT('Ctrl Pts',(-3.05350495842378,-5.16340945640659,
44.3499417651288));
#52695=CARTESIAN_POINT('Ctrl Pts',(-2.1346037880072,-5.51882733762952,44.3963329176028));
#52696=CARTESIAN_POINT('Ctrl Pts',(-1.21570261759073,-5.87424521885241,
44.4427240700767));
#52697=CARTESIAN_POINT('Ctrl Pts',(-0.206107569338182,-5.99518218367789,
44.4891152225507));
#52698=CARTESIAN_POINT('Ctrl Pts',(0.770740670982104,-5.86685156897937,
44.5355063750247));
#52699=CARTESIAN_POINT('Ctrl Pts',(1.7475889113025,-5.73852095428082,44.5818975274987));
#52700=CARTESIAN_POINT('Ctrl Pts',(2.69169034369063,-5.36092276005821,44.6282886799727));
#52701=CARTESIAN_POINT('Ctrl Pts',(3.48761202456127,-4.78022498220296,44.6746798324467));
#52702=CARTESIAN_POINT('Ctrl Pts',(4.2835337054319,-4.1995272043477,44.7210709849206));
#52703=CARTESIAN_POINT('Ctrl Pts',(4.93127563478503,-3.41572984285981,44.7674621373946));
#52704=CARTESIAN_POINT('Ctrl Pts',(5.35164001138475,-2.52466585965103,44.8138532898686));
#52705=CARTESIAN_POINT('Ctrl Pts',(5.77200438798442,-1.63360187644235,44.8602444423426));
#52706=CARTESIAN_POINT('Ctrl Pts',(5.96499121183073,-0.635271271512821,
44.9066355948166));
#52707=CARTESIAN_POINT('Ctrl Pts',(5.90700446200314,0.348262544952162,44.9530267472906));
#52708=CARTESIAN_POINT('Ctrl Pts',(5.84901771217555,1.3317963614172,44.9994178997646));
#52709=CARTESIAN_POINT('Ctrl Pts',(5.54005738867404,2.30053338941769,45.0458090522385));
#52710=CARTESIAN_POINT('Ctrl Pts',(5.01789930495395,3.1360285521156,45.0922002047125));
#52711=CARTESIAN_POINT('Ctrl Pts',(4.49574122123386,3.97152371481352,45.1385913571865));
#52712=CARTESIAN_POINT('Ctrl Pts',(3.76038537729519,4.67377701220886,45.1849825096605));
#52713=CARTESIAN_POINT('Ctrl Pts',(2.90174191068929,5.15692567312065,45.2313736621345));
#52714=CARTESIAN_POINT('Ctrl Pts',(2.04309844408339,5.64007433403244,45.2777648146084));
#52715=CARTESIAN_POINT('Ctrl Pts',(1.06116735481026,5.90411835846068,45.3241559670825));
#52716=CARTESIAN_POINT('Ctrl Pts',(0.0760069248978496,5.91677373757939,
45.3705471195564));
#52717=CARTESIAN_POINT('Ctrl Pts',(-0.909153505014565,5.9294291166981,45.4169382720304));
#52718=CARTESIAN_POINT('Ctrl Pts',(-1.89754327556627,5.69069585050728,45.4633294245044));
#52719=CARTESIAN_POINT('Ctrl Pts',(-2.76831441776762,5.22976326411833,45.5097205769784));
#52720=CARTESIAN_POINT('Ctrl Pts',(-3.63908555996897,4.76883067772938,45.5561117294523));
#52721=CARTESIAN_POINT('Ctrl Pts',(-4.39223807381997,4.0856987711423,45.6025028819263));
#52722=CARTESIAN_POINT('Ctrl Pts',(-4.93568586702171,3.26389239044791,45.6488940344003));
#52723=CARTESIAN_POINT('Ctrl Pts',(-5.47913366022345,2.44208600975352,45.6952851868743));
#52724=CARTESIAN_POINT('Ctrl Pts',(-5.81287673277592,1.48160515495182,45.7416763393483));
#52725=CARTESIAN_POINT('Ctrl Pts',(-5.89610914588454,0.499885441034465,
45.7880674918223));
#52726=CARTESIAN_POINT('Ctrl Pts',(-5.91019755247519,0.333713802232241,
45.7959199304799));
#52727=CARTESIAN_POINT('Ctrl Pts',(-5.91710859473939,0.166933650282954,
45.8037723691375));
#52728=CARTESIAN_POINT('Ctrl Pts',(-5.9169414605903,0.000139691133403882,
45.8116248077952));
#52729=CARTESIAN_POINT('Origin',(0.,0.,0.));
#52730=CARTESIAN_POINT('',(-5.9165283748373,-0.000142876380609669,47.8133751922049));
#52731=CARTESIAN_POINT('',(-5.91667009430184,-0.00015435290976692,47.5616248077952));
#52732=CARTESIAN_POINT('',(-5.91675,-7.2459289488551E-16,0.));
#52733=CARTESIAN_POINT('Ctrl Pts',(-5.9165283748373,-0.000142876380609669,
47.8133751922049));
#52734=CARTESIAN_POINT('Ctrl Pts',(-5.91591637761327,0.684449648370852,
47.7811519553471));
#52735=CARTESIAN_POINT('Ctrl Pts',(-5.79719566143619,1.36924892251219,47.7489287184894));
#52736=CARTESIAN_POINT('Ctrl Pts',(-5.56441112577014,2.01278842444649,47.7167054816317));
#52737=CARTESIAN_POINT('Ctrl Pts',(-5.22927586498499,2.93927943120176,47.6703143291577));
#52738=CARTESIAN_POINT('Ctrl Pts',(-4.65772294875219,3.78025218463893,47.6239231766836));
#52739=CARTESIAN_POINT('Ctrl Pts',(-3.91963473639474,4.43288302929686,47.5775320242096));
#52740=CARTESIAN_POINT('Ctrl Pts',(-3.18154652403728,5.08551387395478,47.5311408717356));
#52741=CARTESIAN_POINT('Ctrl Pts',(-2.27692301555514,5.54980280983347,47.4847497192617));
#52742=CARTESIAN_POINT('Ctrl Pts',(-1.31637028656497,5.76898237879343,47.4383585667877));
#52743=CARTESIAN_POINT('Ctrl Pts',(-0.355817557574798,5.98816194775339,
47.3919674143137));
#52744=CARTESIAN_POINT('Ctrl Pts',(0.660664391923433,5.96223214979463,47.3455762618397));
#52745=CARTESIAN_POINT('Ctrl Pts',(1.608792831805,5.69436335708507,47.2991851093657));
#52746=CARTESIAN_POINT('Ctrl Pts',(2.55692127168663,5.4264945643755,47.2527939568917));
#52747=CARTESIAN_POINT('Ctrl Pts',(3.43669620195162,4.91668677691509,47.2064028044177));
#52748=CARTESIAN_POINT('Ctrl Pts',(4.14054972109162,4.22727293007542,47.1600116519438));
#52749=CARTESIAN_POINT('Ctrl Pts',(4.84440324023159,3.53785908323578,47.1136204994698));
#52750=CARTESIAN_POINT('Ctrl Pts',(5.37233534824662,2.66883917701688,47.0672293469958));
#52751=CARTESIAN_POINT('Ctrl Pts',(5.65979709398515,1.72646612277727,47.0208381945218));
#52752=CARTESIAN_POINT('Ctrl Pts',(5.94725883972366,0.784093068537711,46.9744470420478));
#52753=CARTESIAN_POINT('Ctrl Pts',(5.99425022318572,-0.231633133722414,
46.9280558895739));
#52754=CARTESIAN_POINT('Ctrl Pts',(5.79502572431377,-1.19652215722151,46.8816647370999));
#52755=CARTESIAN_POINT('Ctrl Pts',(5.59580122544179,-2.16141118072072,46.8352735846259));
#52756=CARTESIAN_POINT('Ctrl Pts',(5.15036084423571,-3.07546302545876,46.7888824321519));
#52757=CARTESIAN_POINT('Ctrl Pts',(4.51316747274337,-3.82691883649908,46.7424912796779));
#52758=CARTESIAN_POINT('Ctrl Pts',(3.87597410125107,-4.57837464753936,46.6961001272039));
#52759=CARTESIAN_POINT('Ctrl Pts',(3.0470277394725,-5.16723442488198,46.64970897473));
#52760=CARTESIAN_POINT('Ctrl Pts',(2.12768160575026,-5.52149974216538,46.603317822256));
#52761=CARTESIAN_POINT('Ctrl Pts',(1.20833547202802,-5.87576505944878,46.556926669782));
#52762=CARTESIAN_POINT('Ctrl Pts',(0.19858956636208,-5.99543591667298,46.510535517308));
#52763=CARTESIAN_POINT('Ctrl Pts',(-0.778096980516938,-5.86588045455162,
46.464144364834));
#52764=CARTESIAN_POINT('Ctrl Pts',(-1.75478352739596,-5.73632499243026,
46.41775321236));
#52765=CARTESIAN_POINT('Ctrl Pts',(-2.69841071548808,-5.35754321096334,
46.3713620598861));
#52766=CARTESIAN_POINT('Ctrl Pts',(-3.49360358588342,-4.77584782032288,
46.3249709074121));
#52767=CARTESIAN_POINT('Ctrl Pts',(-4.28879645627876,-4.19415242968242,
46.2785797549381));
#52768=CARTESIAN_POINT('Ctrl Pts',(-4.93555500897735,-3.40954342986841,
46.2321886024641));
#52769=CARTESIAN_POINT('Ctrl Pts',(-5.35480167777096,-2.51795301980031,
46.1857974499901));
#52770=CARTESIAN_POINT('Ctrl Pts',(-5.72358696710265,-1.73367624000276,
46.1449900307284));
#52771=CARTESIAN_POINT('Ctrl Pts',(-5.91633198746874,-0.866621207429096,
46.1041826114666));
#52772=CARTESIAN_POINT('Ctrl Pts',(-5.91708074246689,0.000111828887577881,
46.0633751922049));
#52773=CARTESIAN_POINT('Ctrl Pts',(-5.9169414605903,0.000139691133403882,
45.8116248077952));
#52774=CARTESIAN_POINT('Ctrl Pts',(-5.91612118864406,-0.818462648626552,
45.8501635216115));
#52775=CARTESIAN_POINT('Ctrl Pts',(-5.74480785464818,-1.63739756442216,
45.8887022354279));
#52776=CARTESIAN_POINT('Ctrl Pts',(-5.41472710370765,-2.38636101768265,
45.9272409492443));
#52777=CARTESIAN_POINT('Ctrl Pts',(-5.01739089475736,-3.2879291894494,45.9736321017182));
#52778=CARTESIAN_POINT('Ctrl Pts',(-4.38999672319199,-4.08810695994993,
46.0200232541922));
#52779=CARTESIAN_POINT('Ctrl Pts',(-3.60925452030443,-4.689058575237,46.0664144066662));
#52780=CARTESIAN_POINT('Ctrl Pts',(-2.82851231741688,-5.29001019052406,
46.1128055591401));
#52781=CARTESIAN_POINT('Ctrl Pts',(-1.89442208320712,-5.69173565059769,
46.1591967116142));
#52782=CARTESIAN_POINT('Ctrl Pts',(-0.921192716857027,-5.84511697853441,
46.2055878640882));
#52783=CARTESIAN_POINT('Ctrl Pts',(0.0520366494930682,-5.99849830647113,
46.2519790165621));
#52784=CARTESIAN_POINT('Ctrl Pts',(1.06440514798353,-5.90353550227096,46.2983701690361));
#52785=CARTESIAN_POINT('Ctrl Pts',(1.99213298995529,-5.57183943277922,46.3447613215101));
#52786=CARTESIAN_POINT('Ctrl Pts',(2.91986083192704,-5.24014336328747,46.3911524739841));
#52787=CARTESIAN_POINT('Ctrl Pts',(3.76294801738013,-4.67171402850415,46.4375436264581));
#52788=CARTESIAN_POINT('Ctrl Pts',(4.41831236448827,-3.93605187518555,46.4839347789321));
#52789=CARTESIAN_POINT('Ctrl Pts',(5.07367671159642,-3.20038972186696,46.530325931406));
#52790=CARTESIAN_POINT('Ctrl Pts',(5.54131822035965,-2.29749475001306,46.57671708388));
#52791=CARTESIAN_POINT('Ctrl Pts',(5.76405952185625,-1.3377616913486,46.623108236354));
#52792=CARTESIAN_POINT('Ctrl Pts',(5.98680082335285,-0.378028632684144,
46.6694993888279));
#52793=CARTESIAN_POINT('Ctrl Pts',(5.96464191758284,0.638542512790754,46.715890541302));
#52794=CARTESIAN_POINT('Ctrl Pts',(5.70029211906678,1.58765810918055,46.762281693776));
#52795=CARTESIAN_POINT('Ctrl Pts',(5.43594232055071,2.53677370557039,46.8086728462499));
#52796=CARTESIAN_POINT('Ctrl Pts',(4.92940162928853,3.418433752875,46.8550639987239));
#52797=CARTESIAN_POINT('Ctrl Pts',(4.24260352089231,4.12483986099506,46.9014551511979));
#52798=CARTESIAN_POINT('Ctrl Pts',(3.55580541249617,4.83124596911503,46.9478463036719));
#52799=CARTESIAN_POINT('Ctrl Pts',(2.68874988696585,5.3623981380506,46.9942374561459));
#52800=CARTESIAN_POINT('Ctrl Pts',(1.74744967569917,5.6533537077774,47.0406286086199));
#52801=CARTESIAN_POINT('Ctrl Pts',(0.806149464432386,5.94430927750424,47.0870197610938));
#52802=CARTESIAN_POINT('Ctrl Pts',(-0.20939543257075,5.99506824802238,47.1334109135677));
#52803=CARTESIAN_POINT('Ctrl Pts',(-1.17501685627332,5.79942444573728,47.1798020660417));
#52804=CARTESIAN_POINT('Ctrl Pts',(-2.14063827997589,5.60378064345219,47.2261932185157));
#52805=CARTESIAN_POINT('Ctrl Pts',(-3.05633623037776,5.16173406836383,47.2725843709898));
#52806=CARTESIAN_POINT('Ctrl Pts',(-3.81015058728028,4.52733266025254,47.3189755234638));
#52807=CARTESIAN_POINT('Ctrl Pts',(-4.56396494418272,3.89293125214132,47.3653666759378));
#52808=CARTESIAN_POINT('Ctrl Pts',(-5.15589570758587,3.06617501100719,47.4117578284117));
#52809=CARTESIAN_POINT('Ctrl Pts',(-5.51356896926947,2.14814937456649,47.4581489808856));
#52810=CARTESIAN_POINT('Ctrl Pts',(-5.77949996790739,1.46559493053359,47.4926409231888));
#52811=CARTESIAN_POINT('Ctrl Pts',(-5.91593433074091,0.732587119768138,
47.527132865492));
#52812=CARTESIAN_POINT('Ctrl Pts',(-5.91667009430184,-0.00015435290976692,
47.5616248077952));
#52813=CARTESIAN_POINT('Origin',(0.,0.,0.));
#52814=CARTESIAN_POINT('',(-5.91663288208029,0.000152735557782668,49.5633751922049));
#52815=CARTESIAN_POINT('',(-5.91649558673351,0.000137928394543142,49.3116248077952));
#52816=CARTESIAN_POINT('',(-5.91675,-7.2459289488551E-16,0.));
#52817=CARTESIAN_POINT('Ctrl Pts',(-5.91663288208029,0.000152735557782668,
49.5633751922049));
#52818=CARTESIAN_POINT('Ctrl Pts',(-5.91689330738711,0.265102003771003,
49.5509036041756));
#52819=CARTESIAN_POINT('Ctrl Pts',(-5.89942583762255,0.530017195188502,
49.5384320161463));
#52820=CARTESIAN_POINT('Ctrl Pts',(-5.86395207547737,0.792498879926616,
49.525960428117));
#52821=CARTESIAN_POINT('Ctrl Pts',(-5.73199865425815,1.76886434595278,49.479569275643));
#52822=CARTESIAN_POINT('Ctrl Pts',(-5.35090084560841,2.71155855316966,49.433178123169));
#52823=CARTESIAN_POINT('Ctrl Pts',(-4.76725453460696,3.50532061592798,49.386786970695));
#52824=CARTESIAN_POINT('Ctrl Pts',(-4.18360822360548,4.29908267868635,49.340395818221));
#52825=CARTESIAN_POINT('Ctrl Pts',(-3.39741341025227,4.94391259698615,49.294004665747));
#52826=CARTESIAN_POINT('Ctrl Pts',(-2.50479618696016,5.36096861396988,49.2476135132731));
#52827=CARTESIAN_POINT('Ctrl Pts',(-1.61217896366814,5.77802463095356,49.2012223607991));
#52828=CARTESIAN_POINT('Ctrl Pts',(-0.613139330437237,5.96730674662122,
49.1548312083251));
#52829=CARTESIAN_POINT('Ctrl Pts',(0.370172611413013,5.9056719055447,49.1084400558511));
#52830=CARTESIAN_POINT('Ctrl Pts',(1.35348455326337,5.84403706446818,49.0620489033771));
#52831=CARTESIAN_POINT('Ctrl Pts',(2.32106880373308,5.53148526664742,49.0156577509031));
#52832=CARTESIAN_POINT('Ctrl Pts',(3.15462123323734,5.00623144620666,48.9692665984291));
#52833=CARTESIAN_POINT('Ctrl Pts',(3.98817366274155,4.48097762576594,48.9228754459552));
#52834=CARTESIAN_POINT('Ctrl Pts',(4.68769427128033,3.74302178270524,48.8764842934812));
#52835=CARTESIAN_POINT('Ctrl Pts',(5.16765440677028,2.88259195002832,48.8300931410072));
#52836=CARTESIAN_POINT('Ctrl Pts',(5.64761454226022,2.02216211735141,48.7837019885332));
#52837=CARTESIAN_POINT('Ctrl Pts',(5.90801420470134,1.03925829505829,48.7373108360592));
#52838=CARTESIAN_POINT('Ctrl Pts',(5.91701497238067,0.054057698833775,48.6909196835852));
#52839=CARTESIAN_POINT('Ctrl Pts',(5.92601574006001,-0.931142897390738,
48.6445285311112));
#52840=CARTESIAN_POINT('Ctrl Pts',(5.68361761297757,-1.91864026754664,48.5981373786373));
#52841=CARTESIAN_POINT('Ctrl Pts',(5.21945800970806,-2.78769555423019,48.5517462261633));
#52842=CARTESIAN_POINT('Ctrl Pts',(4.75529840643854,-3.65675084091374,48.5053550736894));
#52843=CARTESIAN_POINT('Ctrl Pts',(4.06937732698195,-4.40736404412495,48.4589639212153));
#52844=CARTESIAN_POINT('Ctrl Pts',(3.24556064268704,-4.94775954678693,48.4125727687413));
#52845=CARTESIAN_POINT('Ctrl Pts',(2.42174395839217,-5.48815504944887,48.3661816162673));
#52846=CARTESIAN_POINT('Ctrl Pts',(1.460031669259,-5.8183328515616,48.3197904637934));
#52847=CARTESIAN_POINT('Ctrl Pts',(0.4780099547046,-5.89792293111597,48.2733993113195));
#52848=CARTESIAN_POINT('Ctrl Pts',(-0.504011759849913,-5.97751301067036,
48.2270081588455));
#52849=CARTESIAN_POINT('Ctrl Pts',(-1.50634289982566,-5.80651536766633,
48.1806170063714));
#52850=CARTESIAN_POINT('Ctrl Pts',(-2.40643091952649,-5.40583746035036,
48.1342258538974));
#52851=CARTESIAN_POINT('Ctrl Pts',(-3.30651893922726,-5.00515955303441,
48.0878347014234));
#52852=CARTESIAN_POINT('Ctrl Pts',(-4.10436383865314,-4.37480138140656,
48.0414435489495));
#52853=CARTESIAN_POINT('Ctrl Pts',(-4.70241509822463,-3.59183527770545,
47.9950523964756));
#52854=CARTESIAN_POINT('Ctrl Pts',(-5.30046635779612,-2.80886917400434,
47.9486612440016));
#52855=CARTESIAN_POINT('Ctrl Pts',(-5.69872397751323,-1.87329513822997,
47.9022700915275));
#52856=CARTESIAN_POINT('Ctrl Pts',(-5.84849398470302,-0.89950349030608,
47.8558789390535));
#52857=CARTESIAN_POINT('Ctrl Pts',(-5.89423393101919,-0.602106310891314,
47.8417110234373));
#52858=CARTESIAN_POINT('Ctrl Pts',(-5.91679745783059,-0.301144577885169,
47.8275431078211));
#52859=CARTESIAN_POINT('Ctrl Pts',(-5.9165283748373,-0.000142876380609669,
47.8133751922049));
#52860=CARTESIAN_POINT('Ctrl Pts',(-5.91667009430184,-0.00015435290976692,
47.5616248077952));
#52861=CARTESIAN_POINT('Ctrl Pts',(-5.91692392185294,-0.252939328242564,
47.573524017966));
#52862=CARTESIAN_POINT('Ctrl Pts',(-5.90102760783804,-0.505692605401303,
47.5854232281369));
#52863=CARTESIAN_POINT('Ctrl Pts',(-5.86872650989343,-0.756331717182153,
47.5973224383077));
#52864=CARTESIAN_POINT('Ctrl Pts',(-5.74279502886973,-1.73349214074265,
47.6437135907817));
#52865=CARTESIAN_POINT('Ctrl Pts',(-5.3675163068583,-2.67851795611633,47.6901047432556));
#52866=CARTESIAN_POINT('Ctrl Pts',(-4.78877474362866,-3.4758631977001,47.7364958957296));
#52867=CARTESIAN_POINT('Ctrl Pts',(-4.21003318039895,-4.27320843928395,
47.7828870482035));
#52868=CARTESIAN_POINT('Ctrl Pts',(-3.427828775951,-4.92287310707781,47.8292782006776));
#52869=CARTESIAN_POINT('Ctrl Pts',(-2.53779972528504,-5.34542431137929,
47.8756693531516));
#52870=CARTESIAN_POINT('Ctrl Pts',(-1.64777067461913,-5.76797551568076,
47.9220605056256));
#52871=CARTESIAN_POINT('Ctrl Pts',(-0.649916977735285,-5.96341325648985,
47.9684516580995));
#52872=CARTESIAN_POINT('Ctrl Pts',(0.333756265546592,-5.90784184533997,
48.0148428105735));
#52873=CARTESIAN_POINT('Ctrl Pts',(1.31742950882841,-5.85227043419009,48.0612339630475));
#52874=CARTESIAN_POINT('Ctrl Pts',(2.28692229850836,-5.5456898710812,48.1076251155215));
#52875=CARTESIAN_POINT('Ctrl Pts',(3.12369715263964,-5.02558500206023,48.1540162679955));
#52876=CARTESIAN_POINT('Ctrl Pts',(3.96047200677097,-4.50548013303922,48.2004074204695));
#52877=CARTESIAN_POINT('Ctrl Pts',(4.66452892535374,-3.77185095810608,48.2467985729434));
#52878=CARTESIAN_POINT('Ctrl Pts',(5.14978461291203,-2.91439649926981,48.2931897254174));
#52879=CARTESIAN_POINT('Ctrl Pts',(5.63504030047034,-2.05694204043349,48.3395808778914));
#52880=CARTESIAN_POINT('Ctrl Pts',(5.90149475700412,-1.07566229769406,48.3859720303654));
#52881=CARTESIAN_POINT('Ctrl Pts',(5.91656925612452,-0.0905359145521563,
48.4323631828394));
#52882=CARTESIAN_POINT('Ctrl Pts',(5.93164375524491,0.894590468589636,48.4787543353134));
#52883=CARTESIAN_POINT('Ctrl Pts',(5.69533829695198,1.88356349213385,48.5251454877873));
#52884=CARTESIAN_POINT('Ctrl Pts',(5.23654536429916,2.75546387419225,48.5715366402613));
#52885=CARTESIAN_POINT('Ctrl Pts',(4.77775243164632,3.6273642562507,48.6179277927353));
#52886=CARTESIAN_POINT('Ctrl Pts',(4.09647202463357,4.38219199682328,48.6643189452093));
#52887=CARTESIAN_POINT('Ctrl Pts',(3.27600261108496,4.92765617778941,48.7107100976833));
#52888=CARTESIAN_POINT('Ctrl Pts',(2.45553319753639,5.47312035875552,48.7571012501573));
#52889=CARTESIAN_POINT('Ctrl Pts',(1.49587477745183,5.80922098011522,48.8034924026312));
#52890=CARTESIAN_POINT('Ctrl Pts',(0.514362408767521,5.89486385142087,48.8498835551052));
#52891=CARTESIAN_POINT('Ctrl Pts',(-0.467149959916903,5.98050672272653,
48.8962747075792));
#52892=CARTESIAN_POINT('Ctrl Pts',(-1.47051627720118,5.81569184397815,48.9426658600532));
#52893=CARTESIAN_POINT('Ctrl Pts',(-2.37305742882386,5.42057072215145,48.9890570125272));
#52894=CARTESIAN_POINT('Ctrl Pts',(-3.27559858044644,5.0254496003248,49.0354481650012));
#52895=CARTESIAN_POINT('Ctrl Pts',(-4.07731456640738,4.4000222354199,49.0818393174752));
#52896=CARTESIAN_POINT('Ctrl Pts',(-4.68018155896538,3.62075808215104,49.1282304699491));
#52897=CARTESIAN_POINT('Ctrl Pts',(-5.2830485515234,2.84149392888212,49.1746216224231));
#52898=CARTESIAN_POINT('Ctrl Pts',(-5.68706655067842,1.90839298724927,49.2210127748971));
#52899=CARTESIAN_POINT('Ctrl Pts',(-5.84283727643217,0.935543198081372,
49.2674039273711));
#52900=CARTESIAN_POINT('Ctrl Pts',(-5.89233176169344,0.626430562710378,
49.2821442208458));
#52901=CARTESIAN_POINT('Ctrl Pts',(-5.91676362954661,0.313304952112986,
49.2968845143205));
#52902=CARTESIAN_POINT('Ctrl Pts',(-5.91649558673351,0.000137928394543142,
49.3116248077952));
#52903=CARTESIAN_POINT('Origin',(0.,0.,0.));
#52904=CARTESIAN_POINT('',(-5.91697841467406,-0.000133927646978338,51.3133751922049));
#52905=CARTESIAN_POINT('',(-5.91711198123886,-0.000102791298586485,51.0616248077951));
#52906=CARTESIAN_POINT('',(-5.91675,-7.2459289488551E-16,0.));
#52907=CARTESIAN_POINT('Ctrl Pts',(-5.91697841467406,-0.000133927646978338,
51.3133751922049));
#52908=CARTESIAN_POINT('Ctrl Pts',(-5.9161664555486,0.830611330087965,51.27426410053));
#52909=CARTESIAN_POINT('Ctrl Pts',(-5.73957473098069,1.66169081825054,51.2351530088552));
#52910=CARTESIAN_POINT('Ctrl Pts',(-5.39991193444408,2.41969822879398,51.1960419171804));
#52911=CARTESIAN_POINT('Ctrl Pts',(-4.99702498066439,3.31879963080272,51.1496507647064));
#52912=CARTESIAN_POINT('Ctrl Pts',(-4.36470952307547,4.11509421835936,51.1032596122324));
#52913=CARTESIAN_POINT('Ctrl Pts',(-3.58027720642218,4.71122102467653,51.0568684597585));
#52914=CARTESIAN_POINT('Ctrl Pts',(-2.79584488976889,5.30734783099369,51.0104773072845));
#52915=CARTESIAN_POINT('Ctrl Pts',(-1.85929571405124,5.70330685607139,50.9640861548105));
#52916=CARTESIAN_POINT('Ctrl Pts',(-0.885139227138412,5.85068517070959,
50.9176950023365));
#52917=CARTESIAN_POINT('Ctrl Pts',(0.0890172597743667,5.99806348534778,
50.8713038498625));
#52918=CARTESIAN_POINT('Ctrl Pts',(1.10078105788233,5.89686108954651,50.8249126973885));
#52919=CARTESIAN_POINT('Ctrl Pts',(2.02644631374435,5.55945174956059,50.7785215449145));
#52920=CARTESIAN_POINT('Ctrl Pts',(2.95211156960648,5.22204240957463,50.7321303924405));
#52921=CARTESIAN_POINT('Ctrl Pts',(3.79167828322265,4.64842612540397,50.6857392399666));
#52922=CARTESIAN_POINT('Ctrl Pts',(4.44249471213787,3.90873753925835,50.6393480874926));
#52923=CARTESIAN_POINT('Ctrl Pts',(5.09331114105305,3.16904895311277,50.5929569350186));
#52924=CARTESIAN_POINT('Ctrl Pts',(5.5553772852673,2.26328806499226,50.5465657825446));
#52925=CARTESIAN_POINT('Ctrl Pts',(5.77219746187205,1.30220001510451,50.5001746300706));
#52926=CARTESIAN_POINT('Ctrl Pts',(5.9890176384768,0.341111965216764,50.4537834775966));
#52927=CARTESIAN_POINT('Ctrl Pts',(5.96059184747205,-0.675303246438216,
50.4073923251226));
#52928=CARTESIAN_POINT('Ctrl Pts',(5.69039563991286,-1.62277104960652,50.3610011726487));
#52929=CARTESIAN_POINT('Ctrl Pts',(5.42019943235367,-2.57023885277483,50.3146100201747));
#52930=CARTESIAN_POINT('Ctrl Pts',(4.90823280824003,-3.44875924745646,50.2682188677007));
#52931=CARTESIAN_POINT('Ctrl Pts',(4.2170926585536,-4.1509177211014,50.2218277152267));
#52932=CARTESIAN_POINT('Ctrl Pts',(3.52595250886718,-4.85307619474633,50.1754365627528));
#52933=CARTESIAN_POINT('Ctrl Pts',(2.65563883360783,-5.37887274735463,50.1290454102787));
#52934=CARTESIAN_POINT('Ctrl Pts',(1.71256273007023,-5.66401953684437,50.0826542578048));
#52935=CARTESIAN_POINT('Ctrl Pts',(0.769486626532637,-5.94916632633411,
50.0362631053308));
#52936=CARTESIAN_POINT('Ctrl Pts',(-0.246351905283146,-5.99366335270539,
49.9898719528568));
#52937=CARTESIAN_POINT('Ctrl Pts',(-1.21074880433904,-5.79207007476359,
49.9434808003828));
#52938=CARTESIAN_POINT('Ctrl Pts',(-2.17514570339494,-5.59047679682179,
49.8970896479088));
#52939=CARTESIAN_POINT('Ctrl Pts',(-3.08810096969077,-5.14279321456688,
49.8506984954348));
#52940=CARTESIAN_POINT('Ctrl Pts',(-3.83798982421993,-4.50375649068248,
49.8043073429609));
#52941=CARTESIAN_POINT('Ctrl Pts',(-4.58787867874904,-3.86471976679812,
49.7579161904869));
#52942=CARTESIAN_POINT('Ctrl Pts',(-5.17470112151149,-3.03432990128429,
49.7115250380129));
#52943=CARTESIAN_POINT('Ctrl Pts',(-5.52670782599837,-2.11411660610968,
49.6651338855389));
#52944=CARTESIAN_POINT('Ctrl Pts',(-5.78408263694966,-1.4412892995228,49.6312143210943));
#52945=CARTESIAN_POINT('Ctrl Pts',(-5.91592459112672,-0.720442248546615,
49.5972947566496));
#52946=CARTESIAN_POINT('Ctrl Pts',(-5.91663288208029,0.000152735557782668,
49.5633751922049));
#52947=CARTESIAN_POINT('Ctrl Pts',(-5.91649558673351,0.000137928394543142,
49.3116248077952));
#52948=CARTESIAN_POINT('Ctrl Pts',(-5.91592003609756,-0.672304945823302,
49.3432756667945));
#52949=CARTESIAN_POINT('Ctrl Pts',(-5.80146273753077,-1.34493875994679,
49.3749265257938));
#52950=CARTESIAN_POINT('Ctrl Pts',(-5.57671451190474,-1.9784447849391,49.406577384793));
#52951=CARTESIAN_POINT('Ctrl Pts',(-5.24729756927107,-2.90698434208879,
49.452968537267));
#52952=CARTESIAN_POINT('Ctrl Pts',(-4.68094023165125,-3.75146481968527,
49.499359689741));
#52953=CARTESIAN_POINT('Ctrl Pts',(-3.94688960784076,-4.40863368152314,
49.545750842215));
#52954=CARTESIAN_POINT('Ctrl Pts',(-3.21283898403027,-5.065802543361,49.592141994689));
#52955=CARTESIAN_POINT('Ctrl Pts',(-2.3110950740291,-5.53565978944027,49.638533147163));
#52956=CARTESIAN_POINT('Ctrl Pts',(-1.35191187208043,-5.76075713812599,
49.684924299637));
#52957=CARTESIAN_POINT('Ctrl Pts',(-0.392728670131761,-5.98585448681172,
49.7313154521109));
#52958=CARTESIAN_POINT('Ctrl Pts',(0.623893823764432,-5.96619193810391,
49.7777066045849));
#52959=CARTESIAN_POINT('Ctrl Pts',(1.57365569546802,-5.70417358312865,49.8240977570589));
#52960=CARTESIAN_POINT('Ctrl Pts',(2.5234175671716,-5.44215522815339,49.8704889095328));
#52961=CARTESIAN_POINT('Ctrl Pts',(3.40631881668261,-4.93778106691066,49.9168800620069));
#52962=CARTESIAN_POINT('Ctrl Pts',(4.11440929518245,-4.25271967875358,49.9632712144809));
#52963=CARTESIAN_POINT('Ctrl Pts',(4.82249977368232,-3.56765829059645,50.0096623669548));
#52964=CARTESIAN_POINT('Ctrl Pts',(5.35577948117102,-2.7019096755249,50.0560535194288));
#52965=CARTESIAN_POINT('Ctrl Pts',(5.6490456287554,-1.76132677223197,50.1024446719028));
#52966=CARTESIAN_POINT('Ctrl Pts',(5.94231177633977,-0.820743868939092,
50.1488358243768));
#52967=CARTESIAN_POINT('Ctrl Pts',(5.99556436401987,0.194673322575037,50.1952269768508));
#52968=CARTESIAN_POINT('Ctrl Pts',(5.8022923298075,1.1607722575073,50.2416181293248));
#52969=CARTESIAN_POINT('Ctrl Pts',(5.60902029559514,2.12687119243956,50.2880092817987));
#52970=CARTESIAN_POINT('Ctrl Pts',(5.16922363949027,3.04365187078983,50.3344004342727));
#52971=CARTESIAN_POINT('Ctrl Pts',(4.5366752092522,3.79902178989515,50.3807915867467));
#52972=CARTESIAN_POINT('Ctrl Pts',(3.90412677901412,4.55439170900048,50.4271827392207));
#52973=CARTESIAN_POINT('Ctrl Pts',(3.07882657464281,5.14835086886089,50.4735738916947));
#52974=CARTESIAN_POINT('Ctrl Pts',(2.16168200784626,5.50827735424564,50.5199650441686));
#52975=CARTESIAN_POINT('Ctrl Pts',(1.24453744104967,5.86820383963041,50.5663561966426));
#52976=CARTESIAN_POINT('Ctrl Pts',(0.235548511827793,5.99409765053951,50.6127473491166));
#52977=CARTESIAN_POINT('Ctrl Pts',(-0.741918202723497,5.87056606255386,
50.6591385015906));
#52978=CARTESIAN_POINT('Ctrl Pts',(-1.71938491727473,5.74703447456822,50.7055296540646));
#52979=CARTESIAN_POINT('Ctrl Pts',(-2.66532941715542,5.37407748768786,50.7519208065386));
#52980=CARTESIAN_POINT('Ctrl Pts',(-3.46409341148329,4.7972956288788,50.7983119590126));
#52981=CARTESIAN_POINT('Ctrl Pts',(-4.26285740581116,4.22051377006975,50.8447031114865));
#52982=CARTESIAN_POINT('Ctrl Pts',(-4.91444089458624,3.43990703933199,50.8910942639605));
#52983=CARTESIAN_POINT('Ctrl Pts',(-5.33917637861769,2.55091828805872,50.9374854164345));
#52984=CARTESIAN_POINT('Ctrl Pts',(-5.71803025962081,1.75796160972512,50.9788652135547));
#52985=CARTESIAN_POINT('Ctrl Pts',(-5.91639904055335,0.878773889402353,
51.0202450106749));
#52986=CARTESIAN_POINT('Ctrl Pts',(-5.91711198123886,-0.000102791298586485,
51.0616248077951));
#52987=CARTESIAN_POINT('Origin',(0.,0.,0.));
#52988=CARTESIAN_POINT('',(-5.91629566222658,7.35963193231049E-5,53.0633751922049));
#52989=CARTESIAN_POINT('',(-5.91624940617419,3.10831558172524E-5,52.8116248077951));
#52990=CARTESIAN_POINT('',(-5.91675,-7.2459289488551E-16,0.));
#52991=CARTESIAN_POINT('Ctrl Pts',(-5.91629566222658,7.35963193231049E-5,
53.0633751922049));
#52992=CARTESIAN_POINT('Ctrl Pts',(-5.91647516542744,0.411417234058072,
53.0440157493585));
#52993=CARTESIAN_POINT('Ctrl Pts',(-5.87419418252669,0.822724493908837,
53.0246563065121));
#52994=CARTESIAN_POINT('Ctrl Pts',(-5.78907949919593,1.22496815067562,53.0052968636658));
#52995=CARTESIAN_POINT('Ctrl Pts',(-5.58511865778604,2.18886711000249,52.9589057111918));
#52996=CARTESIAN_POINT('Ctrl Pts',(-5.13519457400149,3.100720292762,52.9125145587178));
#52997=CARTESIAN_POINT('Ctrl Pts',(-4.49431835109818,3.84903766897162,52.8661234062438));
#52998=CARTESIAN_POINT('Ctrl Pts',(-3.8534421281949,4.59735504518119,52.8197322537698));
#52999=CARTESIAN_POINT('Ctrl Pts',(-3.0216137661729,5.1821366148409,52.7733411012958));
#53000=CARTESIAN_POINT('Ctrl Pts',(-2.10053885840573,5.53188258394083,52.7269499488218));
#53001=CARTESIAN_POINT('Ctrl Pts',(-1.17946395063866,5.88162855304072,52.6805587963479));
#53002=CARTESIAN_POINT('Ctrl Pts',(-0.169142497126457,5.99633892158089,
52.6341676438739));
#53003=CARTESIAN_POINT('Ctrl Pts',(0.806896000590799,5.86198833693917,52.5877764913999));
#53004=CARTESIAN_POINT('Ctrl Pts',(1.78293449830828,5.72763775229742,52.5413853389259));
#53005=CARTESIAN_POINT('Ctrl Pts',(2.72469004023079,5.34422621447368,52.4949941864519));
#53006=CARTESIAN_POINT('Ctrl Pts',(3.51701650898951,4.75863250248173,52.4486030339779));
#53007=CARTESIAN_POINT('Ctrl Pts',(4.3093429777481,4.17303879048989,52.4022118815039));
#53008=CARTESIAN_POINT('Ctrl Pts',(4.95224037334295,3.38526290432992,52.35582072903));
#53009=CARTESIAN_POINT('Ctrl Pts',(5.36710322368081,2.49162425027036,52.309429576556));
#53010=CARTESIAN_POINT('Ctrl Pts',(5.78196607401873,1.5979855962107,52.2630384240821));
#53011=CARTESIAN_POINT('Ctrl Pts',(5.9687943790996,0.598484174251422,52.216647271608));
#53012=CARTESIAN_POINT('Ctrl Pts',(5.9047451048376,-0.384673452523944,52.170256119134));
#53013=CARTESIAN_POINT('Ctrl Pts',(5.84069583057561,-1.3678310792992,52.12386496666));
#53014=CARTESIAN_POINT('Ctrl Pts',(5.52576897697081,-2.33464491089054,52.0774738141861));
#53015=CARTESIAN_POINT('Ctrl Pts',(4.99846987033509,-3.16690501492114,52.0310826617121));
#53016=CARTESIAN_POINT('Ctrl Pts',(4.47117076369931,-3.99916511895182,51.9846915092381));
#53017=CARTESIAN_POINT('Ctrl Pts',(3.73149940403256,-4.69687149542172,51.9383003567641));
#53018=CARTESIAN_POINT('Ctrl Pts',(2.86989357630467,-5.17471731390861,51.8919092042902));
#53019=CARTESIAN_POINT('Ctrl Pts',(2.00828774857684,-5.65256313239547,51.8455180518162));
#53020=CARTESIAN_POINT('Ctrl Pts',(1.02474745278804,-5.91054839289931,51.7991268993422));
#53021=CARTESIAN_POINT('Ctrl Pts',(0.0395277246605722,-5.91712987665164,
51.7527357468682));
#53022=CARTESIAN_POINT('Ctrl Pts',(-0.945692003466838,-5.92371136040397,
51.7063445943942));
#53023=CARTESIAN_POINT('Ctrl Pts',(-1.93259116393294,-5.67888906740469,
51.6599534419202));
#53024=CARTESIAN_POINT('Ctrl Pts',(-2.80050404095068,-5.21259681299055,
51.6135622894462));
#53025=CARTESIAN_POINT('Ctrl Pts',(-3.66841691796848,-4.74630455857639,
51.5671711369723));
#53026=CARTESIAN_POINT('Ctrl Pts',(-4.41734351153807,-4.0585423427473,51.5207799844983));
#53027=CARTESIAN_POINT('Ctrl Pts',(-4.9557144221657,-3.2334011480358,51.4743888320243));
#53028=CARTESIAN_POINT('Ctrl Pts',(-5.4940853327933,-2.40825995332434,51.4279976795503));
#53029=CARTESIAN_POINT('Ctrl Pts',(-5.82190056047894,-1.44573977973047,
51.3816065270763));
#53030=CARTESIAN_POINT('Ctrl Pts',(-5.89907894933658,-0.463525584703147,
51.3352153746023));
#53031=CARTESIAN_POINT('Ctrl Pts',(-5.91119038294624,-0.309388886728128,
51.3279353138032));
#53032=CARTESIAN_POINT('Ctrl Pts',(-5.91712955113041,-0.154767197288363,
51.320655253004));
#53033=CARTESIAN_POINT('Ctrl Pts',(-5.91697841467406,-0.000133927646978338,
51.3133751922049));
#53034=CARTESIAN_POINT('Ctrl Pts',(-5.91711198123886,-0.000102791298586485,
51.0616248077951));
#53035=CARTESIAN_POINT('Ctrl Pts',(-5.91719832286859,-0.106540320374477,
51.0666361631489));
#53036=CARTESIAN_POINT('Ctrl Pts',(-5.91438569706757,-0.212973287512141,
51.0716475185027));
#53037=CARTESIAN_POINT('Ctrl Pts',(-5.9086436045588,-0.319247973600419,
51.0766588738565));
#53038=CARTESIAN_POINT('Ctrl Pts',(-5.85548786718063,-1.30305471217748,
51.1230500263304));
#53039=CARTESIAN_POINT('Ctrl Pts',(-5.55128891313645,-2.2732974175228,51.1694411788044));
#53040=CARTESIAN_POINT('Ctrl Pts',(-5.03324039503204,-3.11134691735899,
51.2158323312784));
#53041=CARTESIAN_POINT('Ctrl Pts',(-4.51519187692764,-3.94939641719518,
51.2622234837524));
#53042=CARTESIAN_POINT('Ctrl Pts',(-3.78329379476302,-4.65525271152223,
51.3086146362264));
#53043=CARTESIAN_POINT('Ctrl Pts',(-2.92703351412233,-5.14261249964901,
51.3550057887004));
#53044=CARTESIAN_POINT('Ctrl Pts',(-2.07077323348164,-5.62997228777579,
51.4013969411744));
#53045=CARTESIAN_POINT('Ctrl Pts',(-1.09015075436489,-5.89883556970231,
51.4477880936484));
#53046=CARTESIAN_POINT('Ctrl Pts',(-0.105064358277646,-5.91632909792562,
51.4941792461223));
#53047=CARTESIAN_POINT('Ctrl Pts',(0.880022037809597,-5.93382262614893,
51.5405703985963));
#53048=CARTESIAN_POINT('Ctrl Pts',(1.86957235086733,-5.69994640066903,51.5869615510703));
#53049=CARTESIAN_POINT('Ctrl Pts',(2.74259671524839,-5.24329588826058,51.6333527035443));
#53050=CARTESIAN_POINT('Ctrl Pts',(3.61562107962945,-4.78664537585214,51.6797438560182));
#53051=CARTESIAN_POINT('Ctrl Pts',(4.37211949533384,-4.10722057651513,51.7261350084922));
#53052=CARTESIAN_POINT('Ctrl Pts',(4.91959677493087,-3.28809307751947,51.7725261609662));
#53053=CARTESIAN_POINT('Ctrl Pts',(5.4670740545279,-2.46896557852381,51.8189173134402));
#53054=CARTESIAN_POINT('Ctrl Pts',(5.80553019801757,-1.51013537986949,51.8653084659142));
#53055=CARTESIAN_POINT('Ctrl Pts',(5.89358301109615,-0.528836274909741,
51.9116996183882));
#53056=CARTESIAN_POINT('Ctrl Pts',(5.98163582417474,0.452462830050005,51.9580907708622));
#53057=CARTESIAN_POINT('Ctrl Pts',(5.81928530684224,1.45623084131518,52.0044819233362));
#53058=CARTESIAN_POINT('Ctrl Pts',(5.42638165470832,2.35973953049624,52.0508730758101));
#53059=CARTESIAN_POINT('Ctrl Pts',(5.0334780025744,3.2632482196773,52.0972642282841));
#53060=CARTESIAN_POINT('Ctrl Pts',(4.41002121563907,4.06649758677425,52.1436553807581));
#53061=CARTESIAN_POINT('Ctrl Pts',(3.63223981092944,4.67127632133242,52.1900465332321));
#53062=CARTESIAN_POINT('Ctrl Pts',(2.85445840621981,5.27605505589058,52.2364376857061));
#53063=CARTESIAN_POINT('Ctrl Pts',(1.92235238373589,5.68236315790995,52.2828288381801));
#53064=CARTESIAN_POINT('Ctrl Pts',(0.949888038006726,5.84052234218767,52.3292199906541));
#53065=CARTESIAN_POINT('Ctrl Pts',(-0.0225763077224432,5.99868152646538,
52.375611143128));
#53066=CARTESIAN_POINT('Ctrl Pts',(-1.03539897669686,5.90869179300144,52.422002295602));
#53067=CARTESIAN_POINT('Ctrl Pts',(-1.9647446499574,5.5815559636006,52.468393448076));
#53068=CARTESIAN_POINT('Ctrl Pts',(-2.89409032321793,5.25442013419976,52.5147846005499));
#53069=CARTESIAN_POINT('Ctrl Pts',(-3.73995900076458,4.69013820886202,52.561175753024));
#53070=CARTESIAN_POINT('Ctrl Pts',(-4.39892841462264,3.95770354086397,52.6075669054979));
#53071=CARTESIAN_POINT('Ctrl Pts',(-5.0578978284807,3.22526887286591,52.6539580579719));
#53072=CARTESIAN_POINT('Ctrl Pts',(-5.52996797865016,2.32468146220754,52.7003492104459));
#53073=CARTESIAN_POINT('Ctrl Pts',(-5.75742001719438,1.36605390082203,52.7467403629199));
#53074=CARTESIAN_POINT('Ctrl Pts',(-5.86346106503545,0.919129477768853,
52.7683685112116));
#53075=CARTESIAN_POINT('Ctrl Pts',(-5.91633330006424,0.459589774967568,
52.7899966595034));
#53076=CARTESIAN_POINT('Ctrl Pts',(-5.91624940617419,3.10831558172524E-5,
52.8116248077951));
#53077=CARTESIAN_POINT('Origin',(0.,0.,0.));
#53078=CARTESIAN_POINT('',(-5.91726077539081,-8.91287485260684E-6,54.8133751922049));
#53079=CARTESIAN_POINT('',(-5.91723769598478,4.20217595612923E-5,54.5616248077952));
#53080=CARTESIAN_POINT('',(-5.91675,-7.2459289488551E-16,0.));
#53081=CARTESIAN_POINT('Ctrl Pts',(-5.91726077539081,-8.91287485260684E-6,
54.8133751922049));
#53082=CARTESIAN_POINT('Ctrl Pts',(-5.9171748721973,0.976903784862937,54.767376245713));
#53083=CARTESIAN_POINT('Ctrl Pts',(-5.67016608464484,1.95385832373982,54.7213772992211));
#53084=CARTESIAN_POINT('Ctrl Pts',(-5.20570418446295,2.81329564071131,54.6753783527292));
#53085=CARTESIAN_POINT('Ctrl Pts',(-4.73728209063319,3.68006087457345,54.6289872002552));
#53086=CARTESIAN_POINT('Ctrl Pts',(-4.04768288561822,4.42729634249545,54.5825960477812));
#53087=CARTESIAN_POINT('Ctrl Pts',(-3.22122215606804,4.96363941472753,54.5362048953072));
#53088=CARTESIAN_POINT('Ctrl Pts',(-2.39476142651782,5.49998248695964,54.4898137428333));
#53089=CARTESIAN_POINT('Ctrl Pts',(-1.43143917243238,5.82543316350179,54.4434225903593));
#53090=CARTESIAN_POINT('Ctrl Pts',(-0.449038419655624,5.9001993962792,54.3970314378853));
#53091=CARTESIAN_POINT('Ctrl Pts',(0.533362333121136,5.97496562905662,54.3506402854113));
#53092=CARTESIAN_POINT('Ctrl Pts',(1.53484158458918,5.79904741806929,54.3042491329373));
#53093=CARTESIAN_POINT('Ctrl Pts',(2.43295094735011,5.39395384722269,54.2578579804633));
#53094=CARTESIAN_POINT('Ctrl Pts',(3.33106031011092,4.98886027637614,54.2114668279893));
#53095=CARTESIAN_POINT('Ctrl Pts',(4.12579978416473,4.35459134567027,54.1650756755154));
#53096=CARTESIAN_POINT('Ctrl Pts',(4.71999854259989,3.56869754616937,54.1186845230414));
#53097=CARTESIAN_POINT('Ctrl Pts',(5.3141973010351,2.78280374666838,54.0722933705674));
#53098=CARTESIAN_POINT('Ctrl Pts',(5.7078553438517,1.84528507837241,54.0259022180934));
#53099=CARTESIAN_POINT('Ctrl Pts',(5.85284107725128,0.870769626606426,53.9795110656194));
#53100=CARTESIAN_POINT('Ctrl Pts',(5.99782681065085,-0.103745825159506,
53.9331199131455));
#53101=CARTESIAN_POINT('Ctrl Pts',(5.89414023463332,-1.11525806039542,53.8867287606715));
#53102=CARTESIAN_POINT('Ctrl Pts',(5.55445885001522,-2.04009198362915,53.8403376081975));
#53103=CARTESIAN_POINT('Ctrl Pts',(5.21477746539714,-2.96492590686283,53.7939464557235));
#53104=CARTESIAN_POINT('Ctrl Pts',(4.63910127217853,-3.80308151809446,53.7475553032495));
#53105=CARTESIAN_POINT('Ctrl Pts',(3.89781677254598,-4.45207960686234,53.7011641507755));
#53106=CARTESIAN_POINT('Ctrl Pts',(3.15653227291338,-5.10107769563026,53.6547729983015));
#53107=CARTESIAN_POINT('Ctrl Pts',(2.24963946686684,-5.56091826193439,53.6083818458276));
#53108=CARTESIAN_POINT('Ctrl Pts',(1.28802189141507,-5.77537773876444,53.5619906933536));
#53109=CARTESIAN_POINT('Ctrl Pts',(0.326404315963302,-5.9898372155945,53.5155995408796));
#53110=CARTESIAN_POINT('Ctrl Pts',(-0.689938028893665,-5.95891560295047,
53.4692083884056));
#53111=CARTESIAN_POINT('Ctrl Pts',(-1.63673948214485,-5.68639360981707,
53.4228172359316));
#53112=CARTESIAN_POINT('Ctrl Pts',(-2.5835409353961,-5.41387161668366,53.3764260834576));
#53113=CARTESIAN_POINT('Ctrl Pts',(-3.46080149704152,-4.89974924306087,
53.3300349309837));
#53114=CARTESIAN_POINT('Ctrl Pts',(-4.16126069119583,-4.20688695808299,
53.2836437785097));
#53115=CARTESIAN_POINT('Ctrl Pts',(-4.86171988535005,-3.51402467310519,
53.2372526260357));
#53116=CARTESIAN_POINT('Ctrl Pts',(-5.38537771201318,-2.64242247677237,
53.1908614735617));
#53117=CARTESIAN_POINT('Ctrl Pts',(-5.66820782582712,-1.69864901065889,
53.1444703210877));
#53118=CARTESIAN_POINT('Ctrl Pts',(-5.83301040353528,-1.14872065299335,
53.1174386114601));
#53119=CARTESIAN_POINT('Ctrl Pts',(-5.91604502079844,-0.574288065881491,
53.0904069018325));
#53120=CARTESIAN_POINT('Ctrl Pts',(-5.91629566222658,7.35963193231049E-5,
53.0633751922049));
#53121=CARTESIAN_POINT('Ctrl Pts',(-5.91624940617419,3.10831558172524E-5,
52.8116248077951));
#53122=CARTESIAN_POINT('Ctrl Pts',(-5.91615335242415,-0.526137576953405,
52.8363878119774));
#53123=CARTESIAN_POINT('Ctrl Pts',(-5.84663736162251,-1.05233112966596,
52.8611508161596));
#53124=CARTESIAN_POINT('Ctrl Pts',(-5.70802065118634,-1.55964379265648,
52.8859138203418));
#53125=CARTESIAN_POINT('Ctrl Pts',(-5.44833531971509,-2.51004621263684,
52.9323049728158));
#53126=CARTESIAN_POINT('Ctrl Pts',(-4.9461307298536,-3.39418334048491,52.9786961252898));
#53127=CARTESIAN_POINT('Ctrl Pts',(-4.26281019283623,-4.10395391959914,
53.0250872777638));
#53128=CARTESIAN_POINT('Ctrl Pts',(-3.57948965581886,-4.81372449871337,
53.0714784302378));
#53129=CARTESIAN_POINT('Ctrl Pts',(-2.7150531716456,-5.34912852909375,53.1178695827118));
#53130=CARTESIAN_POINT('Ctrl Pts',(-1.77519324801468,-5.64470348614918,
53.1642607351857));
#53131=CARTESIAN_POINT('Ctrl Pts',(-0.835333324383751,-5.94027844320462,
53.2106518876597));
#53132=CARTESIAN_POINT('Ctrl Pts',(0.179950038704843,-5.99602432693511,
53.2570430401337));
#53133=CARTESIAN_POINT('Ctrl Pts',(1.1465206593178,-5.80512522622028,53.3034341926077));
#53134=CARTESIAN_POINT('Ctrl Pts',(2.11309127993076,-5.61422612550546,53.3498253450817));
#53135=CARTESIAN_POINT('Ctrl Pts',(3.03094915806809,-5.17668204034532,53.3962164975557));
#53136=CARTESIAN_POINT('Ctrl Pts',(3.78787008451714,-4.54599040222939,53.4426076500296));
#53137=CARTESIAN_POINT('Ctrl Pts',(4.54479101096619,-3.91529876411345,53.4889988025036));
#53138=CARTESIAN_POINT('Ctrl Pts',(5.14077498572698,-3.09145957304172,53.5353899549776));
#53139=CARTESIAN_POINT('Ctrl Pts',(5.50295252446638,-2.17520160624497,53.5817811074516));
#53140=CARTESIAN_POINT('Ctrl Pts',(5.86513006320579,-1.25894363944822,53.6281722599256));
#53141=CARTESIAN_POINT('Ctrl Pts',(5.99350116592383,-0.250266896926448,
53.6745634123995));
#53142=CARTESIAN_POINT('Ctrl Pts',(5.87237021586824,0.727500214519055,53.7209545648735));
#53143=CARTESIAN_POINT('Ctrl Pts',(5.75123926581264,1.70526732596456,53.7673457173475));
#53144=CARTESIAN_POINT('Ctrl Pts',(5.38060626298342,2.65212480633379,53.8137368698215));
#53145=CARTESIAN_POINT('Ctrl Pts',(4.8057875865732,3.45230273688165,53.8601280222955));
#53146=CARTESIAN_POINT('Ctrl Pts',(4.23096891016299,4.25248066742951,53.9065191747695));
#53147=CARTESIAN_POINT('Ctrl Pts',(3.45196456017177,4.905979048156,53.9529103272435));
#53148=CARTESIAN_POINT('Ctrl Pts',(2.56402146886796,5.3328962507746,53.9993014797174));
#53149=CARTESIAN_POINT('Ctrl Pts',(1.67607837756421,5.75981345339318,54.0456926321914));
#53150=CARTESIAN_POINT('Ctrl Pts',(0.679196544947876,5.96014947790391,54.0920837846654));
#53151=CARTESIAN_POINT('Ctrl Pts',(-0.304737756597728,5.90940973482508,
54.1384749371394));
#53152=CARTESIAN_POINT('Ctrl Pts',(-1.28867205814344,5.85866999174624,54.1848660896134));
#53153=CARTESIAN_POINT('Ctrl Pts',(-2.25965882861843,5.5568544810778,54.2312572420874));
#53154=CARTESIAN_POINT('Ctrl Pts',(-3.09897792074494,5.04086543770779,54.2776483945614));
#53155=CARTESIAN_POINT('Ctrl Pts',(-3.93829701287136,4.52487639433785,54.3240395470353));
#53156=CARTESIAN_POINT('Ctrl Pts',(-4.64594842664933,3.7947138182664,54.3704306995093));
#53157=CARTESIAN_POINT('Ctrl Pts',(-5.135409376579,2.93965287904646,54.4168218519833));
#53158=CARTESIAN_POINT('Ctrl Pts',(-5.62487032650872,2.08459193982642,54.4632130044573));
#53159=CARTESIAN_POINT('Ctrl Pts',(-5.89614081259009,1.10463263745785,54.5096041569313));
#53160=CARTESIAN_POINT('Ctrl Pts',(-5.91605326443084,0.11959216846805,54.5559953094053));
#53161=CARTESIAN_POINT('Ctrl Pts',(-5.91685871338391,0.0797477625241243,
54.5578718088686));
#53162=CARTESIAN_POINT('Ctrl Pts',(-5.91725289962306,0.0398950429634057,
54.5597483083319));
#53163=CARTESIAN_POINT('Ctrl Pts',(-5.91723769598478,4.20217595612923E-5,
54.5616248077952));
#53164=CARTESIAN_POINT('Origin',(0.,0.,0.));
#53165=CARTESIAN_POINT('',(-5.91627540825074,-5.94123360231347E-5,56.5633751922049));
#53166=CARTESIAN_POINT('',(-5.9163456729308,-9.83204200377886E-5,56.3116248077952));
#53167=CARTESIAN_POINT('',(-5.91675,-7.2459289488551E-16,0.));
#53168=CARTESIAN_POINT('Ctrl Pts',(-5.91627540825074,-5.94123360231347E-5,
56.5633751922049));
#53169=CARTESIAN_POINT('Ctrl Pts',(-5.91607976903247,0.557640762099893,
56.5371278945414));
#53170=CARTESIAN_POINT('Ctrl Pts',(-5.83786039751333,1.11539468426929,56.510880596878));
#53171=CARTESIAN_POINT('Ctrl Pts',(-5.68235729093,1.65069804519026,56.4846332992146));
#53172=CARTESIAN_POINT('Ctrl Pts',(-5.40751115552233,2.59682743933861,56.4382421467406));
#53173=CARTESIAN_POINT('Ctrl Pts',(-4.89123613253373,3.47282287809166,56.3918509942667));
#53174=CARTESIAN_POINT('Ctrl Pts',(-4.19665589020436,4.17157856900639,56.3454598417927));
#53175=CARTESIAN_POINT('Ctrl Pts',(-3.50207564787502,4.87033425992108,56.2990686893187));
#53176=CARTESIAN_POINT('Ctrl Pts',(-2.62919018620492,5.39185020299748,56.2526775368446));
#53177=CARTESIAN_POINT('Ctrl Pts',(-1.68472504844259,5.67236193567815,56.2062863843706));
#53178=CARTESIAN_POINT('Ctrl Pts',(-0.740259910680251,5.95287366835883,
56.1598952318966));
#53179=CARTESIAN_POINT('Ctrl Pts',(0.275784903174342,5.99238119064378,56.1135040794227));
#53180=CARTESIAN_POINT('Ctrl Pts',(1.23918011048882,5.78605401564393,56.0671129269488));
#53181=CARTESIAN_POINT('Ctrl Pts',(2.20257531780331,5.57972684064408,56.0207217744748));
#53182=CARTESIAN_POINT('Ctrl Pts',(3.11332091857771,5.12756496835941,55.9743306220008));
#53183=CARTESIAN_POINT('Ctrl Pts',(3.86006230413533,4.48485311090271,55.9279394695268));
#53184=CARTESIAN_POINT('Ctrl Pts',(4.60680368969294,3.84214125344602,55.8815483170528));
#53185=CARTESIAN_POINT('Ctrl Pts',(5.18954086003379,3.00887941081727,55.8351571645788));
#53186=CARTESIAN_POINT('Ctrl Pts',(5.53702398478864,2.0869484445131,55.7887660121048));
#53187=CARTESIAN_POINT('Ctrl Pts',(5.88450710954352,1.16501747820888,55.7423748596309));
#53188=CARTESIAN_POINT('Ctrl Pts',(5.99673618871238,0.154417388229369,55.6959837071569));
#53189=CARTESIAN_POINT('Ctrl Pts',(5.85998925077836,-0.82128825569492,55.6495925546829));
#53190=CARTESIAN_POINT('Ctrl Pts',(5.72324231284433,-1.79699389961915,55.6032014022089));
#53191=CARTESIAN_POINT('Ctrl Pts',(5.3375193578074,-2.73780509748804,55.5568102497349));
#53192=CARTESIAN_POINT('Ctrl Pts',(4.74998177593861,-3.52869119454103,55.5104190972609));
#53193=CARTESIAN_POINT('Ctrl Pts',(4.16244419406982,-4.31957729159402,55.4640279447869));
#53194=CARTESIAN_POINT('Ctrl Pts',(3.37309198536915,-4.96053828783114,55.4176367923129));
#53195=CARTESIAN_POINT('Ctrl Pts',(2.47843728915764,-5.37320546991209,55.371245639839));
#53196=CARTESIAN_POINT('Ctrl Pts',(1.58378259294619,-5.78587265199302,55.324854487365));
#53197=CARTESIAN_POINT('Ctrl Pts',(0.583825409223878,-5.97024601991783,
55.278463334891));
#53198=CARTESIAN_POINT('Ctrl Pts',(-0.399171974063911,-5.90378269868584,
55.232072182417));
#53199=CARTESIAN_POINT('Ctrl Pts',(-1.38216935735181,-5.83731937745384,
55.185681029943));
#53200=CARTESIAN_POINT('Ctrl Pts',(-2.34820694020522,-5.52001936706497,
55.139289877469));
#53201=CARTESIAN_POINT('Ctrl Pts',(-3.17916970025765,-4.9906781538328,55.0928987249951));
#53202=CARTESIAN_POINT('Ctrl Pts',(-4.01013246031003,-4.46133694060066,
55.0465075725211));
#53203=CARTESIAN_POINT('Ctrl Pts',(-4.70602039756146,-3.71995452452523,
55.0001164200471));
#53204=CARTESIAN_POINT('Ctrl Pts',(-5.18174901764866,-2.85717789720512,
54.9537252675731));
#53205=CARTESIAN_POINT('Ctrl Pts',(-5.65747763773589,-1.99440126988496,
54.9073341150992));
#53206=CARTESIAN_POINT('Ctrl Pts',(-5.91304694065887,-1.01023043132008,
54.8609429626251));
#53207=CARTESIAN_POINT('Ctrl Pts',(-5.91720910079805,-0.0249975121364856,
54.8145518101512));
#53208=CARTESIAN_POINT('Ctrl Pts',(-5.91724428906172,-0.0166680306718219,
54.8141596041691));
#53209=CARTESIAN_POINT('Ctrl Pts',(-5.91726150783685,-0.00833847329425605,
54.813767398187));
#53210=CARTESIAN_POINT('Ctrl Pts',(-5.91726077539081,-8.91287485260684E-6,
54.8133751922049));
#53211=CARTESIAN_POINT('Ctrl Pts',(-5.91723769598478,4.20217595612923E-5,
54.5616248077952));
#53212=CARTESIAN_POINT('Ctrl Pts',(-5.91687703258142,-0.945358414009718,
54.6061394608058));
#53213=CARTESIAN_POINT('Ctrl Pts',(-5.68613561487586,-1.89092859694345,
54.6506541138165));
#53214=CARTESIAN_POINT('Ctrl Pts',(-5.25001479529728,-2.72971301852433,
54.6951687668272));
#53215=CARTESIAN_POINT('Ctrl Pts',(-4.79550945672283,-3.60385610091598,
54.7415599193012));
#53216=CARTESIAN_POINT('Ctrl Pts',(-4.11794436197377,-4.3620206300883,54.7879510717752));
#53217=CARTESIAN_POINT('Ctrl Pts',(-3.30016371684655,-4.91150770704385,
54.8343422242492));
#53218=CARTESIAN_POINT('Ctrl Pts',(-2.48238307171933,-5.46099478399941,
54.8807333767231));
#53219=CARTESIAN_POINT('Ctrl Pts',(-1.52438687621396,-5.80180440873821,
54.9271245291971));
#53220=CARTESIAN_POINT('Ctrl Pts',(-0.543306952184463,-5.8922666326338,
54.9735156816711));
#53221=CARTESIAN_POINT('Ctrl Pts',(0.437772971845032,-5.98272885652939,
55.0199068341451));
#53222=CARTESIAN_POINT('Ctrl Pts',(1.44193662439864,-5.82284367958176,55.0662979866191));
#53223=CARTESIAN_POINT('Ctrl Pts',(2.34640740300649,-5.43215986633843,55.1126891390931));
#53224=CARTESIAN_POINT('Ctrl Pts',(3.2508781816143,-5.04147605309511,55.1590802915671));
#53225=CARTESIAN_POINT('Ctrl Pts',(4.05565608627635,-4.41999360355611,55.205471444041));
#53226=CARTESIAN_POINT('Ctrl Pts',(4.66234291603613,-3.64369963740555,55.251862596515));
#53227=CARTESIAN_POINT('Ctrl Pts',(5.26902974579598,-2.8674056712549,55.298253748989));
#53228=CARTESIAN_POINT('Ctrl Pts',(5.6776255006535,-1.93630018849265,55.344644901463));
#53229=CARTESIAN_POINT('Ctrl Pts',(5.83817218975984,-0.964227150134441,
55.391036053937));
#53230=CARTESIAN_POINT('Ctrl Pts',(5.99871887886617,0.00784588822371104,
55.437427206411));
#53231=CARTESIAN_POINT('Ctrl Pts',(5.91121650222135,1.02088648217782,55.483818358885));
#53232=CARTESIAN_POINT('Ctrl Pts',(5.5863637586731,1.95103266762128,55.5302095113589));
#53233=CARTESIAN_POINT('Ctrl Pts',(5.26151101512484,2.88117885306474,55.5766006638329));
#53234=CARTESIAN_POINT('Ctrl Pts',(4.69930790467315,3.72843062999755,55.6229918163069));
#53235=CARTESIAN_POINT('Ctrl Pts',(3.96849360904772,4.38919662230903,55.6693829687809));
#53236=CARTESIAN_POINT('Ctrl Pts',(3.23767931342226,5.04996261462054,55.7157741212549));
#53237=CARTESIAN_POINT('Ctrl Pts',(2.3382538326232,5.52424282231063,55.7621652737288));
#53238=CARTESIAN_POINT('Ctrl Pts',(1.38018769229769,5.75404817918408,55.8085564262028));
#53239=CARTESIAN_POINT('Ctrl Pts',(0.422121551972288,5.9838535360575,55.8549475786768));
#53240=CARTESIAN_POINT('Ctrl Pts',(-0.594585247879595,5.96918404211424,
55.9013387311508));
#53241=CARTESIAN_POINT('Ctrl Pts',(-1.54562248523716,5.7118333000422,55.9477298836248));
#53242=CARTESIAN_POINT('Ctrl Pts',(-2.49665972259472,5.45448255797015,55.9941210360988));
#53243=CARTESIAN_POINT('Ctrl Pts',(-3.38202739745815,4.95445056776933,56.0405121885727));
#53244=CARTESIAN_POINT('Ctrl Pts',(-4.09347379729039,4.27287500229513,56.0869033410467));
#53245=CARTESIAN_POINT('Ctrl Pts',(-4.80492019712272,3.59129943682085,56.1332944935207));
#53246=CARTESIAN_POINT('Ctrl Pts',(-5.34244532192383,2.72818029607314,56.1796856459947));
#53247=CARTESIAN_POINT('Ctrl Pts',(-5.64032730614178,1.78904901943268,56.2260767984687));
#53248=CARTESIAN_POINT('Ctrl Pts',(-5.823431263147,1.21177794561567,56.2545928015775));
#53249=CARTESIAN_POINT('Ctrl Pts',(-5.91598865378374,0.605786509134923,
56.2831088046863));
#53250=CARTESIAN_POINT('Ctrl Pts',(-5.9163456729308,-9.83204200377886E-5,
56.3116248077952));
#53251=CARTESIAN_POINT('Origin',(0.,0.,0.));
#53252=CARTESIAN_POINT('',(-5.91702729634208,0.000124615492362937,58.3133751922049));
#53253=CARTESIAN_POINT('',(-5.91688099001312,0.000147016541328388,58.0616248077952));
#53254=CARTESIAN_POINT('',(-5.91675,-7.2459289488551E-16,0.));
#53255=CARTESIAN_POINT('Ctrl Pts',(-5.91702729634208,0.000124615492362937,
58.3133751922049));
#53256=CARTESIAN_POINT('Ctrl Pts',(-5.91715596758306,0.138093166993387,
58.3068795433699));
#53257=CARTESIAN_POINT('Ctrl Pts',(-5.91242878598758,0.27605291677057,58.3003838945349));
#53258=CARTESIAN_POINT('Ctrl Pts',(-5.90278469289257,0.413668088609088,
58.2938882457));
#53259=CARTESIAN_POINT('Ctrl Pts',(-5.83390772546236,1.39649930096326,58.247497093226));
#53260=CARTESIAN_POINT('Ctrl Pts',(-5.51423647159942,2.36175480989941,58.201105940752));
#53261=CARTESIAN_POINT('Ctrl Pts',(-4.98285634368328,3.19141521529174,58.154714788278));
#53262=CARTESIAN_POINT('Ctrl Pts',(-4.45147621576713,4.02107562068407,58.108323635804));
#53263=CARTESIAN_POINT('Ctrl Pts',(-3.70838721379777,4.71514092253258,58.0619324833301));
#53264=CARTESIAN_POINT('Ctrl Pts',(-2.84444498940382,5.18874947559003,58.0155413308561));
#53265=CARTESIAN_POINT('Ctrl Pts',(-1.98050276500986,5.66235802864748,57.9691501783821));
#53266=CARTESIAN_POINT('Ctrl Pts',(-0.995707318191299,5.91550983291386,
57.9227590259081));
#53267=CARTESIAN_POINT('Ctrl Pts',(-0.0104671488781131,5.91725264434219,
57.8763678734341));
#53268=CARTESIAN_POINT('Ctrl Pts',(0.974773020435017,5.91899545577053,57.8299767209601));
#53269=CARTESIAN_POINT('Ctrl Pts',(1.96045791224277,5.66932927436084,57.7835855684861));
#53270=CARTESIAN_POINT('Ctrl Pts',(2.82607027637954,5.19878016568737,57.7371944160122));
#53271=CARTESIAN_POINT('Ctrl Pts',(3.6916826405164,4.72823105701384,57.6908032635382));
#53272=CARTESIAN_POINT('Ctrl Pts',(4.43722247698224,4.03679902107647,57.6444121110642));
#53273=CARTESIAN_POINT('Ctrl Pts',(4.97153447668531,3.2090237402222,57.5980209585902));
#53274=CARTESIAN_POINT('Ctrl Pts',(5.50584647638837,2.38124845936792,57.5516298061162));
#53275=CARTESIAN_POINT('Ctrl Pts',(5.82893063932866,1.41712993359675,57.5052386536423));
#53276=CARTESIAN_POINT('Ctrl Pts',(5.90128426518759,0.434548546919226,57.4588475011683));
#53277=CARTESIAN_POINT('Ctrl Pts',(5.97363789104652,-0.548032839758186,
57.4124563486943));
#53278=CARTESIAN_POINT('Ctrl Pts',(5.79526097982415,-1.54907708734194,57.3660651962203));
#53279=CARTESIAN_POINT('Ctrl Pts',(5.38796323461345,-2.44618899528104,57.3196740437463));
#53280=CARTESIAN_POINT('Ctrl Pts',(4.98066548940273,-3.34330090322018,57.2732828912723));
#53281=CARTESIAN_POINT('Ctrl Pts',(4.34444691020367,-4.13648047151466,57.2268917387983));
#53282=CARTESIAN_POINT('Ctrl Pts',(3.55709636677232,-4.72874759906632,57.1805005863244));
#53283=CARTESIAN_POINT('Ctrl Pts',(2.76974582334101,-5.32101472661796,57.1341094338504));
#53284=CARTESIAN_POINT('Ctrl Pts',(1.83126331567744,-5.71236941342681,57.0877182813764));
#53285=CARTESIAN_POINT('Ctrl Pts',(0.856394775358902,-5.85496169132799,
57.0413271289024));
#53286=CARTESIAN_POINT('Ctrl Pts',(-0.118473764959746,-5.99755396922917,
56.9949359764284));
#53287=CARTESIAN_POINT('Ctrl Pts',(-1.12972833793337,-5.89138383822262,
56.9485448239544));
#53288=CARTESIAN_POINT('Ctrl Pts',(-2.05372535181664,-5.54943245724155,
56.9021536714805));
#53289=CARTESIAN_POINT('Ctrl Pts',(-2.97772236569985,-5.2074810762605,56.8557625190065));
#53290=CARTESIAN_POINT('Ctrl Pts',(-3.81446182049285,-4.62974844530485,
56.8093713665324));
#53291=CARTESIAN_POINT('Ctrl Pts',(-4.46163765567354,-3.88687250210966,
56.7629802140585));
#53292=CARTESIAN_POINT('Ctrl Pts',(-5.10881349085423,-3.14399655891447,
56.7165890615845));
#53293=CARTESIAN_POINT('Ctrl Pts',(-5.56642570642268,-2.23597730347984,
56.6701979091106));
#53294=CARTESIAN_POINT('Ctrl Pts',(-5.77852319029356,-1.27383600099065,
56.6238067566366));
#53295=CARTESIAN_POINT('Ctrl Pts',(-5.87061965034974,-0.856057315379074,
56.603662901826));
#53296=CARTESIAN_POINT('Ctrl Pts',(-5.91642555429848,-0.428074192589743,
56.5835190470154));
#53297=CARTESIAN_POINT('Ctrl Pts',(-5.91627540825074,-5.94123360231347E-5,
56.5633751922049));
#53298=CARTESIAN_POINT('Ctrl Pts',(-5.9163456729308,-9.83204200377886E-5,
56.3116248077952));
#53299=CARTESIAN_POINT('Ctrl Pts',(-5.91656946904121,-0.379894948476797,
56.3294999571603));
#53300=CARTESIAN_POINT('Ctrl Pts',(-5.88056440059847,-0.759649686812157,
56.3473751065255));
#53301=CARTESIAN_POINT('Ctrl Pts',(-5.80792311789336,-1.1322621476414,56.3652502558907));
#53302=CARTESIAN_POINT('Ctrl Pts',(-5.61939810179222,-2.09929862554175,
56.4116414083646));
#53303=CARTESIAN_POINT('Ctrl Pts',(-5.18410922595517,-3.0182281688093,56.4580325608386));
#53304=CARTESIAN_POINT('Ctrl Pts',(-4.55527818301399,-3.77669553839045,
56.5044237133126));
#53305=CARTESIAN_POINT('Ctrl Pts',(-3.92644714007281,-4.53516290797161,
56.5508148657866));
#53306=CARTESIAN_POINT('Ctrl Pts',(-3.10407393002749,-5.13316810386637,
56.5972060182606));
#53307=CARTESIAN_POINT('Ctrl Pts',(-2.18870808823997,-5.4975945120402,56.6435971707346));
#53308=CARTESIAN_POINT('Ctrl Pts',(-1.2733422464525,-5.862020920214,56.6899883232086));
#53309=CARTESIAN_POINT('Ctrl Pts',(-0.264983772922841,-5.9928685406669,
56.7363794756825));
#53310=CARTESIAN_POINT('Ctrl Pts',(0.713077839509047,-5.87413895895754,
56.7827706281565));
#53311=CARTESIAN_POINT('Ctrl Pts',(1.69113945194105,-5.75540937724817,56.8291617806305));
#53312=CARTESIAN_POINT('Ctrl Pts',(2.63890420327526,-5.38710259337649,56.8755529331045));
#53313=CARTESIAN_POINT('Ctrl Pts',(3.44049124499301,-4.81425056550529,56.9219440855785));
#53314=CARTESIAN_POINT('Ctrl Pts',(4.24207828671072,-4.24139853763412,56.9683352380525));
#53315=CARTESIAN_POINT('Ctrl Pts',(4.89748761881198,-3.46400126576346,57.0147263905264));
#53316=CARTESIAN_POINT('Ctrl Pts',(5.32658396571914,-2.57710918870065,57.0611175430004));
#53317=CARTESIAN_POINT('Ctrl Pts',(5.75568031262631,-1.69021711163785,57.1075086954744));
#53318=CARTESIAN_POINT('Ctrl Pts',(5.95846367433938,-0.693830229382904,
57.1538998479484));
#53319=CARTESIAN_POINT('Ctrl Pts',(5.91014023151901,0.290225702035549,57.2002910004224));
#53320=CARTESIAN_POINT('Ctrl Pts',(5.86181678869864,1.274281633454,57.2466821528964));
#53321=CARTESIAN_POINT('Ctrl Pts',(5.56238654134484,2.24600661403597,57.2930733053703));
#53322=CARTESIAN_POINT('Ctrl Pts',(5.0484600841085,3.08659023738248,57.3394644578443));
#53323=CARTESIAN_POINT('Ctrl Pts',(4.53453362687216,3.927173860729,57.3858556103183));
#53324=CARTESIAN_POINT('Ctrl Pts',(3.80611095975329,4.63661612684007,57.4322467627923));
#53325=CARTESIAN_POINT('Ctrl Pts',(2.95225451794705,5.12817528713702,57.4786379152663));
#53326=CARTESIAN_POINT('Ctrl Pts',(2.09839807614086,5.61973444743394,57.5250290677402));
#53327=CARTESIAN_POINT('Ctrl Pts',(1.11910785964732,5.89341050191678,57.5714202202142));
#53328=CARTESIAN_POINT('Ctrl Pts',(0.134119257521085,5.91574175730344,57.6178113726882));
#53329=CARTESIAN_POINT('Ctrl Pts',(-0.850869344605262,5.93807301269011,
57.6642025251622));
#53330=CARTESIAN_POINT('Ctrl Pts',(-1.84155633236431,5.70905946898055,57.7105936776362));
#53331=CARTESIAN_POINT('Ctrl Pts',(-2.71681286170871,5.25670204489428,57.7569848301102));
#53332=CARTESIAN_POINT('Ctrl Pts',(-3.5920693910531,4.80434462080802,57.8033759825841));
#53333=CARTESIAN_POINT('Ctrl Pts',(-4.35189546198286,4.12864331634505,57.8497671350581));
#53334=CARTESIAN_POINT('Ctrl Pts',(-4.90338902290551,3.31221445628018,57.8961582875321));
#53335=CARTESIAN_POINT('Ctrl Pts',(-5.4548825838281,2.49578559621541,57.9425494400061));
#53336=CARTESIAN_POINT('Ctrl Pts',(-5.79804363474364,1.53862918054877,57.9889405924801));
#53337=CARTESIAN_POINT('Ctrl Pts',(-5.89091472397156,0.557774353333574,
58.0353317449541));
#53338=CARTESIAN_POINT('Ctrl Pts',(-5.90846020592207,0.372468346802949,
58.0440960992345));
#53339=CARTESIAN_POINT('Ctrl Pts',(-5.91707236649847,0.186316499212652,
58.0528604535148));
#53340=CARTESIAN_POINT('Ctrl Pts',(-5.91688099001312,0.000147016541328388,
58.0616248077952));
#53341=CARTESIAN_POINT('Origin',(0.,0.,0.));
#53342=CARTESIAN_POINT('',(-5.91658334351688,-0.000149097059289338,60.0633751922048));
#53343=CARTESIAN_POINT('',(-5.91673072200561,-0.000155070081382937,59.8116248077951));
#53344=CARTESIAN_POINT('',(-5.91675,-7.2459289488551E-16,0.));
#53345=CARTESIAN_POINT('Ctrl Pts',(-5.91658334351688,-0.000149097059289338,
60.0633751922048));
#53346=CARTESIAN_POINT('Ctrl Pts',(-5.91591710183977,0.703798585125833,
60.0302400397244));
#53347=CARTESIAN_POINT('Ctrl Pts',(-5.79023326449385,1.40797780184198,59.9971048872439));
#53348=CARTESIAN_POINT('Ctrl Pts',(-5.54437260154774,2.06734633609866,59.9639697347634));
#53349=CARTESIAN_POINT('Ctrl Pts',(-5.20015328616037,2.99050086895518,59.9175785822894));
#53350=CARTESIAN_POINT('Ctrl Pts',(-4.62036770117985,3.82581912179531,59.8711874298154));
#53351=CARTESIAN_POINT('Ctrl Pts',(-3.87590479394297,4.47116880093722,59.8247962773414));
#53352=CARTESIAN_POINT('Ctrl Pts',(-3.13144188670613,5.11651848007909,59.7784051248674));
#53353=CARTESIAN_POINT('Ctrl Pts',(-2.22230165721294,5.57189958552276,59.7320139723935));
#53354=CARTESIAN_POINT('Ctrl Pts',(-1.25964242937086,5.78163379749245,59.6856228199195));
#53355=CARTESIAN_POINT('Ctrl Pts',(-0.29698320152883,5.99136800946213,59.6392316674455));
#53356=CARTESIAN_POINT('Ctrl Pts',(0.719195024662093,5.95545532795785,59.5928405149715));
#53357=CARTESIAN_POINT('Ctrl Pts',(1.66464665457408,5.67828670759027,59.5464493624975));
#53358=CARTESIAN_POINT('Ctrl Pts',(2.61009828448608,5.40111808722269,59.5000582100235));
#53359=CARTESIAN_POINT('Ctrl Pts',(3.48482331811929,4.88269352799172,59.4536670575496));
#53360=CARTESIAN_POINT('Ctrl Pts',(4.18187129231742,4.1863995166099,59.4072759050756));
#53361=CARTESIAN_POINT('Ctrl Pts',(4.87891926651564,3.490105505228,59.3608847526016));
#53362=CARTESIAN_POINT('Ctrl Pts',(5.39829018127884,2.61594204169528,59.3144936001276));
#53363=CARTESIAN_POINT('Ctrl Pts',(5.67648184134843,1.67079092738194,59.2681024476536));
#53364=CARTESIAN_POINT('Ctrl Pts',(5.954673501418,0.725639813068655,59.2217112951796));
#53365=CARTESIAN_POINT('Ctrl Pts',(5.99168590679389,-0.2904989520251,59.1753201427057));
#53366=CARTESIAN_POINT('Ctrl Pts',(5.78299364235101,-1.25338459808161,59.1289289902317));
#53367=CARTESIAN_POINT('Ctrl Pts',(5.57430137790812,-2.21627024413813,59.0825378377577));
#53368=CARTESIAN_POINT('Ctrl Pts',(5.11990444364646,-3.12590277115739,59.0361466852837));
#53369=CARTESIAN_POINT('Ctrl Pts',(4.47536082717046,-3.87106366323371,58.9897555328097));
#53370=CARTESIAN_POINT('Ctrl Pts',(3.83081721069445,-4.61622455531003,58.9433643803357));
#53371=CARTESIAN_POINT('Ctrl Pts',(2.99612691200424,-5.19691381244332,58.8969732278618));
#53372=CARTESIAN_POINT('Ctrl Pts',(2.07334544638051,-5.54213199753971,58.8505820753878));
#53373=CARTESIAN_POINT('Ctrl Pts',(1.15056398075677,-5.88735018263611,58.8041909229138));
#53374=CARTESIAN_POINT('Ctrl Pts',(0.13969134819945,-5.99709729569552,58.7577997704398));
#53375=CARTESIAN_POINT('Ctrl Pts',(-0.835675558454431,-5.85795482904931,
58.7114086179658));
#53376=CARTESIAN_POINT('Ctrl Pts',(-1.81104246510831,-5.71881236240311,
58.6650174654918));
#53377=CARTESIAN_POINT('Ctrl Pts',(-2.75090364585892,-5.33078031605133,
58.6186263130179));
#53378=CARTESIAN_POINT('Ctrl Pts',(-3.5403446021856,-4.74130240714043,58.5722351605439));
#53379=CARTESIAN_POINT('Ctrl Pts',(-4.32978555851227,-4.15182449822952,
58.5258440080699));
#53380=CARTESIAN_POINT('Ctrl Pts',(-4.96880629041501,-3.36090072675949,
58.4794528555959));
#53381=CARTESIAN_POINT('Ctrl Pts',(-5.37927531586764,-2.46523538313838,
58.4330617031219));
#53382=CARTESIAN_POINT('Ctrl Pts',(-5.73227082525564,-1.6949803222015,58.3931661994829));
#53383=CARTESIAN_POINT('Ctrl Pts',(-5.91623701286255,-0.847261840938569,
58.3532706958439));
#53384=CARTESIAN_POINT('Ctrl Pts',(-5.91702729634208,0.000124615492362937,
58.3133751922049));
#53385=CARTESIAN_POINT('Ctrl Pts',(-5.91688099001312,0.000147016541328388,
58.0616248077952));
#53386=CARTESIAN_POINT('Ctrl Pts',(-5.91605937963967,-0.799108847634678,
58.0992516059888));
#53387=CARTESIAN_POINT('Ctrl Pts',(-5.75297761825815,-1.59868974831479,
58.1368784041824));
#53388=CARTESIAN_POINT('Ctrl Pts',(-5.43790532219926,-2.33306112674712,
58.174505202376));
#53389=CARTESIAN_POINT('Ctrl Pts',(-5.04944370365874,-3.23848854084873,
58.22089635485));
#53390=CARTESIAN_POINT('Ctrl Pts',(-4.42993933903741,-4.04479013028813,
58.267287507324));
#53391=CARTESIAN_POINT('Ctrl Pts',(-3.65513749247627,-4.65338139694523,
58.313678659798));
#53392=CARTESIAN_POINT('Ctrl Pts',(-2.88033564591512,-5.26197266360233,
58.360069812272));
#53393=CARTESIAN_POINT('Ctrl Pts',(-1.95023631741417,-5.67285360747713,
58.4064609647459));
#53394=CARTESIAN_POINT('Ctrl Pts',(-0.978560447999752,-5.83578683332009,
58.4528521172199));
#53395=CARTESIAN_POINT('Ctrl Pts',(-0.00688457858533637,-5.99872005916305,
58.4992432696939));
#53396=CARTESIAN_POINT('Ctrl Pts',(1.00636783174254,-5.91370556697417,58.5456344221679));
#53397=CARTESIAN_POINT('Ctrl Pts',(1.93730892061392,-5.59113786813126,58.5920255746419));
#53398=CARTESIAN_POINT('Ctrl Pts',(2.86825000948531,-5.26857016928834,58.6384167271159));
#53399=CARTESIAN_POINT('Ctrl Pts',(3.7168797769002,-4.7084492637914,58.6848078795899));
#53400=CARTESIAN_POINT('Ctrl Pts',(4.37943836326497,-3.97925974732797,58.7311990320639));
#53401=CARTESIAN_POINT('Ctrl Pts',(5.04199694962974,-3.25007023086454,58.7775901845378));
#53402=CARTESIAN_POINT('Ctrl Pts',(5.51848435494438,-2.35181210343462,58.8239813370118));
#53403=CARTESIAN_POINT('Ctrl Pts',(5.75064164442725,-1.39431316128073,58.8703724894858));
#53404=CARTESIAN_POINT('Ctrl Pts',(5.98279893391012,-0.436814219126841,
58.9167636419597));
#53405=CARTESIAN_POINT('Ctrl Pts',(5.97062610756122,0.579925537751025,58.9631547944338));
#53406=CARTESIAN_POINT('Ctrl Pts',(5.71561150670597,1.53159185775846,59.0095459469077));
#53407=CARTESIAN_POINT('Ctrl Pts',(5.46059690585071,2.48325817776589,59.0559370993817));
#53408=CARTESIAN_POINT('Ctrl Pts',(4.96274053048909,3.36985106090288,59.1023282518557));
#53409=CARTESIAN_POINT('Ctrl Pts',(4.28291404643916,4.08296899145165,59.1487194043297));
#53410=CARTESIAN_POINT('Ctrl Pts',(3.60308756238927,4.79608692200038,59.1951105568037));
#53411=CARTESIAN_POINT('Ctrl Pts',(2.74129096965108,5.33572989996091,59.2415017092776));
#53412=CARTESIAN_POINT('Ctrl Pts',(1.80289400293608,5.63591711512144,59.2878928617516));
#53413=CARTESIAN_POINT('Ctrl Pts',(0.864497036220978,5.93610433028201,59.3342840142256));
#53414=CARTESIAN_POINT('Ctrl Pts',(-0.150500304470951,5.99683578264253,
59.3806751666996));
#53415=CARTESIAN_POINT('Ctrl Pts',(-1.11799680845635,5.81068598795556,59.4270663191736));
#53416=CARTESIAN_POINT('Ctrl Pts',(-2.08549331244169,5.6245361932686,59.4734574716476));
#53417=CARTESIAN_POINT('Ctrl Pts',(-3.0054889797205,5.19150515153418,59.5198486241216));
#53418=CARTESIAN_POINT('Ctrl Pts',(-3.76549821889715,4.56453849560105,59.5662397765955));
#53419=CARTESIAN_POINT('Ctrl Pts',(-4.52550745807381,3.93757183966792,59.6126309290695));
#53420=CARTESIAN_POINT('Ctrl Pts',(-5.1255302691483,3.11666956953608,59.6590220815435));
#53421=CARTESIAN_POINT('Ctrl Pts',(-5.49220334927571,2.20220137238773,59.7054132340175));
#53422=CARTESIAN_POINT('Ctrl Pts',(-5.77203346648078,1.50431609894628,59.7408170919434));
#53423=CARTESIAN_POINT('Ctrl Pts',(-5.91595773098113,0.751936838973634,
59.7762209498693));
#53424=CARTESIAN_POINT('Ctrl Pts',(-5.91673072200561,-0.000155070081382937,
59.8116248077951));
#53425=CARTESIAN_POINT('Origin',(0.,0.,0.));
#53426=CARTESIAN_POINT('',(-5.91657547456529,0.000148352692112552,61.8133751922048));
#53427=CARTESIAN_POINT('',(-5.91644646386006,0.000128480793576948,61.5616248077951));
#53428=CARTESIAN_POINT('',(-5.91675,-7.2459289488551E-16,0.));
#53429=CARTESIAN_POINT('Ctrl Pts',(-5.91657547456529,0.000148352692112552,
61.8133751922048));
#53430=CARTESIAN_POINT('Ctrl Pts',(-5.9168426692125,0.284478488460568,61.7999916885528));
#53431=CARTESIAN_POINT('Ctrl Pts',(-5.89671750618213,0.568771121108608,
61.7866081849008));
#53432=CARTESIAN_POINT('Ctrl Pts',(-5.85588508619642,0.850057825547872,
61.7732246812488));
#53433=CARTESIAN_POINT('Ctrl Pts',(-5.71434793189889,1.82508011670782,61.7268335287748));
#53434=CARTESIAN_POINT('Ctrl Pts',(-5.32400912976953,2.76398560624496,61.6804423763008));
#53435=CARTESIAN_POINT('Ctrl Pts',(-4.73259444730769,3.55197665989223,61.6340512238268));
#53436=CARTESIAN_POINT('Ctrl Pts',(-4.14117976484579,4.33996771353959,61.5876600713528));
#53437=CARTESIAN_POINT('Ctrl Pts',(-3.34868920205137,4.97704433129704,61.5412689188788));
#53438=CARTESIAN_POINT('Ctrl Pts',(-2.45201861239238,5.38531272584916,61.4948777664049));
#53439=CARTESIAN_POINT('Ctrl Pts',(-1.55534802273349,5.79358112040123,61.4484866139309));
#53440=CARTESIAN_POINT('Ctrl Pts',(-0.554497406209885,5.97304129174803,
61.4020954614569));
#53441=CARTESIAN_POINT('Ctrl Pts',(0.428161709040809,5.90175109301285,61.3557043089829));
#53442=CARTESIAN_POINT('Ctrl Pts',(1.41082082429162,5.83046089427766,61.3093131565089));
#53443=CARTESIAN_POINT('Ctrl Pts',(2.37528843826953,5.50842032546052,61.2629220040349));
#53444=CARTESIAN_POINT('Ctrl Pts',(3.20364148603252,4.97500448728938,61.2165308515609));
#53445=CARTESIAN_POINT('Ctrl Pts',(4.0319945337955,4.44158864911823,61.1701396990869));
#53446=CARTESIAN_POINT('Ctrl Pts',(4.72423301534339,3.69679754159311,61.123748546613));
#53447=CARTESIAN_POINT('Ctrl Pts',(5.19571864559717,2.8316949295584,61.077357394139));
#53448=CARTESIAN_POINT('Ctrl Pts',(5.6672042758509,1.96659231752379,61.030966241665));
#53449=CARTESIAN_POINT('Ctrl Pts',(5.91793705481057,0.981178200979634,60.984575089191));
#53450=CARTESIAN_POINT('Ctrl Pts',(5.91726050698192,-0.00406327743461797,
60.938183936717));
#53451=CARTESIAN_POINT('Ctrl Pts',(5.91658395915327,-0.989304755848871,
60.8917927842431));
#53452=CARTESIAN_POINT('Ctrl Pts',(5.66449808453628,-1.97437359613322,60.8454016317691));
#53453=CARTESIAN_POINT('Ctrl Pts',(5.19182479843574,-2.83882787095668,60.7990104792951));
#53454=CARTESIAN_POINT('Ctrl Pts',(4.71915151233514,-3.70328214578024,60.7526193268211));
#53455=CARTESIAN_POINT('Ctrl Pts',(4.02589081475093,-4.44712185514289,60.7062281743471));
#53456=CARTESIAN_POINT('Ctrl Pts',(3.19680597404423,-4.97939956041544,60.6598370218731));
#53457=CARTESIAN_POINT('Ctrl Pts',(2.36772113333763,-5.51167726568792,60.6134458693991));
#53458=CARTESIAN_POINT('Ctrl Pts',(1.40281214950857,-5.83239296687034,60.5670547169252));
#53459=CARTESIAN_POINT('Ctrl Pts',(0.420056053873144,-5.90233354952841,
60.5206635644512));
#53460=CARTESIAN_POINT('Ctrl Pts',(-0.562700041762392,-5.97227413218649,
60.4742724119772));
#53461=CARTESIAN_POINT('Ctrl Pts',(-1.5633032492043,-5.79143959632015,60.4278812595032));
#53462=CARTESIAN_POINT('Ctrl Pts',(-2.45941229276507,-5.38194013273498,
60.3814901070292));
#53463=CARTESIAN_POINT('Ctrl Pts',(-3.35552133632579,-4.97244066914982,
60.3350989545552));
#53464=CARTESIAN_POINT('Ctrl Pts',(-4.14713621600539,-4.33427627784585,
60.2887078020812));
#53465=CARTESIAN_POINT('Ctrl Pts',(-4.73746814131828,-3.54547373818747,
60.2423166496073));
#53466=CARTESIAN_POINT('Ctrl Pts',(-5.32780006663118,-2.75667119852909,
60.1959254971333));
#53467=CARTESIAN_POINT('Ctrl Pts',(-5.71684903757736,-1.8172305105163,60.1495343446593));
#53468=CARTESIAN_POINT('Ctrl Pts',(-5.85704700015334,-0.842014760073484,
60.1031431921854));
#53469=CARTESIAN_POINT('Ctrl Pts',(-5.89710774647858,-0.563352573597715,
60.0898871921919));
#53470=CARTESIAN_POINT('Ctrl Pts',(-5.91684987917482,-0.281769363510951,
60.0766311921983));
#53471=CARTESIAN_POINT('Ctrl Pts',(-5.91658334351688,-0.000149097059289338,
60.0633751922048));
#53472=CARTESIAN_POINT('Ctrl Pts',(-5.91673072200561,-0.000155070081382937,
59.8116248077951));
#53473=CARTESIAN_POINT('Ctrl Pts',(-5.91697061337809,-0.233560574909101,
59.8226121023432));
#53474=CARTESIAN_POINT('Ctrl Pts',(-5.90342332074282,-0.466938404398139,
59.8335993968914));
#53475=CARTESIAN_POINT('Ctrl Pts',(-5.87587228115627,-0.698651164660174,
59.8445866914395));
#53476=CARTESIAN_POINT('Ctrl Pts',(-5.75954478372911,-1.67700138039482,
59.8909778439134));
#53477=CARTESIAN_POINT('Ctrl Pts',(-5.39356643969452,-2.62566768769933,
59.9373689963874));
#53478=CARTESIAN_POINT('Ctrl Pts',(-4.82268451464387,-3.42865900703989,
59.9837601488614));
#53479=CARTESIAN_POINT('Ctrl Pts',(-4.25180258959316,-4.23165032638054,
60.0301513013354));
#53480=CARTESIAN_POINT('Ctrl Pts',(-3.47601708352634,-4.88896665775721,
60.0765424538094));
#53481=CARTESIAN_POINT('Ctrl Pts',(-2.59018136863848,-5.32023956151416,
60.1229336062834));
#53482=CARTESIAN_POINT('Ctrl Pts',(-1.70434565375068,-5.75151246527109,
60.1693247587573));
#53483=CARTESIAN_POINT('Ctrl Pts',(-0.708459730041834,-5.95674194140831,
60.2157159112313));
#53484=CARTESIAN_POINT('Ctrl Pts',(0.275711897420253,-5.9108350902356,60.2621070637053));
#53485=CARTESIAN_POINT('Ctrl Pts',(1.25988352488228,-5.8649282390629,60.3084982161793));
#53486=CARTESIAN_POINT('Ctrl Pts',(2.23234085609756,-5.56788506058028,60.3548893686533));
#53487=CARTESIAN_POINT('Ctrl Pts',(3.07418394196869,-5.05602428843925,60.4012805211273));
#53488=CARTESIAN_POINT('Ctrl Pts',(3.91602702783991,-4.54416351629815,60.4476716736012));
#53489=CARTESIAN_POINT('Ctrl Pts',(4.62725586836695,-3.81748515049858,60.4940628260752));
#53490=CARTESIAN_POINT('Ctrl Pts',(5.12091027494375,-2.96483835483668,60.5404539785492));
#53491=CARTESIAN_POINT('Ctrl Pts',(5.61456468152053,-2.11219155917483,60.5868451310232));
#53492=CARTESIAN_POINT('Ctrl Pts',(5.8906446541471,-1.13357633365067,60.6332362834972));
#53493=CARTESIAN_POINT('Ctrl Pts',(5.91539457842234,-0.148645537839881,
60.6796274359712));
#53494=CARTESIAN_POINT('Ctrl Pts',(5.94014450269758,0.836285257970903,60.7260185884451));
#53495=CARTESIAN_POINT('Ctrl Pts',(5.71356437862149,1.8275316240683,60.7724097409191));
#53496=CARTESIAN_POINT('Ctrl Pts',(5.26335759672681,2.70389632259119,60.8188008933931));
#53497=CARTESIAN_POINT('Ctrl Pts',(4.81315081483215,3.58026102111402,60.8651920458671));
#53498=CARTESIAN_POINT('Ctrl Pts',(4.13931737511893,4.34174405206235,60.9115831983411));
#53499=CARTESIAN_POINT('Ctrl Pts',(3.32424522315754,4.89524077146601,60.9579743508151));
#53500=CARTESIAN_POINT('Ctrl Pts',(2.50917307119606,5.44873749086974,61.0043655032891));
#53501=CARTESIAN_POINT('Ctrl Pts',(1.55286220698639,5.79424789872876,61.050756655763));
#53502=CARTESIAN_POINT('Ctrl Pts',(0.572238391115561,5.88952729327051,61.097147808237));
#53503=CARTESIAN_POINT('Ctrl Pts',(-0.408385424755208,5.98480668781225,
61.143538960711));
#53504=CARTESIAN_POINT('Ctrl Pts',(-1.41332219228712,5.82985506903674,61.189930113185));
#53505=CARTESIAN_POINT('Ctrl Pts',(-2.31970078218799,5.44361798762822,61.236321265659));
#53506=CARTESIAN_POINT('Ctrl Pts',(-3.22607937208887,5.05738090621969,61.282712418133));
#53507=CARTESIAN_POINT('Ctrl Pts',(-4.0338997843587,4.43985836217815,61.3291035706069));
#53508=CARTESIAN_POINT('Ctrl Pts',(-4.64439181811148,3.66655330720706,61.3754947230809));
#53509=CARTESIAN_POINT('Ctrl Pts',(-5.25488385186429,2.89324825223592,61.4218858755549));
#53510=CARTESIAN_POINT('Ctrl Pts',(-5.66804750710004,1.96416068633522,61.4682770280289));
#53511=CARTESIAN_POINT('Ctrl Pts',(-5.83336628722356,0.992887845105691,
61.5146681805029));
#53512=CARTESIAN_POINT('Ctrl Pts',(-5.88914425298273,0.665183858659447,
61.5303203896003));
#53513=CARTESIAN_POINT('Ctrl Pts',(-5.91670846302273,0.332677654485142,
61.5459725986977));
#53514=CARTESIAN_POINT('Ctrl Pts',(-5.91644646386006,0.000128480793576948,
61.5616248077951));
#53515=CARTESIAN_POINT('Origin',(0.,0.,0.));
#53516=CARTESIAN_POINT('',(-5.91675,7.2459289488551E-16,66.));
#53517=CARTESIAN_POINT('Origin',(0.,0.,66.));
#53518=CARTESIAN_POINT('',(-5.91675,-7.2459289488551E-16,64.));
#53519=CARTESIAN_POINT('',(-5.91675,-7.2459289488551E-16,0.));
#53520=CARTESIAN_POINT('',(-0.0185920708322156,-5.91672078920428,64.));
#53521=CARTESIAN_POINT('Origin',(0.,0.,64.));
#53522=CARTESIAN_POINT('',(-5.9170192319132,-0.000147776431128344,63.5633751922049));
#53523=CARTESIAN_POINT('Ctrl Pts',(-0.0185920708322163,-5.91672078920428,
64.));
#53524=CARTESIAN_POINT('Ctrl Pts',(-1.00409531133336,-5.91362404918467,
63.953608847526));
#53525=CARTESIAN_POINT('Ctrl Pts',(-1.98830837177191,-5.65954316834941,
63.907217695052));
#53526=CARTESIAN_POINT('Ctrl Pts',(-2.85153274099139,-5.18487830611679,
63.8608265425781));
#53527=CARTESIAN_POINT('Ctrl Pts',(-3.71475711021086,-4.71021344388416,
63.8144353901041));
#53528=CARTESIAN_POINT('Ctrl Pts',(-4.45699278821126,-4.01496460025418,
63.7680442376301));
#53529=CARTESIAN_POINT('Ctrl Pts',(-4.98725841148824,-3.18453283331056,
63.7216530851561));
#53530=CARTESIAN_POINT('Ctrl Pts',(-5.51752403476525,-2.35410106636689,
63.6752619326821));
#53531=CARTESIAN_POINT('Ctrl Pts',(-5.83581960331881,-1.38848637610957,
63.6288707802081));
#53532=CARTESIAN_POINT('Ctrl Pts',(-5.90333451661355,-0.405580965178079,
63.5824796277342));
#53533=CARTESIAN_POINT('Ctrl Pts',(-5.91260233486136,-0.27065686828223,
63.5761114825577));
#53534=CARTESIAN_POINT('Ctrl Pts',(-5.91714463294472,-0.135406958180736,
63.5697433373813));
#53535=CARTESIAN_POINT('Ctrl Pts',(-5.9170192319132,-0.000147776431128344,
63.5633751922049));
#53536=CARTESIAN_POINT('',(-5.9171574445836,-8.64418186984388E-5,63.3116248077951));
#53537=CARTESIAN_POINT('',(-5.91675,-7.2459289488551E-16,0.));
#53538=CARTESIAN_POINT('',(4.63776713187073,-3.67456288307085,64.));
#53539=CARTESIAN_POINT('Ctrl Pts',(-5.9171574445836,-8.64418186984388E-5,
63.3116248077951));
#53540=CARTESIAN_POINT('Ctrl Pts',(-5.91721937759278,-0.0871536346831795,
63.3157242475262));
#53541=CARTESIAN_POINT('Ctrl Pts',(-5.91533756169338,-0.174218156234632,
63.3198236872572));
#53542=CARTESIAN_POINT('Ctrl Pts',(-5.91149447524869,-0.261196029287235,
63.3239231269883));
#53543=CARTESIAN_POINT('Ctrl Pts',(-5.86800433490684,-1.24547779347176,
63.3703142794623));
#53544=CARTESIAN_POINT('Ctrl Pts',(-5.57334936954011,-2.21866315124588,
63.4167054319362));
#53545=CARTESIAN_POINT('Ctrl Pts',(-5.06355767648185,-3.06175989147063,
63.4630965844102));
#53546=CARTESIAN_POINT('Ctrl Pts',(-4.55376598342356,-3.90485663169542,
63.5094877368842));
#53547=CARTESIAN_POINT('Ctrl Pts',(-3.82883756267365,-4.61786475437092,
63.5558788893582));
#53548=CARTESIAN_POINT('Ctrl Pts',(-2.97740495481013,-5.11361285815225,
63.6022700418322));
#53549=CARTESIAN_POINT('Ctrl Pts',(-2.12597234694665,-5.60936096193355,
63.6486611943062));
#53550=CARTESIAN_POINT('Ctrl Pts',(-1.14803555196965,-5.88784904682074,
63.6950523467801));
#53551=CARTESIAN_POINT('Ctrl Pts',(-0.163169671587142,-5.91501470558879,
63.7414434992541));
#53552=CARTESIAN_POINT('Ctrl Pts',(0.821696208795361,-5.94218036435685,
63.7878346517281));
#53553=CARTESIAN_POINT('Ctrl Pts',(1.8134911745833,-5.71802359700571,63.8342258042021));
#53554=CARTESIAN_POINT('Ctrl Pts',(2.6909610407991,-5.26997560876332,63.8806169566761));
#53555=CARTESIAN_POINT('Ctrl Pts',(3.44365501703819,-4.88563987850002,63.9204113044507));
#53556=CARTESIAN_POINT('Ctrl Pts',(4.11222612983174,-4.33656017974518,63.9602056522253));
#53557=CARTESIAN_POINT('Ctrl Pts',(4.63776713187073,-3.67456288307085,64.));
#53558=CARTESIAN_POINT('Origin',(0.,0.,64.));
#53559=CARTESIAN_POINT('Origin',(0.,0.,-3.23514056400933));
#53560=CARTESIAN_POINT('',(-4.91810492716115,0.000123316961498904,62.3898594359907));
#53561=CARTESIAN_POINT('',(-4.91858868497457,-7.18540524885514E-5,62.7351405640092));
#53562=CARTESIAN_POINT('',(-4.91825,1.47989506776076E-12,-3.23514056400933));
#53563=CARTESIAN_POINT('',(-4.31134524531351,2.36723698448027,64.));
#53564=CARTESIAN_POINT('Ctrl Pts',(-4.91810492716115,0.000123316961498816,
62.3898594359907));
#53565=CARTESIAN_POINT('Ctrl Pts',(-4.9175571550679,-0.582778007190868,
62.4228670848126));
#53566=CARTESIAN_POINT('Ctrl Pts',(-4.66822121487943,-1.98538387797463,
62.5022658861086));
#53567=CARTESIAN_POINT('Ctrl Pts',(-3.36401880748098,-3.86991586995366,
62.6280558398784));
#53568=CARTESIAN_POINT('Ctrl Pts',(-1.09843433267496,-5.00862398811822,
62.7672292973006));
#53569=CARTESIAN_POINT('Ctrl Pts',(1.4357556111677,-4.92254766049344,62.9064027547223));
#53570=CARTESIAN_POINT('Ctrl Pts',(3.61885342162015,-3.63273659425221,63.0455762121445));
#53571=CARTESIAN_POINT('Ctrl Pts',(4.91701390374655,-1.45459279213023,63.1847496695662));
#53572=CARTESIAN_POINT('Ctrl Pts',(5.01279380401881,1.07924733972977,63.3239231269884));
#53573=CARTESIAN_POINT('Ctrl Pts',(3.88276674436703,3.34917871604949,63.4630965844101));
#53574=CARTESIAN_POINT('Ctrl Pts',(1.80327337436161,4.80010868768094,63.6022700418323));
#53575=CARTESIAN_POINT('Ctrl Pts',(-0.717195690581678,5.07726303778206,
63.741443499254));
#53576=CARTESIAN_POINT('Ctrl Pts',(-2.95110573148774,4.15852613293832,63.8740201519768));
#53577=CARTESIAN_POINT('Ctrl Pts',(-3.97259884441697,2.98278400958921,63.9602056522253));
#53578=CARTESIAN_POINT('Ctrl Pts',(-4.31134524531351,2.36723698448027,64.));
#53579=CARTESIAN_POINT('',(0.837162017642518,4.84647736182856,64.));
#53580=CARTESIAN_POINT('Origin',(0.,0.,64.));
#53581=CARTESIAN_POINT('Ctrl Pts',(-4.91858868497457,-7.18540524887162E-5,
62.7351405640092));
#53582=CARTESIAN_POINT('Ctrl Pts',(-4.91864016628146,-0.0724457453455965,
62.7392400037402));
#53583=CARTESIAN_POINT('Ctrl Pts',(-4.89937421430555,-0.963808652612014,
62.7897305959453));
#53584=CARTESIAN_POINT('Ctrl Pts',(-4.38787150941422,-2.6531979430407,62.8866123406244));
#53585=CARTESIAN_POINT('Ctrl Pts',(-2.5800990640586,-4.43124443783022,63.0257857980463));
#53586=CARTESIAN_POINT('Ctrl Pts',(-0.141393199236074,-5.12571725998609,
63.1649592554683));
#53587=CARTESIAN_POINT('Ctrl Pts',(2.33187113869595,-4.56673182658543,63.3041327128902));
#53588=CARTESIAN_POINT('Ctrl Pts',(4.23494465804981,-2.89109992630838,63.4433061703121));
#53589=CARTESIAN_POINT('Ctrl Pts',(5.10236059910481,-0.508337431653702,
63.5824796277342));
#53590=CARTESIAN_POINT('Ctrl Pts',(4.72219820521398,1.9984257720543,63.721653085156));
#53591=CARTESIAN_POINT('Ctrl Pts',(3.18703877163087,4.01712720269185,63.8608265425781));
#53592=CARTESIAN_POINT('Ctrl Pts',(1.64440293964314,4.70703764334184,63.953608847526));
#53593=CARTESIAN_POINT('Ctrl Pts',(0.837162017642518,4.84647736182856,64.));
#53594=CARTESIAN_POINT('Origin',(0.,0.,-3.23514056400933));
#53595=CARTESIAN_POINT('',(-4.91811146816273,-0.000123935709421355,60.6398594359907));
#53596=CARTESIAN_POINT('',(-4.91799768806857,0.000106798609499636,60.9851405640092));
#53597=CARTESIAN_POINT('',(-4.91825,1.47989506776076E-12,-3.23514056400933));
#53598=CARTESIAN_POINT('Ctrl Pts',(-4.91811146816274,-0.000123935709421541,
60.6398594359907));
#53599=CARTESIAN_POINT('Ctrl Pts',(-4.91833302374643,-0.234218476711904,
60.6531154359842));
#53600=CARTESIAN_POINT('Ctrl Pts',(-4.84449183696287,-1.28741970532662,
60.7127625884516));
#53601=CARTESIAN_POINT('Ctrl Pts',(-4.10529641718065,-3.07236274745144,
60.8188008933932));
#53602=CARTESIAN_POINT('Ctrl Pts',(-2.13122625265585,-4.663769525259,60.957974350815));
#53603=CARTESIAN_POINT('Ctrl Pts',(0.364003421574487,-5.11472120786763,
61.0971478082371));
#53604=CARTESIAN_POINT('Ctrl Pts',(2.77022150230343,-4.31494430466559,61.236321265659));
#53605=CARTESIAN_POINT('Ctrl Pts',(4.49902334075878,-2.46001229778389,61.375494723081));
#53606=CARTESIAN_POINT('Ctrl Pts',(5.12765629947872,-0.00352107013592945,
61.5146681805029));
#53607=CARTESIAN_POINT('Ctrl Pts',(4.50239758982308,2.45383118170519,61.6538416379248));
#53608=CARTESIAN_POINT('Ctrl Pts',(2.77614487750337,4.31113571438885,61.7930150953468));
#53609=CARTESIAN_POINT('Ctrl Pts',(0.371027452000867,5.11421647371715,61.9321885527688));
#53610=CARTESIAN_POINT('Ctrl Pts',(-2.12481919255064,4.6666920788757,62.0713620101907));
#53611=CARTESIAN_POINT('Ctrl Pts',(-4.10107307033674,3.0779979096349,62.2105354676127));
#53612=CARTESIAN_POINT('Ctrl Pts',(-4.84361095490587,1.29192670121819,62.3167012762126));
#53613=CARTESIAN_POINT('Ctrl Pts',(-4.91832703052422,0.236470414648976,
62.3764759323386));
#53614=CARTESIAN_POINT('Ctrl Pts',(-4.91810492716115,0.000123316961498816,
62.3898594359907));
#53615=CARTESIAN_POINT('Ctrl Pts',(-4.91799768806857,0.000106798609499498,
60.9851405640092));
#53616=CARTESIAN_POINT('Ctrl Pts',(-4.91756998676071,-0.542764083599964,
61.0158795073858));
#53617=CARTESIAN_POINT('Ctrl Pts',(-4.69265409152509,-1.90528028643671,
61.0930096032364));
#53618=CARTESIAN_POINT('Ctrl Pts',(-3.45757268999299,-3.78656344121777,
61.2165308515608));
#53619=CARTESIAN_POINT('Ctrl Pts',(-1.22048811252045,-4.98028918333677,
61.355704308983));
#53620=CARTESIAN_POINT('Ctrl Pts',(1.31504858454702,-4.95615968794384,61.4948777664048));
#53621=CARTESIAN_POINT('Ctrl Pts',(3.52900980989584,-3.72007544198956,61.6340512238268));
#53622=CARTESIAN_POINT('Ctrl Pts',(4.8800044701548,-1.57430240300827,61.7732246812487));
#53623=CARTESIAN_POINT('Ctrl Pts',(5.0376669914975,0.956442797563212,61.9123981386707));
#53624=CARTESIAN_POINT('Ctrl Pts',(3.96344342536178,3.25330411499177,62.0515715960926));
#53625=CARTESIAN_POINT('Ctrl Pts',(1.92001895732006,4.75461875552336,62.1907450535146));
#53626=CARTESIAN_POINT('Ctrl Pts',(-0.592917275387842,5.09326210086,62.3299185109366));
#53627=CARTESIAN_POINT('Ctrl Pts',(-2.96086476568654,4.18642510396251,62.4690919683585));
#53628=CARTESIAN_POINT('Ctrl Pts',(-4.55635401914054,2.31272501981761,62.6041659860494));
#53629=CARTESIAN_POINT('Ctrl Pts',(-4.91805758004674,0.746570619418092,
62.6928488512663));
#53630=CARTESIAN_POINT('Ctrl Pts',(-4.91858868497457,-7.18540524887162E-5,
62.7351405640092));
#53631=CARTESIAN_POINT('Origin',(0.,0.,-3.23514056400933));
#53632=CARTESIAN_POINT('',(-4.91848050031426,0.00010358560867039,58.8898594359906));
#53633=CARTESIAN_POINT('',(-4.91823397532498,-0.000128900733881165,59.2351405640092));
#53634=CARTESIAN_POINT('',(-4.91825,1.47989506776076E-12,-3.23514056400933));
#53635=CARTESIAN_POINT('Ctrl Pts',(-4.91848050031426,0.00010358560867018,
58.8898594359906));
#53636=CARTESIAN_POINT('Ctrl Pts',(-4.91782358364168,-0.704279469166761,
58.9297549396297));
#53637=CARTESIAN_POINT('Ctrl Pts',(-4.58708483673057,-2.2283277297391,59.0160415957427));
#53638=CARTESIAN_POINT('Ctrl Pts',(-3.06791804765684,-4.10861903535706,
59.1487194043298));
#53639=CARTESIAN_POINT('Ctrl Pts',(-0.724162310693165,-5.07626442106874,
59.2878928617516));
#53640=CARTESIAN_POINT('Ctrl Pts',(1.79667649020643,-4.80258525321274,59.4270663191736));
#53641=CARTESIAN_POINT('Ctrl Pts',(3.87816492297812,-3.35450567968201,59.5662397765956));
#53642=CARTESIAN_POINT('Ctrl Pts',(5.01130611802573,-1.08613190555986,59.7054132340175));
#53643=CARTESIAN_POINT('Ctrl Pts',(4.91900734112638,1.44783918401923,59.8445866914394));
#53644=CARTESIAN_POINT('Ctrl Pts',(3.6238388779325,3.62776285217508,59.9837601488615));
#53645=CARTESIAN_POINT('Ctrl Pts',(1.44251480813104,4.92057136450247,60.1229336062833));
#53646=CARTESIAN_POINT('Ctrl Pts',(-1.09155468659011,5.01012773200588,60.2621070637055));
#53647=CARTESIAN_POINT('Ctrl Pts',(-3.35870080584726,3.87453228424406,60.4012805211271));
#53648=CARTESIAN_POINT('Ctrl Pts',(-4.66681476051984,1.9898847672322,60.5271979785559));
#53649=CARTESIAN_POINT('Ctrl Pts',(-4.91755766022277,0.58502681223606,60.6067242835102));
#53650=CARTESIAN_POINT('Ctrl Pts',(-4.91811146816274,-0.000123935709421541,
60.6398594359907));
#53651=CARTESIAN_POINT('Ctrl Pts',(-4.91823397532498,-0.000128900733881599,
59.2351405640092));
#53652=CARTESIAN_POINT('Ctrl Pts',(-4.91843338306455,-0.19414531584724,
59.2461278585573));
#53653=CARTESIAN_POINT('Ctrl Pts',(-4.85962517914547,-1.20722825103876,
59.3035063055794));
#53654=CARTESIAN_POINT('Ctrl Pts',(-4.17914144614525,-2.97113587204582,
59.4072759050756));
#53655=CARTESIAN_POINT('Ctrl Pts',(-2.24454539330572,-4.61030233004723,
59.5464493624975));
#53656=CARTESIAN_POINT('Ctrl Pts',(0.238920670469636,-5.12208829582852,
59.6856228199195));
#53657=CARTESIAN_POINT('Ctrl Pts',(2.6639622571092,-4.38134416472343,59.8247962773414));
#53658=CARTESIAN_POINT('Ctrl Pts',(4.43757171073933,-2.56920783687788,59.9639697347634));
#53659=CARTESIAN_POINT('Ctrl Pts',(5.12603936208722,-0.128810152540617,
60.1031431921853));
#53660=CARTESIAN_POINT('Ctrl Pts',(4.56101074237015,2.34308612838655,60.2423166496072));
#53661=CARTESIAN_POINT('Ctrl Pts',(2.88065515110656,4.24201573516153,60.3814901070293));
#53662=CARTESIAN_POINT('Ctrl Pts',(0.495878420013193,5.10362382919256,60.5206635644512));
#53663=CARTESIAN_POINT('Ctrl Pts',(-2.01015796326168,4.7172170354076,60.6598370218731));
#53664=CARTESIAN_POINT('Ctrl Pts',(-4.02464027668354,3.1772853572572,60.7990104792952));
#53665=CARTESIAN_POINT('Ctrl Pts',(-4.82739314863554,1.37212243363073,60.9074449933404));
#53666=CARTESIAN_POINT('Ctrl Pts',(-4.91821547272759,0.276535576824915,
60.9694883549118));
#53667=CARTESIAN_POINT('Ctrl Pts',(-4.91799768806857,0.000106798609499498,
60.9851405640092));
#53668=CARTESIAN_POINT('Origin',(0.,0.,-3.23514056400933));
#53669=CARTESIAN_POINT('',(-4.91785549949367,-4.93860172708709E-5,57.1398594359907));
#53670=CARTESIAN_POINT('',(-4.91835888437606,0.000122206298215147,57.4851405640092));
#53671=CARTESIAN_POINT('',(-4.91825,1.47989506776076E-12,-3.23514056400933));
#53672=CARTESIAN_POINT('Ctrl Pts',(-4.91785549949367,-4.93860172707736E-5,
57.1398594359907));
#53673=CARTESIAN_POINT('Ctrl Pts',(-4.91798030716673,-0.355833168158426,
57.1600032908012));
#53674=CARTESIAN_POINT('Ctrl Pts',(-4.79221627138776,-1.53089751854342,
57.2265382980858));
#53675=CARTESIAN_POINT('Ctrl Pts',(-3.86627298300154,-3.36820497383239,
57.3394644578443));
#53676=CARTESIAN_POINT('Ctrl Pts',(-1.77967451752562,-4.80891153344568,
57.4786379152663));
#53677=CARTESIAN_POINT('Ctrl Pts',(0.742116737907104,-5.07367069015669,
57.6178113726882));
#53678=CARTESIAN_POINT('Ctrl Pts',(3.08243444271975,-4.09773955140781,57.7569848301102));
#53679=CARTESIAN_POINT('Ctrl Pts',(4.66898889937891,-2.11976748307766,57.8961582875321));
#53680=CARTESIAN_POINT('Ctrl Pts',(5.1138119408897,0.376562024175001,58.0353317449541));
#53681=CARTESIAN_POINT('Ctrl Pts',(4.30812874434728,2.78080891953505,58.1745052023761));
#53682=CARTESIAN_POINT('Ctrl Pts',(2.4489570872563,4.50505057791964,58.313678659798));
#53683=CARTESIAN_POINT('Ctrl Pts',(-0.00907040374824587,5.12764948613034,
58.45285211722));
#53684=CARTESIAN_POINT('Ctrl Pts',(-2.46487986315524,4.49635839152627,58.5920255746418));
#53685=CARTESIAN_POINT('Ctrl Pts',(-4.31793981191222,2.76555009094761,58.7311990320639));
#53686=CARTESIAN_POINT('Ctrl Pts',(-4.88659449671919,1.04848275830739,58.8304769858468));
#53687=CARTESIAN_POINT('Ctrl Pts',(-4.91858745722994,0.114788814563554,
58.8833637871557));
#53688=CARTESIAN_POINT('Ctrl Pts',(-4.91848050031426,0.00010358560867018,
58.8898594359906));
#53689=CARTESIAN_POINT('Ctrl Pts',(-4.91835888437606,0.000122206298215008,
57.4851405640092));
#53690=CARTESIAN_POINT('Ctrl Pts',(-4.91767592747949,-0.664252687686942,
57.5227673622028));
#53691=CARTESIAN_POINT('Ctrl Pts',(-4.61497929133975,-2.14835763545905,
57.6067853128706));
#53692=CARTESIAN_POINT('Ctrl Pts',(-3.16739287834083,-4.03243027853956,
57.7371944160121));
#53693=CARTESIAN_POINT('Ctrl Pts',(-0.847980520678397,-5.05705454129148,
57.8763678734341));
#53694=CARTESIAN_POINT('Ctrl Pts',(1.67879279259075,-4.84505173931014,58.0155413308561));
#53695=CARTESIAN_POINT('Ctrl Pts',(3.79504243314771,-3.44826398752403,58.1547147882779));
#53696=CARTESIAN_POINT('Ctrl Pts',(4.98327119785246,-1.20825484302812,58.2938882457));
#53697=CARTESIAN_POINT('Ctrl Pts',(4.95291551110372,1.32721495505253,58.4330617031219));
#53698=CARTESIAN_POINT('Ctrl Pts',(3.71139840215604,3.53813418308582,58.5722351605439));
#53699=CARTESIAN_POINT('Ctrl Pts',(1.56231431431994,4.88385560600616,58.7114086179658));
#53700=CARTESIAN_POINT('Ctrl Pts',(-0.968810376189768,5.0353031737954,58.8505820753878));
#53701=CARTESIAN_POINT('Ctrl Pts',(-3.26302697682058,3.95544264850191,58.9897555328096));
#53702=CARTESIAN_POINT('Ctrl Pts',(-4.6411916976814,2.06995008540387,59.1179416956836));
#53703=CARTESIAN_POINT('Ctrl Pts',(-4.91759143286374,0.625041341663855,
59.1997367060834));
#53704=CARTESIAN_POINT('Ctrl Pts',(-4.91823397532498,-0.000128900733881599,
59.2351405640092));
#53705=CARTESIAN_POINT('Origin',(0.,0.,-3.23514056400933));
#53706=CARTESIAN_POINT('',(-4.91867501376679,-7.41635971235237E-6,55.3898594359907));
#53707=CARTESIAN_POINT('',(-4.91791390643375,-8.17280424678102E-5,55.7351405640092));
#53708=CARTESIAN_POINT('',(-4.91825,1.47989506776076E-12,-3.23514056400933));
#53709=CARTESIAN_POINT('Ctrl Pts',(-4.91867457786214,-7.40875330833691E-6,
55.3898594359907));
#53710=CARTESIAN_POINT('Ctrl Pts',(-4.91867518670192,-0.00693128766223378,
55.3902516419728));
#53711=CARTESIAN_POINT('Ctrl Pts',(-4.91696789858484,-0.832829426367756,
55.4370350004289));
#53712=CARTESIAN_POINT('Ctrl Pts',(-4.4902920805669,-2.47591368105495,55.530209511359));
#53713=CARTESIAN_POINT('Ctrl Pts',(-2.75493862771526,-4.32471787315188,
55.6693829687808));
#53714=CARTESIAN_POINT('Ctrl Pts',(-0.345906130887604,-5.11597698132539,
55.808556426203));
#53715=CARTESIAN_POINT('Ctrl Pts',(2.14771253755835,-4.65620042318322,55.9477298836247));
#53716=CARTESIAN_POINT('Ctrl Pts',(4.11614022189969,-3.05781968050709,56.0869033410469));
#53717=CARTESIAN_POINT('Ctrl Pts',(5.07802736785512,-0.711694861686717,
56.2260767984686));
#53718=CARTESIAN_POINT('Ctrl Pts',(4.79815885796941,1.80846429285365,56.3652502558907));
#53719=CARTESIAN_POINT('Ctrl Pts',(3.34497235117331,3.88639054840388,56.5044237133125));
#53720=CARTESIAN_POINT('Ctrl Pts',(1.07382287671086,5.01395811253837,56.6435971707346));
#53721=CARTESIAN_POINT('Ctrl Pts',(-1.45991392427294,4.91543719912591,56.7827706281565));
#53722=CARTESIAN_POINT('Ctrl Pts',(-3.63665060667076,3.61491962425697,56.9219440855785));
#53723=CARTESIAN_POINT('Ctrl Pts',(-4.73775454991443,1.74660915227116,57.0409736881899));
#53724=CARTESIAN_POINT('Ctrl Pts',(-4.91769287599503,0.463534318367552,
57.1136121383273));
#53725=CARTESIAN_POINT('Ctrl Pts',(-4.91785549949367,-4.93860172707736E-5,
57.1398594359907));
#53726=CARTESIAN_POINT('Ctrl Pts',(-4.91791390643376,-8.1728042467602E-5,
55.7351405640092));
#53727=CARTESIAN_POINT('Ctrl Pts',(-4.91809993511853,-0.315784565908389,
55.7530157133744));
#53728=CARTESIAN_POINT('Ctrl Pts',(-4.81049686766967,-1.45070185646176,
55.8172820152136));
#53729=CARTESIAN_POINT('Ctrl Pts',(-3.94741803979709,-3.27273011660468,
55.9279394695267));
#53730=CARTESIAN_POINT('Ctrl Pts',(-1.89664504433241,-4.76399088715083,
56.0671129269487));
#53731=CARTESIAN_POINT('Ctrl Pts',(0.617924134239044,-5.09028892710146,
56.2062863843707));
#53732=CARTESIAN_POINT('Ctrl Pts',(2.98138920623766,-4.17183293025696,56.3454598417926));
#53733=CARTESIAN_POINT('Ctrl Pts',(4.61580013163112,-2.23321757602816,56.4846332992146));
#53734=CARTESIAN_POINT('Ctrl Pts',(5.12148615964254,0.251497740818248,56.6238067566365));
#53735=CARTESIAN_POINT('Ctrl Pts',(4.37478933416524,2.67471304605202,56.7629802140585));
#53736=CARTESIAN_POINT('Ctrl Pts',(2.55830319774378,4.44386727360986,56.9021536714803));
#53737=CARTESIAN_POINT('Ctrl Pts',(0.116222271253945,5.12634021312587,57.0413271289025));
#53738=CARTESIAN_POINT('Ctrl Pts',(-2.35427907367985,4.55524331296145,57.1805005863242));
#53739=CARTESIAN_POINT('Ctrl Pts',(-4.24907667710245,2.87022977985227,57.3196740437464));
#53740=CARTESIAN_POINT('Ctrl Pts',(-4.87346654761257,1.12866042388539,57.4212207029745));
#53741=CARTESIAN_POINT('Ctrl Pts',(-4.91851796451275,0.154874064690948,
57.4763762097288));
#53742=CARTESIAN_POINT('Ctrl Pts',(-4.91835888437606,0.000122206298215008,
57.4851405640092));
#53743=CARTESIAN_POINT('Origin',(0.,0.,-3.23514056400933));
#53744=CARTESIAN_POINT('',(-4.91787233544528,6.11763386092418E-5,53.6398594359907));
#53745=CARTESIAN_POINT('',(-4.91865539329482,3.49302451308799E-5,53.9851405640092));
#53746=CARTESIAN_POINT('',(-4.91825,1.47989506776076E-12,-3.23514056400933));
#53747=CARTESIAN_POINT('Ctrl Pts',(-4.91787233544528,6.11763386090813E-5,
53.6398594359907));
#53748=CARTESIAN_POINT('Ctrl Pts',(-4.91766399181008,-0.477372253351672,
53.6668911456183));
#53749=CARTESIAN_POINT('Ctrl Pts',(-4.73018855874724,-1.77432527829267,
53.7403140077199));
#53750=CARTESIAN_POINT('Ctrl Pts',(-3.6059785727194,-3.64551643226655,53.8601280222955));
#53751=CARTESIAN_POINT('Ctrl Pts',(-1.41833159220866,-4.92759647489319,
53.9993014797174));
#53752=CARTESIAN_POINT('Ctrl Pts',(1.11614716940514,-5.00470648700459,54.1384749371395));
#53753=CARTESIAN_POINT('Ctrl Pts',(3.3776888316379,-3.85799036824427,54.2776483945613));
#53754=CARTESIAN_POINT('Ctrl Pts',(4.81326720014988,-1.76786039742912,54.4168218519834));
#53755=CARTESIAN_POINT('Ctrl Pts',(5.07183305260184,0.754573396941915,54.5559953094052));
#53756=CARTESIAN_POINT('Ctrl Pts',(4.09015797637785,3.09248755100316,54.6951687668272));
#53757=CARTESIAN_POINT('Ctrl Pts',(2.10829593137106,4.6741801196147,54.8343422242492));
#53758=CARTESIAN_POINT('Ctrl Pts',(-0.389118356134408,5.11287183779883,
54.9735156816711));
#53759=CARTESIAN_POINT('Ctrl Pts',(-2.79137956853432,4.30128720608217,55.1126891390931));
#53760=CARTESIAN_POINT('Ctrl Pts',(-4.50620442915501,2.44313837439632,55.251470390533));
#53761=CARTESIAN_POINT('Ctrl Pts',(-4.91860317153563,0.812043273740878,
55.3438604894988));
#53762=CARTESIAN_POINT('Ctrl Pts',(-4.91867457786214,-7.40875330833691E-6,
55.3898594359907));
#53763=CARTESIAN_POINT('Ctrl Pts',(-4.91865539329482,3.49302451308105E-5,
53.9851405640092));
#53764=CARTESIAN_POINT('Ctrl Pts',(-4.9183555947936,-0.785821442463661,
54.0296552170199));
#53765=CARTESIAN_POINT('Ctrl Pts',(-4.52666642387898,-2.39094983544162,
54.1205610225047));
#53766=CARTESIAN_POINT('Ctrl Pts',(-2.8597871012007,-4.25611199721682,54.2578579804633));
#53767=CARTESIAN_POINT('Ctrl Pts',(-0.470807616579455,-5.10599762879083,
54.3970314378853));
#53768=CARTESIAN_POINT('Ctrl Pts',(2.0333008302056,-4.70728789547995,54.5362048953072));
#53769=CARTESIAN_POINT('Ctrl Pts',(4.04019596500318,-3.15748130024849,54.6753783527292));
#53770=CARTESIAN_POINT('Ctrl Pts',(5.05912159376628,-0.835559870107751,
54.8145518101511));
#53771=CARTESIAN_POINT('Ctrl Pts',(4.84091469102418,1.69068523128142,54.9537252675731));
#53772=CARTESIAN_POINT('Ctrl Pts',(3.4389344917701,3.80349854191647,55.092898724995));
#53773=CARTESIAN_POINT('Ctrl Pts',(1.1960142884793,4.98622316175281,55.232072182417));
#53774=CARTESIAN_POINT('Ctrl Pts',(-1.33937332382694,4.94964147150757,55.3712456398389));
#53775=CARTESIAN_POINT('Ctrl Pts',(-3.54723721881863,3.70269897648656,55.5104190972609));
#53776=CARTESIAN_POINT('Ctrl Pts',(-4.7155139620973,1.82676430424734,55.6317174053177));
#53777=CARTESIAN_POINT('Ctrl Pts',(-4.91761713719032,0.503555076445749,
55.7066245609004));
#53778=CARTESIAN_POINT('Ctrl Pts',(-4.91791390643376,-8.1728042467602E-5,
55.7351405640092));
#53779=CARTESIAN_POINT('Origin',(0.,0.,-3.23514056400933));
#53780=CARTESIAN_POINT('',(-4.91843986782789,-0.000111326259341174,51.8898594359907));
#53781=CARTESIAN_POINT('',(-4.91783388548041,2.58376204584354E-5,52.2351405640092));
#53782=CARTESIAN_POINT('',(-4.91825,1.47989506776076E-12,-3.23514056400933));
#53783=CARTESIAN_POINT('Ctrl Pts',(-4.91843986782789,-0.000111326259340933,
51.8898594359907));
#53784=CARTESIAN_POINT('Ctrl Pts',(-4.91856549876998,-0.128648965742937,
51.8971394967898));
#53785=CARTESIAN_POINT('Ctrl Pts',(-4.88216901645989,-1.07620347337075,
51.950810710063));
#53786=CARTESIAN_POINT('Ctrl Pts',(-4.29441973117786,-2.80193338559416,
52.0508730758102));
#53787=CARTESIAN_POINT('Ctrl Pts',(-2.42680243173636,-4.51702352021277,
52.190046533232));
#53788=CARTESIAN_POINT('Ctrl Pts',(0.0342531119126611,-5.12754310066344,
52.3292199906541));
#53789=CARTESIAN_POINT('Ctrl Pts',(2.48693256926547,-4.48419869327436,52.468393448076));
#53790=CARTESIAN_POINT('Ctrl Pts',(4.33146985646582,-2.74431055228173,52.6075669054979));
#53791=CARTESIAN_POINT('Ctrl Pts',(5.1168109631927,-0.333342304227799,52.7467403629199));
#53792=CARTESIAN_POINT('Ctrl Pts',(4.65091246580963,2.15913981951461,52.8859138203419));
#53793=CARTESIAN_POINT('Ctrl Pts',(3.04770287479204,4.12363658823389,53.0250872777638));
#53794=CARTESIAN_POINT('Ctrl Pts',(0.699223121180822,5.07975969428112,53.1642607351858));
#53795=CARTESIAN_POINT('Ctrl Pts',(-1.82024119051244,4.79370352996499,53.3034341926077));
#53796=CARTESIAN_POINT('Ctrl Pts',(-3.89459273900518,3.33541885257685,53.4426076500297));
#53797=CARTESIAN_POINT('Ctrl Pts',(-4.79865591701777,1.50316999994343,53.554749397824));
#53798=CARTESIAN_POINT('Ctrl Pts',(-4.91802154601144,0.341987207742299,
53.6204999931443));
#53799=CARTESIAN_POINT('Ctrl Pts',(-4.91787233544528,6.11763386090813E-5,
53.6398594359907));
#53800=CARTESIAN_POINT('Ctrl Pts',(-4.91783388548041,2.58376204580538E-5,
52.2351405640092));
#53801=CARTESIAN_POINT('Ctrl Pts',(-4.91775404158717,-0.437347553613739,
52.2599035681915));
#53802=CARTESIAN_POINT('Ctrl Pts',(-4.75171544922939,-1.69415819232811,
52.3310577248477));
#53803=CARTESIAN_POINT('Ctrl Pts',(-3.69397722364766,-3.5563188648122,52.448603033978));
#53804=CARTESIAN_POINT('Ctrl Pts',(-1.53830997137995,-4.891469516311,52.5877764913998));
#53805=CARTESIAN_POINT('Ctrl Pts',(0.993527980457018,-5.03048444477228,
52.7269499488219));
#53806=CARTESIAN_POINT('Ctrl Pts',(3.28241352191931,-3.93936962827405,52.8661234062438));
#53807=CARTESIAN_POINT('Ctrl Pts',(4.76863392190279,-1.88494087862853,53.0052968636658));
#53808=CARTESIAN_POINT('Ctrl Pts',(5.08875620657422,0.630421975425304,53.1444703210877));
#53809=CARTESIAN_POINT('Ctrl Pts',(4.16449925833512,2.9916245627373,53.2836437785097));
#53810=CARTESIAN_POINT('Ctrl Pts',(2.22187629251225,4.62127010007193,53.4228172359315));
#53811=CARTESIAN_POINT('Ctrl Pts',(-0.264073294642276,5.12085314104043,
53.5619906933537));
#53812=CARTESIAN_POINT('Ctrl Pts',(-2.68544770655171,4.36820812375314,53.7011641507754));
#53813=CARTESIAN_POINT('Ctrl Pts',(-4.45013604008643,2.54738313211239,53.8403376081976));
#53814=CARTESIAN_POINT('Ctrl Pts',(-4.9102397975167,0.885267346271903,53.9349964126087));
#53815=CARTESIAN_POINT('Ctrl Pts',(-4.91866803119467,0.0331624278634732,
53.9832640645459));
#53816=CARTESIAN_POINT('Ctrl Pts',(-4.91865539329482,3.49302451308105E-5,
53.9851405640092));
#53817=CARTESIAN_POINT('Origin',(0.,0.,-3.23514056400933));
#53818=CARTESIAN_POINT('',(-4.91815264668802,0.000126960182705925,50.1398594359907));
#53819=CARTESIAN_POINT('',(-4.91855089394144,-8.54444238024277E-5,50.4851405640092));
#53820=CARTESIAN_POINT('',(-4.91825,1.47989506776076E-12,-3.23514056400933));
#53821=CARTESIAN_POINT('Ctrl Pts',(-4.91815264668802,0.000126960182705964,
50.1398594359907));
#53822=CARTESIAN_POINT('Ctrl Pts',(-4.91756388563138,-0.598861721200149,
50.1737790004354));
#53823=CARTESIAN_POINT('Ctrl Pts',(-4.65808367092927,-2.01757209091749,
50.254089717354));
#53824=CARTESIAN_POINT('Ctrl Pts',(-3.32584524149952,-3.90277144532342,
50.3807915867467));
#53825=CARTESIAN_POINT('Ctrl Pts',(-1.0491854679113,-5.01917138368084,50.5199650441687));
#53826=CARTESIAN_POINT('Ctrl Pts',(1.48403692230487,-4.90820801699284,50.6591385015906));
#53827=CARTESIAN_POINT('Ctrl Pts',(3.65436027550235,-3.59701577723358,50.7983119590126));
#53828=CARTESIAN_POINT('Ctrl Pts',(4.93106447073476,-1.40622711902959,50.9374854164345));
#53829=CARTESIAN_POINT('Ctrl Pts',(5.00195058892939,1.12843335237216,51.0766588738565));
#53830=CARTESIAN_POINT('Ctrl Pts',(3.8496844899148,3.38715232207621,51.2158323312784));
#53831=CARTESIAN_POINT('Ctrl Pts',(1.75603561718453,4.81759384299012,51.3550057887004));
#53832=CARTESIAN_POINT('Ctrl Pts',(-0.767025505920936,5.06996483203814,
51.4941792461224));
#53833=CARTESIAN_POINT('Ctrl Pts',(-3.10252201167498,4.08255173781169,51.6333527035442));
#53834=CARTESIAN_POINT('Ctrl Pts',(-4.59686080493138,2.20068426365062,51.7652461001671));
#53835=CARTESIAN_POINT('Ctrl Pts',(-4.91776493345185,0.690438868332923,
51.8507483443159));
#53836=CARTESIAN_POINT('Ctrl Pts',(-4.91843986782789,-0.000111326259340933,
51.8898594359907));
#53837=CARTESIAN_POINT('Ctrl Pts',(-4.91855089394144,-8.5444423802896E-5,
50.4851405640092));
#53838=CARTESIAN_POINT('Ctrl Pts',(-4.91862266471435,-0.0885607691173009,
50.490151919363));
#53839=CARTESIAN_POINT('Ctrl Pts',(-4.89464160083773,-0.996031568323749,
50.5415544271908));
#53840=CARTESIAN_POINT('Ctrl Pts',(-4.36160057317046,-2.69616617387836,
50.6393480874925));
#53841=CARTESIAN_POINT('Ctrl Pts',(-2.53644770583317,-4.45637797236955,
50.7785215449146));
#53842=CARTESIAN_POINT('Ctrl Pts',(-0.0910444821465626,-5.12684917852256,
50.9176950023364));
#53843=CARTESIAN_POINT('Ctrl Pts',(2.37662230816716,-4.54362608511847,51.0568684597585));
#53844=CARTESIAN_POINT('Ctrl Pts',(4.26312165309721,-2.84932717811426,51.1960419171803));
#53845=CARTESIAN_POINT('Ctrl Pts',(5.10713834860655,-0.458267918623071,
51.3352153746024));
#53846=CARTESIAN_POINT('Ctrl Pts',(4.70228073325844,2.04485390741571,51.4743888320243));
#53847=CARTESIAN_POINT('Ctrl Pts',(3.14755068263376,4.04793728920033,51.6135622894463));
#53848=CARTESIAN_POINT('Ctrl Pts',(0.823134181134756,5.06115813988206,51.7527357468682));
#53849=CARTESIAN_POINT('Ctrl Pts',(-1.70256747518846,4.83674845216052,51.8919092042902));
#53850=CARTESIAN_POINT('Ctrl Pts',(-3.8119317156975,3.42958425933908,52.0310826617121));
#53851=CARTESIAN_POINT('Ctrl Pts',(-4.77968458069813,1.58336278879033,52.1454931149518));
#53852=CARTESIAN_POINT('Ctrl Pts',(-4.91790362158959,0.382030238009249,
52.2135124157175));
#53853=CARTESIAN_POINT('Ctrl Pts',(-4.91783388548041,2.58376204580538E-5,
52.2351405640092));
#53854=CARTESIAN_POINT('Origin',(0.,0.,-3.23514056400933));
#53855=CARTESIAN_POINT('',(-4.91806577589784,-0.000118764820635008,48.3898594359907));
#53856=CARTESIAN_POINT('',(-4.91803852105498,0.000114651850740416,48.7351405640092));
#53857=CARTESIAN_POINT('',(-4.91825,1.47989506776076E-12,-3.23514056400933));
#53858=CARTESIAN_POINT('Ctrl Pts',(-4.91806577589784,-0.000118764820635602,
48.3898594359907));
#53859=CARTESIAN_POINT('Ctrl Pts',(-4.91828944893322,-0.250323965044822,
48.4040273516069));
#53860=CARTESIAN_POINT('Ctrl Pts',(-4.83812024217588,-1.31965428743371,
48.4645864196971));
#53861=CARTESIAN_POINT('Ctrl Pts',(-4.07492088157485,-3.11253776422747,
48.5715366402614));
#53862=CARTESIAN_POINT('Ctrl Pts',(-2.08531475831404,-4.68447797343466,
48.7107100976832));
#53863=CARTESIAN_POINT('Ctrl Pts',(0.414223905235385,-5.11089914605722,
48.8498835551053));
#53864=CARTESIAN_POINT('Ctrl Pts',(2.81247030707573,-4.28752636104482,48.9890570125271));
#53865=CARTESIAN_POINT('Ctrl Pts',(4.52296915308285,-2.41570312023185,49.1282304699492));
#53866=CARTESIAN_POINT('Ctrl Pts',(5.12744352931481,0.0468441941396368,
49.2674039273711));
#53867=CARTESIAN_POINT('Ctrl Pts',(4.47807826639135,2.49793646134371,49.4065773847931));
#53868=CARTESIAN_POINT('Ctrl Pts',(2.73366592873352,4.33819572114011,49.545750842215));
#53869=CARTESIAN_POINT('Ctrl Pts',(0.320776467523109,5.11761409083573,49.6849242996369));
#53870=CARTESIAN_POINT('Ctrl Pts',(-2.17055408191953,4.64559646356626,49.8240977570589));
#53871=CARTESIAN_POINT('Ctrl Pts',(-4.13110808915714,3.03756769151527,49.9632712144808));
#53872=CARTESIAN_POINT('Ctrl Pts',(-4.84983985353235,1.25969268032143,50.0685251074581));
#53873=CARTESIAN_POINT('Ctrl Pts',(-4.91836912309232,0.220363870376499,
50.1273878479614));
#53874=CARTESIAN_POINT('Ctrl Pts',(-4.91815264668802,0.000126960182705964,
50.1398594359907));
#53875=CARTESIAN_POINT('Ctrl Pts',(-4.91803852105498,0.00011465185073993,
48.7351405640092));
#53876=CARTESIAN_POINT('Ctrl Pts',(-4.91756009930081,-0.558847982386848,
48.7667914230085));
#53877=CARTESIAN_POINT('Ctrl Pts',(-4.68296776004553,-1.93748212711608,
48.8448334344818));
#53878=CARTESIAN_POINT('Ctrl Pts',(-3.4202133466128,-3.8203419036388,48.9692665984293));
#53879=CARTESIAN_POINT('Ctrl Pts',(-1.17151161743895,-4.99203687158382,
49.108440055851));
#53880=CARTESIAN_POINT('Ctrl Pts',(1.36366575896105,-4.94300387364647,49.2476135132731));
#53881=CARTESIAN_POINT('Ctrl Pts',(3.56537906630424,-3.68523319623146,49.386786970695));
#53882=CARTESIAN_POINT('Ctrl Pts',(4.89523223976419,-1.52629384976162,49.5259604281169));
#53883=CARTESIAN_POINT('Ctrl Pts',(5.02802957243399,1.00587783342514,49.6651338855389));
#53884=CARTESIAN_POINT('Ctrl Pts',(3.93129746246441,3.29207713437395,49.8043073429608));
#53885=CARTESIAN_POINT('Ctrl Pts',(1.87322534678482,4.77324820192809,49.9434808003828));
#53886=CARTESIAN_POINT('Ctrl Pts',(-0.642916015185119,5.08719280099207,
50.0826542578048));
#53887=CARTESIAN_POINT('Ctrl Pts',(-3.00184187982617,4.15714047460132,50.2218277152267));
#53888=CARTESIAN_POINT('Ctrl Pts',(-4.56820390101119,2.28061542819862,50.3559898172948));
#53889=CARTESIAN_POINT('Ctrl Pts',(-4.91795826783286,0.730473601480565,
50.443760766889));
#53890=CARTESIAN_POINT('Ctrl Pts',(-4.91855089394144,-8.5444423802896E-5,
50.4851405640092));
#53891=CARTESIAN_POINT('Origin',(0.,0.,-3.23514056400933));
#53892=CARTESIAN_POINT('',(-4.91852492696798,9.29568479803354E-5,46.6398594359908));
#53893=CARTESIAN_POINT('',(-4.91818357904255,-0.000128304591264783,46.9851405640093));
#53894=CARTESIAN_POINT('',(-4.91825,1.47989506776076E-12,-3.23514056400933));
#53895=CARTESIAN_POINT('Ctrl Pts',(-4.91852492696797,9.29568479802155E-5,
46.6398594359907));
#53896=CARTESIAN_POINT('Ctrl Pts',(-4.91790253050555,-0.720371784076569,
46.6806668552525));
#53897=CARTESIAN_POINT('Ctrl Pts',(-4.57554428714781,-2.26045534775418,
46.7678654269881));
#53898=CARTESIAN_POINT('Ctrl Pts',(-3.02741419179187,-4.13855467961632,
46.901455151198));
#53899=CARTESIAN_POINT('Ctrl Pts',(-0.674267066511626,-5.08313244445339,
47.0406286086197));
#53900=CARTESIAN_POINT('Ctrl Pts',(1.84376198687486,-4.78470618330867,47.179802066042));
#53901=CARTESIAN_POINT('Ctrl Pts',(3.91092661804106,-3.31625157567016,47.3189755234636));
#53902=CARTESIAN_POINT('Ctrl Pts',(5.02173262887484,-1.03685723652329,47.4581489808859));
#53903=CARTESIAN_POINT('Ctrl Pts',(4.90454902045194,1.49608503462231,47.5973224383075));
#53904=CARTESIAN_POINT('Ctrl Pts',(3.58803129184512,3.66318208304981,47.7364958957298));
#53905=CARTESIAN_POINT('Ctrl Pts',(1.39411416634107,4.93450273239808,47.8756693531515));
#53906=CARTESIAN_POINT('Ctrl Pts',(-1.14071273091822,4.99916452923466,48.0148428105736));
#53907=CARTESIAN_POINT('Ctrl Pts',(-3.39659538808254,3.84135539809756,48.1540162679954));
#53908=CARTESIAN_POINT('Ctrl Pts',(-4.67679570780214,1.95769151108293,48.2790218098013));
#53909=CARTESIAN_POINT('Ctrl Pts',(-4.91755705821536,0.568943166959013,
48.3576361991329));
#53910=CARTESIAN_POINT('Ctrl Pts',(-4.91806577589784,-0.000118764820635602,
48.3898594359907));
#53911=CARTESIAN_POINT('Ctrl Pts',(-4.91818357904256,-0.000128304591265078,
46.9851405640093));
#53912=CARTESIAN_POINT('Ctrl Pts',(-4.91839457111651,-0.210253745911707,
46.9970397741801));
#53913=CARTESIAN_POINT('Ctrl Pts',(-4.853665043705,-1.23946090468466,47.055330136825));
#53914=CARTESIAN_POINT('Ctrl Pts',(-4.14975662342901,-3.01204109589393,
47.1600116519437));
#53915=CARTESIAN_POINT('Ctrl Pts',(-2.19915360039652,-4.63212640575685,
47.2991851093658));
#53916=CARTESIAN_POINT('Ctrl Pts',(0.289219549406528,-5.11949447204388,
47.4383585667875));
#53917=CARTESIAN_POINT('Ctrl Pts',(2.7068683833997,-4.35496672226068,47.5775320242097));
#53918=CARTESIAN_POINT('Ctrl Pts',(4.4625930328204,-2.52549698484668,47.7167054816315));
#53919=CARTESIAN_POINT('Ctrl Pts',(5.12705728980988,-0.0784547261432202,
47.8558789390536));
#53920=CARTESIAN_POINT('Ctrl Pts',(4.53777635673904,2.38777246262433,47.9950523964754));
#53921=CARTESIAN_POINT('Ctrl Pts',(2.83885007366626,4.27010560247541,48.1342258538975));
#53922=CARTESIAN_POINT('Ctrl Pts',(0.445725457324341,5.10824827252355,48.2733993113193));
#53923=CARTESIAN_POINT('Ctrl Pts',(-2.0563946542149,4.69724521641816,48.4125727687414));
#53924=CARTESIAN_POINT('Ctrl Pts',(-4.05565420445089,3.13760108537823,48.5517462261632));
#53925=CARTESIAN_POINT('Ctrl Pts',(-4.83403602491591,1.33988709455419,48.659268824586));
#53926=CARTESIAN_POINT('Ctrl Pts',(-4.91826132944894,0.260432176572912,
48.7204002705346));
#53927=CARTESIAN_POINT('Ctrl Pts',(-4.91803852105498,0.00011465185073993,
48.7351405640092));
#53928=CARTESIAN_POINT('Origin',(0.,0.,-3.23514056400933));
#53929=CARTESIAN_POINT('',(-4.91784060085492,-3.50728131554851E-5,44.8898594359907));
#53930=CARTESIAN_POINT('',(-4.9184091500483,0.000116117112846786,45.2351405640092));
#53931=CARTESIAN_POINT('',(-4.91825,1.47989506776076E-12,-3.23514056400933));
#53932=CARTESIAN_POINT('Ctrl Pts',(-4.91784060085492,-3.50728131557135E-5,
44.8898594359907));
#53933=CARTESIAN_POINT('Ctrl Pts',(-4.9179329091661,-0.371928468127181,
44.910915206424));
#53934=CARTESIAN_POINT('Ctrl Pts',(-4.78457091277955,-1.5631312913108,44.9783621293313));
#53935=CARTESIAN_POINT('Ctrl Pts',(-3.83300314301673,-3.40601797271547,
45.0922002047124));
#53936=CARTESIAN_POINT('Ctrl Pts',(-1.73235436152806,-4.82615995289543,
45.2313736621346));
#53937=CARTESIAN_POINT('Ctrl Pts',(0.791915773395165,-5.06613668713003,
45.3705471195564));
#53938=CARTESIAN_POINT('Ctrl Pts',(3.12253474826594,-4.06726545368122,45.5097205769784));
#53939=CARTESIAN_POINT('Ctrl Pts',(4.68958454492302,-2.07380527553964,45.6488940344003));
#53940=CARTESIAN_POINT('Ctrl Pts',(5.10986656930181,0.426772970991213,45.7880674918224));
#53941=CARTESIAN_POINT('Ctrl Pts',(4.28060713724999,2.82299026944149,45.9272409492442));
#53942=CARTESIAN_POINT('Ctrl Pts',(2.40458924210636,4.52888751257782,46.0664144066663));
#53943=CARTESIAN_POINT('Ctrl Pts',(-0.0594349938974569,5.12731303962781,
46.205587864088));
#53944=CARTESIAN_POINT('Ctrl Pts',(-2.50892529093627,4.47193083682398,46.3447613215102));
#53945=CARTESIAN_POINT('Ctrl Pts',(-4.34489542661782,2.72300482125766,46.4839347789319));
#53946=CARTESIAN_POINT('Ctrl Pts',(-4.89158902769067,1.01625748485721,46.5823008170923));
#53947=CARTESIAN_POINT('Ctrl Pts',(-4.91861009030007,0.0986751013434063,
46.6342757027785));
#53948=CARTESIAN_POINT('Ctrl Pts',(-4.91852492696797,9.29568479802155E-5,
46.6398594359907));
#53949=CARTESIAN_POINT('Ctrl Pts',(-4.9184091500483,0.000116117112846665,
45.2351405640092));
#53950=CARTESIAN_POINT('Ctrl Pts',(-4.91772730570839,-0.680340376321463,
45.2736792778256));
#53951=CARTESIAN_POINT('Ctrl Pts',(-4.60390647175906,-2.18050870666077,
45.358609144116));
#53952=CARTESIAN_POINT('Ctrl Pts',(-3.12763256847743,-4.06334666422225,
45.4899301628804));
#53953=CARTESIAN_POINT('Ctrl Pts',(-0.798267987718407,-5.06513966409919,
45.6291036203023));
#53954=CARTESIAN_POINT('Ctrl Pts',(1.72630109211463,-4.82832850336539,45.7682770777242));
#53955=CARTESIAN_POINT('Ctrl Pts',(3.82872905502739,-3.41082181009738,45.9074505351462));
#53956=CARTESIAN_POINT('Ctrl Pts',(4.99489858245798,-1.15924964869784,46.0466239925681));
#53957=CARTESIAN_POINT('Ctrl Pts',(4.93964035540605,1.37579967883806,46.1857974499902));
#53958=CARTESIAN_POINT('Ctrl Pts',(3.67646694696398,3.57441776866221,46.3249709074119));
#53959=CARTESIAN_POINT('Ctrl Pts',(1.51426852463472,4.89896544510649,46.4641443648341));
#53960=CARTESIAN_POINT('Ctrl Pts',(-1.01822162097875,5.02554438122063,46.6033178222559));
#53961=CARTESIAN_POINT('Ctrl Pts',(-3.30172089569737,3.92320159104299,46.7424912796779));
#53962=CARTESIAN_POINT('Ctrl Pts',(-4.65162733209287,2.0377723478988,46.869765526929));
#53963=CARTESIAN_POINT('Ctrl Pts',(-4.91757198160569,0.608957045980571,
46.9506486217061));
#53964=CARTESIAN_POINT('Ctrl Pts',(-4.91818357904256,-0.000128304591265078,
46.9851405640093));
#53965=CARTESIAN_POINT('Origin',(0.,0.,-3.23514056400933));
#53966=CARTESIAN_POINT('',(-4.91866555055193,-2.44668497558952E-5,43.1398594359907));
#53967=CARTESIAN_POINT('',(-4.91788690158348,-6.94023299557811E-5,43.4851405640093));
#53968=CARTESIAN_POINT('',(-4.91825,1.47989506776076E-12,-3.23514056400933));
#53969=CARTESIAN_POINT('Ctrl Pts',(-4.91866555055193,-2.44668497561802E-5,
43.1398594359907));
#53970=CARTESIAN_POINT('Ctrl Pts',(-4.91867189362211,-0.0230471355164739,
43.1411635575955));
#53971=CARTESIAN_POINT('Ctrl Pts',(-4.91288415686364,-0.865045545929546,
43.1888588316743));
#53972=CARTESIAN_POINT('Ctrl Pts',(-4.4657564416411,-2.51989899178081,43.2829452582272));
#53973=CARTESIAN_POINT('Ctrl Pts',(-2.71232729414031,-4.35156893249991,
43.4221187156491));
#53974=CARTESIAN_POINT('Ctrl Pts',(-0.29563906707815,-5.11912776426357,
43.5612921730711));
#53975=CARTESIAN_POINT('Ctrl Pts',(2.19334327284283,-4.63488045286089,43.700465630493));
#53976=CARTESIAN_POINT('Ctrl Pts',(4.14597631470871,-3.01724243684715,43.8396390879149));
#53977=CARTESIAN_POINT('Ctrl Pts',(5.08477284786202,-0.661782902832914,
43.978812545337));
#53978=CARTESIAN_POINT('Ctrl Pts',(4.78016421891062,1.85550574374848,44.1179860027588));
#53979=CARTESIAN_POINT('Ctrl Pts',(3.30663791293829,3.91905820798263,44.2571594601809));
#53980=CARTESIAN_POINT('Ctrl Pts',(1.0245227529157,5.02426359316417,44.3963329176028));
#53981=CARTESIAN_POINT('Ctrl Pts',(-1.50812412558962,4.90086044962019,44.5355063750247));
#53982=CARTESIAN_POINT('Ctrl Pts',(-3.67198180171369,3.57902517073021,44.6746798324467));
#53983=CARTESIAN_POINT('Ctrl Pts',(-4.74638679107565,1.71438527582161,44.7927975194353));
#53984=CARTESIAN_POINT('Ctrl Pts',(-4.91772953076433,0.447446119031382,
44.86452405395));
#53985=CARTESIAN_POINT('Ctrl Pts',(-4.91784060085492,-3.50728131557135E-5,
44.8898594359907));
#53986=CARTESIAN_POINT('Ctrl Pts',(-4.91788690158348,-6.94023299559199E-5,
43.4851405640093));
#53987=CARTESIAN_POINT('Ctrl Pts',(-4.91805177856022,-0.331883298593633,
43.5039276289972));
#53988=CARTESIAN_POINT('Ctrl Pts',(-4.80327533823206,-1.48293720817835,
43.5691058464591));
#53989=CARTESIAN_POINT('Ctrl Pts',(-3.91508206282783,-3.3113447477378,43.680675216395));
#53990=CARTESIAN_POINT('Ctrl Pts',(-1.84976046732335,-4.78239038667639,
43.8198486738169));
#53991=CARTESIAN_POINT('Ctrl Pts',(0.667892389093657,-5.08397397255705,
43.9590221312389));
#53992=CARTESIAN_POINT('Ctrl Pts',(3.02222214943982,-4.14234774934242,44.0981955886608));
#53993=CARTESIAN_POINT('Ctrl Pts',(4.63751267753772,-2.18777232881387,44.2373690460827));
#53994=CARTESIAN_POINT('Ctrl Pts',(5.1187688298422,0.301790098715543,44.3765425035047));
#53995=CARTESIAN_POINT('Ctrl Pts',(4.34830661102557,2.71755427058194,44.5157159609267));
#53996=CARTESIAN_POINT('Ctrl Pts',(2.51453103518521,4.46878118396249,44.6548894183486));
#53997=CARTESIAN_POINT('Ctrl Pts',(0.0658644970599633,5.12723448508783,
44.7940628757706));
#53998=CARTESIAN_POINT('Ctrl Pts',(-2.3989082188817,4.5318992656974,44.9332363331925));
#53999=CARTESIAN_POINT('Ctrl Pts',(-4.27706380323859,2.82835585103309,45.0724097906145));
#54000=CARTESIAN_POINT('Ctrl Pts',(-4.87886413646883,1.09643166737844,45.1730445342201));
#54001=CARTESIAN_POINT('Ctrl Pts',(-4.91854807894143,0.138762230195914,
45.2272881253516));
#54002=CARTESIAN_POINT('Ctrl Pts',(-4.9184091500483,0.000116117112846665,
45.2351405640092));
#54003=CARTESIAN_POINT('Origin',(0.,0.,-3.23514056400933));
#54004=CARTESIAN_POINT('',(-4.91789641267672,7.41105149974438E-5,41.3898594359907));
#54005=CARTESIAN_POINT('',(-4.91866999096577,1.81579422332736E-5,41.7351405640092));
#54006=CARTESIAN_POINT('',(-4.91825,1.47989506776076E-12,-3.23514056400933));
#54007=CARTESIAN_POINT('Ctrl Pts',(-4.91789641267672,7.41105149971999E-5,
41.3898594359907));
#54008=CARTESIAN_POINT('Ctrl Pts',(-4.9176339004058,-0.493458636834103,
41.4178030612411));
#54009=CARTESIAN_POINT('Ctrl Pts',(-4.72122846096945,-1.80654367572432,
41.4921378389654));
#54010=CARTESIAN_POINT('Ctrl Pts',(-3.56999746819571,-3.68075937843173,
41.6128637691637));
#54011=CARTESIAN_POINT('Ctrl Pts',(-1.36986311464964,-4.94128997043882,
41.7520372265857));
#54012=CARTESIAN_POINT('Ctrl Pts',(1.16525077861143,-4.99350199236792,41.8912106840076));
#54013=CARTESIAN_POINT('Ctrl Pts',(3.4154200191569,-3.82462777503633,42.0303841414296));
#54014=CARTESIAN_POINT('Ctrl Pts',(4.83039936830708,-1.72049802891365,42.1695575988515));
#54015=CARTESIAN_POINT('Ctrl Pts',(5.06417678586922,0.804353781802734,42.3087310562735));
#54016=CARTESIAN_POINT('Ctrl Pts',(4.05958550029279,3.13251290350884,42.4479045136954));
#54017=CARTESIAN_POINT('Ctrl Pts',(2.06228328777852,4.69466283835021,42.5870779711175));
#54018=CARTESIAN_POINT('Ctrl Pts',(-0.439319463318189,5.10880318019658,
42.7262514285393));
#54019=CARTESIAN_POINT('Ctrl Pts',(-2.83349320925637,4.2736621015161,42.8654248859613));
#54020=CARTESIAN_POINT('Ctrl Pts',(-4.51883670867307,2.41107924578458,43.0032942217785));
#54021=CARTESIAN_POINT('Ctrl Pts',(-4.91844625336389,0.795931806725344,
43.0947724051215));
#54022=CARTESIAN_POINT('Ctrl Pts',(-4.91866555055193,-2.44668497561802E-5,
43.1398594359907));
#54023=CARTESIAN_POINT('Ctrl Pts',(-4.91866999096577,1.81579422333582E-5,
41.7351405640093));
#54024=CARTESIAN_POINT('Ctrl Pts',(-4.91850286965307,-0.801930133740765,
41.7805671326427));
#54025=CARTESIAN_POINT('Ctrl Pts',(-4.5141559940908,-2.42301760416976,41.8723848537502));
#54026=CARTESIAN_POINT('Ctrl Pts',(-2.81784457349484,-4.28399621342882,
42.0105937273315));
#54027=CARTESIAN_POINT('Ctrl Pts',(-0.420632547238203,-5.1103757060759,
42.1497671847535));
#54028=CARTESIAN_POINT('Ctrl Pts',(2.07943887829429,-4.68708924050791,42.2889406421754));
#54029=CARTESIAN_POINT('Ctrl Pts',(4.07101462212891,-3.11764519204149,42.4281140995974));
#54030=CARTESIAN_POINT('Ctrl Pts',(5.06708461819206,-0.785827633217498,
42.5672875570193));
#54031=CARTESIAN_POINT('Ctrl Pts',(4.82407484420597,1.73815232202072,42.7064610144413));
#54032=CARTESIAN_POINT('Ctrl Pts',(3.40140970642374,3.83709311928876,42.8456344718632));
#54033=CARTESIAN_POINT('Ctrl Pts',(1.14698068971451,4.99773017423599,42.9848079292852));
#54034=CARTESIAN_POINT('Ctrl Pts',(-1.38792530268207,4.93624705127506,43.1239813867072));
#54035=CARTESIAN_POINT('Ctrl Pts',(-3.58343491738278,3.66767852870569,43.2631548441291));
#54036=CARTESIAN_POINT('Ctrl Pts',(-4.7245853073055,1.79454803810771,43.3835412365631));
#54037=CARTESIAN_POINT('Ctrl Pts',(-4.9176446456221,0.48746922211443,43.4575364765232));
#54038=CARTESIAN_POINT('Ctrl Pts',(-4.91788690158348,-6.94023299559199E-5,
43.4851405640093));
#54039=CARTESIAN_POINT('Origin',(0.,0.,-3.23514056400933));
#54040=CARTESIAN_POINT('',(-4.9183905850055,-0.000118608231170829,39.6398594359908));
#54041=CARTESIAN_POINT('',(-4.9178455584335,4.04671957601743E-5,39.9851405640093));
#54042=CARTESIAN_POINT('',(-4.91825,1.47989506776076E-12,-3.23514056400933));
#54043=CARTESIAN_POINT('Ctrl Pts',(-4.9183905850055,-0.000118608231171394,
39.6398594359908));
#54044=CARTESIAN_POINT('Ctrl Pts',(-4.91853719113951,-0.144761324033651,
39.6480514124127));
#54045=CARTESIAN_POINT('Ctrl Pts',(-4.87687342658784,-1.10843139516826,
39.7026345413085));
#54046=CARTESIAN_POINT('Ctrl Pts',(-4.26669129572166,-2.84397906318768,
39.8036088226782));
#54047=CARTESIAN_POINT('Ctrl Pts',(-2.3823180541456,-4.54064226885678,39.9427822801004));
#54048=CARTESIAN_POINT('Ctrl Pts',(0.0846154423188459,-5.12695930857248,
40.0819557375222));
#54049=CARTESIAN_POINT('Ctrl Pts',(2.53085749770598,-4.45955511807427,40.2211291949443));
#54050=CARTESIAN_POINT('Ctrl Pts',(4.35821619854518,-2.70163341176691,40.3603026523661));
#54051=CARTESIAN_POINT('Ctrl Pts',(5.11983830092096,-0.283067654915984,
40.4994761097881));
#54052=CARTESIAN_POINT('Ctrl Pts',(4.62948050901625,2.20471806394278,40.6386495672101));
#54053=CARTESIAN_POINT('Ctrl Pts',(3.00705248801675,4.15337294968188,40.7778230246319));
#54054=CARTESIAN_POINT('Ctrl Pts',(0.649294748622445,5.08638259023525,40.916996482054));
#54055=CARTESIAN_POINT('Ctrl Pts',(-1.86723831197507,4.77559343025863,41.0561699394759));
#54056=CARTESIAN_POINT('Ctrl Pts',(-3.92716616611468,3.29700431127425,41.1953433968979));
#54057=CARTESIAN_POINT('Ctrl Pts',(-4.80598396548452,1.47093491011835,41.3065732290695));
#54058=CARTESIAN_POINT('Ctrl Pts',(-4.91806971525364,0.325889344254859,
41.3714119087671));
#54059=CARTESIAN_POINT('Ctrl Pts',(-4.91789641267672,7.41105149971999E-5,
41.3898594359907));
#54060=CARTESIAN_POINT('Ctrl Pts',(-4.9178455584335,4.04671957601049E-5,
39.9851405640093));
#54061=CARTESIAN_POINT('Ctrl Pts',(-4.91771552974485,-0.453436438311404,
40.0108154838143));
#54062=CARTESIAN_POINT('Ctrl Pts',(-4.74319322071268,-1.72638364779156,
40.0828815560932));
#54063=CARTESIAN_POINT('Ctrl Pts',(-3.65886799445027,-3.59243045809301,
40.2013387808461));
#54064=CARTESIAN_POINT('Ctrl Pts',(-1.49019055396033,-4.90634321159193,
40.3405122382681));
#54065=CARTESIAN_POINT('Ctrl Pts',(1.04289070214805,-5.02048310229404,40.4796856956901));
#54066=CARTESIAN_POINT('Ctrl Pts',(3.32094863246379,-3.90693892677934,40.618859153112));
#54067=CARTESIAN_POINT('Ctrl Pts',(4.7869182362722,-1.83801126119823,40.758032610534));
#54068=CARTESIAN_POINT('Ctrl Pts',(5.0823185691137,0.680374572635465,40.8972060679559));
#54069=CARTESIAN_POINT('Ctrl Pts',(4.13491389701701,3.03238497907216,41.0363795253779));
#54070=CARTESIAN_POINT('Ctrl Pts',(2.17637786502656,4.64287098524924,41.1755529827997));
#54071=CARTESIAN_POINT('Ctrl Pts',(-0.314358828238725,5.11801232161034,
41.3147264402218));
#54072=CARTESIAN_POINT('Ctrl Pts',(-2.72822377098922,4.34162027962559,41.4538998976437));
#54073=CARTESIAN_POINT('Ctrl Pts',(-4.47494238848132,2.50354992297337,41.5930733550657));
#54074=CARTESIAN_POINT('Ctrl Pts',(-4.91442322697852,0.853050173826952,
41.6868202438542));
#54075=CARTESIAN_POINT('Ctrl Pts',(-4.91867353960531,0.0170466588037495,
41.7341759801687));
#54076=CARTESIAN_POINT('Ctrl Pts',(-4.91866999096577,1.81579422333582E-5,
41.7351405640093));
#54077=CARTESIAN_POINT('Origin',(0.,0.,-3.23514056400933));
#54078=CARTESIAN_POINT('',(-4.91820219920178,0.000128750537505862,37.8898594359907));
#54079=CARTESIAN_POINT('',(-4.91850879678059,-9.71121811843556E-5,38.2351405640093));
#54080=CARTESIAN_POINT('',(-4.91825,1.47989506776076E-12,-3.23514056400933));
#54081=CARTESIAN_POINT('Ctrl Pts',(-4.91820219920178,0.000128750537505828,
37.8898594359907));
#54082=CARTESIAN_POINT('Ctrl Pts',(-4.91757825260023,-0.614945723327355,
37.9246909160581));
#54083=CARTESIAN_POINT('Ctrl Pts',(-4.64776325516924,-2.04975402890738,
38.0059135485996));
#54084=CARTESIAN_POINT('Ctrl Pts',(-3.28735082876793,-3.93525044354685,
38.1335273336149));
#54085=CARTESIAN_POINT('Ctrl Pts',(-0.999835326585605,-5.02923461816492,
38.2727007910369));
#54086=CARTESIAN_POINT('Ctrl Pts',(1.53217495314691,-4.89339467423037,38.4118742484588));
#54087=CARTESIAN_POINT('Ctrl Pts',(3.68951476027582,-3.56094823867799,38.5510477058808));
#54088=CARTESIAN_POINT('Ctrl Pts',(4.94463890588947,-1.35772516187962,38.6902211633027));
#54089=CARTESIAN_POINT('Ctrl Pts',(4.99062554934078,1.17750929979514,38.8293946207247));
#54090=CARTESIAN_POINT('Ctrl Pts',(3.81622934465927,3.42480147071306,38.9685680781466));
#54091=CARTESIAN_POINT('Ctrl Pts',(1.70863132174512,4.83460965654813,39.1077415355686));
#54092=CARTESIAN_POINT('Ctrl Pts',(-0.81678693997971,5.06218634776669,39.2469149929905));
#54093=CARTESIAN_POINT('Ctrl Pts',(-3.14247216978798,4.05188106771966,39.3860884504125));
#54094=CARTESIAN_POINT('Ctrl Pts',(-4.60805110144555,2.16853876589775,39.5170699314125));
#54095=CARTESIAN_POINT('Ctrl Pts',(-4.91770696078166,0.674350198934236,
39.6016602599387));
#54096=CARTESIAN_POINT('Ctrl Pts',(-4.9183905850055,-0.000118608231171394,
39.6398594359908));
#54097=CARTESIAN_POINT('Ctrl Pts',(-4.91850879678059,-9.71121811845985E-5,
38.2351405640093));
#54098=CARTESIAN_POINT('Ctrl Pts',(-4.91860204053572,-0.10467486996608,
38.2410638349858));
#54099=CARTESIAN_POINT('Ctrl Pts',(-4.8897482500804,-1.02825589750399,38.2933782584363));
#54100=CARTESIAN_POINT('Ctrl Pts',(-4.33490776837895,-2.73887682028504,
38.3920838343608));
#54101=CARTESIAN_POINT('Ctrl Pts',(-2.4925537144267,-4.48107660922512,38.5312572917828));
#54102=CARTESIAN_POINT('Ctrl Pts',(-0.0406829233315988,-5.12749612352813,
38.6704307492046));
#54103=CARTESIAN_POINT('Ctrl Pts',(2.42113626829065,-4.52006313754736,38.8096042066267));
#54104=CARTESIAN_POINT('Ctrl Pts',(4.29090279124404,-2.80731630443399,38.9487776640485));
#54105=CARTESIAN_POINT('Ctrl Pts',(5.11139320288289,-0.408082249760327,
39.0879511214706));
#54106=CARTESIAN_POINT('Ctrl Pts',(4.6819688426782,2.09094221661848,39.2271245788925));
#54107=CARTESIAN_POINT('Ctrl Pts',(3.10763901629375,4.0786580319335,39.3662980363144));
#54108=CARTESIAN_POINT('Ctrl Pts',(0.773382540198208,5.06899901790909,39.5054714937364));
#54109=CARTESIAN_POINT('Ctrl Pts',(-1.74999307091798,4.81979209601264,39.6446449511584));
#54110=CARTESIAN_POINT('Ctrl Pts',(-3.84543404598807,3.39197709234639,39.7838184085803));
#54111=CARTESIAN_POINT('Ctrl Pts',(-4.7874375644823,1.55112965427828,39.8973169461972));
#54112=CARTESIAN_POINT('Ctrl Pts',(-4.91795047422635,0.365935790564356,
39.9644243313403));
#54113=CARTESIAN_POINT('Ctrl Pts',(-4.9178455584335,4.04671957601049E-5,
39.9851405640093));
#54114=CARTESIAN_POINT('Origin',(0.,0.,-3.23514056400933));
#54115=CARTESIAN_POINT('',(-4.91802291969686,-0.000111909727839232,36.1398594359907));
#54116=CARTESIAN_POINT('',(-4.91808249072253,0.000120892635755293,36.4851405640093));
#54117=CARTESIAN_POINT('',(-4.91825,1.47989506776076E-12,-3.23514056400933));
#54118=CARTESIAN_POINT('Ctrl Pts',(-4.91802291969686,-0.000111909727839483,
36.1398594359907));
#54119=CARTESIAN_POINT('Ctrl Pts',(-4.91824438810614,-0.266428183199001,
36.1549392672297));
#54120=CARTESIAN_POINT('Ctrl Pts',(-4.83158217849615,-1.35188938642552,
36.2164102509426));
#54121=CARTESIAN_POINT('Ctrl Pts',(-4.04415220241896,-3.15241248704969,
36.3242723871296));
#54122=CARTESIAN_POINT('Ctrl Pts',(-2.0392020752804,-4.70473446870373,36.4634458445515));
#54123=CARTESIAN_POINT('Ctrl Pts',(0.464404425081292,-5.10658399077132,
36.6026193019735));
#54124=CARTESIAN_POINT('Ctrl Pts',(2.85444776800653,-4.25969476190013,36.7417927593954));
#54125=CARTESIAN_POINT('Ctrl Pts',(4.54647859476008,-2.3711608786047,36.8809662168174));
#54126=CARTESIAN_POINT('Ctrl Pts',(5.12673606933716,0.0972049391453199,
37.0201396742393));
#54127=CARTESIAN_POINT('Ctrl Pts',(4.45332690351699,2.5418007426328,37.1593131316613));
#54128=CARTESIAN_POINT('Ctrl Pts',(2.69092323862078,4.3648371846711,37.2984865890832));
#54129=CARTESIAN_POINT('Ctrl Pts',(0.270494535863632,5.12051796509932,37.4376600465052));
#54130=CARTESIAN_POINT('Ctrl Pts',(-2.21607956065588,4.62405264953592,37.576833503927));
#54131=CARTESIAN_POINT('Ctrl Pts',(-4.16074453993469,2.9968444067453,37.7160069613491));
#54132=CARTESIAN_POINT('Ctrl Pts',(-4.85590344258394,1.22745946040092,37.8203489387036));
#54133=CARTESIAN_POINT('Ctrl Pts',(-4.91840927103161,0.204256149366557,
37.8782997635842));
#54134=CARTESIAN_POINT('Ctrl Pts',(-4.91820219920178,0.000128750537505828,
37.8898594359907));
#54135=CARTESIAN_POINT('Ctrl Pts',(-4.91808249072253,0.000120892635755154,
36.4851405640093));
#54136=CARTESIAN_POINT('Ctrl Pts',(-4.91755648739828,-0.574931667043208,
36.5177033386313));
#54137=CARTESIAN_POINT('Ctrl Pts',(-4.67310068886124,-1.9696788349413,36.5966572657274));
#54138=CARTESIAN_POINT('Ctrl Pts',(-3.38252402474393,-3.85375178482954,
36.7220023452973));
#54139=CARTESIAN_POINT('Ctrl Pts',(-1.12242209698828,-5.0033029323877,36.8611758027193));
#54140=CARTESIAN_POINT('Ctrl Pts',(1.41215136985344,-4.92937116736687,37.0003492601412));
#54141=CARTESIAN_POINT('Ctrl Pts',(3.60140433654983,-3.6500353973252,37.1395227175632));
#54142=CARTESIAN_POINT('Ctrl Pts',(4.90998772824735,-1.47813805360231,37.2786961749851));
#54143=CARTESIAN_POINT('Ctrl Pts',(5.01790704510018,1.05521584700991,37.4178696324071));
#54144=CARTESIAN_POINT('Ctrl Pts',(3.89877223200052,3.33053249196408,37.5570430898291));
#54145=CARTESIAN_POINT('Ctrl Pts',(1.82625097191763,4.79141722088745,37.696216547251));
#54146=CARTESIAN_POINT('Ctrl Pts',(-0.692852653537991,5.08063251943419,
37.835390004673));
#54147=CARTESIAN_POINT('Ctrl Pts',(-3.04252952350951,4.12745511127861,37.9745634620949));
#54148=CARTESIAN_POINT('Ctrl Pts',(-4.57986334488089,2.24849431797034,38.1078136485404));
#54149=CARTESIAN_POINT('Ctrl Pts',(-4.91787175396287,0.714379791895642,
38.1946726825118));
#54150=CARTESIAN_POINT('Ctrl Pts',(-4.91850879678059,-9.71121811845985E-5,
38.2351405640093));
#54151=CARTESIAN_POINT('Origin',(0.,0.,-3.23514056400933));
#54152=CARTESIAN_POINT('',(-4.91856546994177,8.07004106879134E-5,34.3898594359908));
#54153=CARTESIAN_POINT('',(-4.91813464082657,-0.000125816539483792,34.7351405640093));
#54154=CARTESIAN_POINT('',(-4.91825,1.47989506776076E-12,-3.23514056400933));
#54155=CARTESIAN_POINT('Ctrl Pts',(-4.91856546994177,8.07004106878097E-5,
34.3898594359908));
#54156=CARTESIAN_POINT('Ctrl Pts',(-4.91799365147455,-0.736466546762098,
34.4315787708752));
#54157=CARTESIAN_POINT('Ctrl Pts',(-4.56381414385588,-2.29257248088249,
34.5196892582337));
#54158=CARTESIAN_POINT('Ctrl Pts',(-2.98661825458746,-4.16809104101649,
34.6541908980661));
#54159=CARTESIAN_POINT('Ctrl Pts',(-0.624306769841251,-5.08951005323373,
34.7933643554881));
#54160=CARTESIAN_POINT('Ctrl Pts',(1.89066959956818,-4.76636549061291,34.93253781291));
#54161=CARTESIAN_POINT('Ctrl Pts',(3.94331099153097,-3.27767752362979,35.071711270332));
#54162=CARTESIAN_POINT('Ctrl Pts',(5.03167464890124,-0.987482532727304,
35.2108847277539));
#54163=CARTESIAN_POINT('Ctrl Pts',(4.88961751469062,1.54418654471136,35.3500581851759));
#54164=CARTESIAN_POINT('Ctrl Pts',(3.55187753674385,3.69824789445101,35.4892316425978));
#54165=CARTESIAN_POINT('Ctrl Pts',(1.34557902206557,4.94795802530842,35.6284051000198));
#54166=CARTESIAN_POINT('Ctrl Pts',(-1.18976072063133,4.98771901298376,35.7675785574417));
#54167=CARTESIAN_POINT('Ctrl Pts',(-3.43416227081397,3.807807902528,35.9067520148637));
#54168=CARTESIAN_POINT('Ctrl Pts',(-4.68659538479648,1.92549284030058,36.0308456410467));
#54169=CARTESIAN_POINT('Ctrl Pts',(-4.91756306915899,0.552859423746898,
36.1085481147557));
#54170=CARTESIAN_POINT('Ctrl Pts',(-4.91802291969686,-0.000111909727839483,
36.1398594359907));
#54171=CARTESIAN_POINT('Ctrl Pts',(-4.91813464082657,-0.000125816539484104,
34.7351405640093));
#54172=CARTESIAN_POINT('Ctrl Pts',(-4.91835367199364,-0.226361035175407,
34.7479516898028));
#54173=CARTESIAN_POINT('Ctrl Pts',(-4.84753997352677,-1.27169443624834,
34.8071539680704));
#54174=CARTESIAN_POINT('Ctrl Pts',(-4.11997143710345,-3.05265572158056,
34.912747398812));
#54175=CARTESIAN_POINT('Ctrl Pts',(-2.15354963574969,-4.65350357939147,
35.0519208562339));
#54176=CARTESIAN_POINT('Ctrl Pts',(0.339490524783248,-5.11640672548902,
35.1910943136559));
#54177=CARTESIAN_POINT('Ctrl Pts',(2.74951335423154,-4.32816911776206,35.3302677710778));
#54178=CARTESIAN_POINT('Ctrl Pts',(4.48718380920458,-2.4815424758523,35.4694412284998));
#54179=CARTESIAN_POINT('Ctrl Pts',(5.12758056511281,-0.0280917305306554,
35.6086146859217));
#54180=CARTESIAN_POINT('Ctrl Pts',(4.51410417181047,2.43222842740771,35.7477881433437));
#54181=CARTESIAN_POINT('Ctrl Pts',(2.79677110733593,4.29778349503762,35.8869616007656));
#54182=CARTESIAN_POINT('Ctrl Pts',(0.395529491558261,5.1123798781345,36.0261350581876));
#54183=CARTESIAN_POINT('Ctrl Pts',(-2.10243294662056,4.67682021270983,36.1653085156095));
#54184=CARTESIAN_POINT('Ctrl Pts',(-4.08627684754628,3.09761410157141,36.3044819730315));
#54185=CARTESIAN_POINT('Ctrl Pts',(-4.84051203245055,1.30765216918706,36.4110926558314));
#54186=CARTESIAN_POINT('Ctrl Pts',(-4.91830586765535,0.24432748044256,36.4713121861573));
#54187=CARTESIAN_POINT('Ctrl Pts',(-4.91808249072253,0.000120892635755154,
36.4851405640093));
#54188=CARTESIAN_POINT('Origin',(0.,0.,-3.23514056400933));
#54189=CARTESIAN_POINT('',(-4.91783086310991,-2.02920551994784E-5,32.6398594359908));
#54190=CARTESIAN_POINT('',(-4.91845769753215,0.000108139753099631,32.9851405640093));
#54191=CARTESIAN_POINT('',(-4.91825,1.47989506776076E-12,-3.23514056400933));
#54192=CARTESIAN_POINT('Ctrl Pts',(-4.91783086310991,-2.02920551998012E-5,
32.6398594359908));
#54193=CARTESIAN_POINT('Ctrl Pts',(-4.91788645067138,-0.388022414657125,
32.6618271220468));
#54194=CARTESIAN_POINT('Ctrl Pts',(-4.77675395009793,-1.59536399838191,
32.7301859605768));
#54195=CARTESIAN_POINT('Ctrl Pts',(-3.79936349942357,-3.44350236301427,
32.8449359515807));
#54196=CARTESIAN_POINT('Ctrl Pts',(-1.68486707003129,-4.84294275014284,
32.9841094090027));
#54197=CARTESIAN_POINT('Ctrl Pts',(0.841638405786343,-5.05811390922963,
33.1232828664246));
#54198=CARTESIAN_POINT('Ctrl Pts',(3.16233379535394,-4.03639895099572,33.2624563238466));
#54199=CARTESIAN_POINT('Ctrl Pts',(4.70972774489857,-2.02764298972218,33.4016297812685));
#54200=CARTESIAN_POINT('Ctrl Pts',(5.10542820383288,0.476942743256107,33.5408032386905));
#54201=CARTESIAN_POINT('Ctrl Pts',(4.25267254224057,2.86489926058667,33.6799766961124));
#54202=CARTESIAN_POINT('Ctrl Pts',(2.35998940503126,4.55228750552699,33.8191501535344));
#54203=CARTESIAN_POINT('Ctrl Pts',(-0.109793849828778,5.12648191602942,
33.9583236109563));
#54204=CARTESIAN_POINT('Ctrl Pts',(-2.55272866057358,4.44707183552539,34.0974970683783));
#54205=CARTESIAN_POINT('Ctrl Pts',(-4.37143185095318,2.68019683928419,34.2366705258002));
#54206=CARTESIAN_POINT('Ctrl Pts',(-4.89642245145228,0.984033726224288,
34.3341246483377));
#54207=CARTESIAN_POINT('Ctrl Pts',(-4.9186295033589,0.0825607877462077,
34.3851876184012));
#54208=CARTESIAN_POINT('Ctrl Pts',(-4.91856546994177,8.07004106878097E-5,
34.3898594359908));
#54209=CARTESIAN_POINT('Ctrl Pts',(-4.91845769753216,0.000108139753099545,
32.9851405640093));
#54210=CARTESIAN_POINT('Ctrl Pts',(-4.9177893045039,-0.696429685266491,
33.0245911934484));
#54211=CARTESIAN_POINT('Ctrl Pts',(-4.5926463194941,-2.21265079041603,33.1104329753614));
#54212=CARTESIAN_POINT('Ctrl Pts',(-3.0875705083242,-4.0938710230262,33.2426659097486));
#54213=CARTESIAN_POINT('Ctrl Pts',(-0.748478438807404,-5.07273610822475,
33.3818393671704));
#54214=CARTESIAN_POINT('Ctrl Pts',(1.77364284015155,-4.81113943599913,33.5210128245925));
#54215=CARTESIAN_POINT('Ctrl Pts',(3.86204628565767,-3.37305056061788,33.6601862820144));
#54216=CARTESIAN_POINT('Ctrl Pts',(5.00604406515782,-1.11013261133297,33.7993597394364));
#54217=CARTESIAN_POINT('Ctrl Pts',(4.92588862905106,1.42425166709831,33.9385331968583));
#54218=CARTESIAN_POINT('Ctrl Pts',(3.64118079059058,3.61035649864124,34.0777066542803));
#54219=CARTESIAN_POINT('Ctrl Pts',(1.4660766401138,4.91360263781672,34.2168801117022));
#54220=CARTESIAN_POINT('Ctrl Pts',(-1.06753462895041,5.01530073006979,34.3560535691242));
#54221=CARTESIAN_POINT('Ctrl Pts',(-3.34009626844846,3.89058202773615,34.4952270265461));
#54222=CARTESIAN_POINT('Ctrl Pts',(-4.66187956111484,2.00558801068489,34.6215893581745));
#54223=CARTESIAN_POINT('Ctrl Pts',(-4.9175605248158,0.592873175137666,34.7015605373289));
#54224=CARTESIAN_POINT('Ctrl Pts',(-4.91813464082657,-0.000125816539484104,
34.7351405640093));
#54225=CARTESIAN_POINT('Origin',(0.,0.,-3.23514056400933));
#54226=CARTESIAN_POINT('',(-4.91864785516252,-4.10080702071888E-5,30.8898594359907));
#54227=CARTESIAN_POINT('',(-4.91786460607134,-5.61405901616796E-5,31.2351405640093));
#54228=CARTESIAN_POINT('',(-4.91825,1.47989506776076E-12,-3.23514056400933));
#54229=CARTESIAN_POINT('Ctrl Pts',(-4.91864785516252,-4.10080702073533E-5,
30.8898594359907));
#54230=CARTESIAN_POINT('Ctrl Pts',(-4.9186650757863,-0.0391628390810305,
30.8920754732183));
#54231=CARTESIAN_POINT('Ctrl Pts',(-4.90864151106169,-0.897263340327606,
30.9406826629198));
#54232=CARTESIAN_POINT('Ctrl Pts',(-4.44078995181737,-2.56364118563321,
31.0356810050954));
#54233=CARTESIAN_POINT('Ctrl Pts',(-2.66945427843709,-4.37800015762571,
31.1748544625173));
#54234=CARTESIAN_POINT('Ctrl Pts',(-0.245343480361355,-5.12178465981157,
31.3140279199393));
#54235=CARTESIAN_POINT('Ctrl Pts',(2.23876239696327,-4.61311331475612,31.4532013773612));
#54236=CARTESIAN_POINT('Ctrl Pts',(4.17541240862802,-2.97637409320671,31.5923748347831));
#54237=CARTESIAN_POINT('Ctrl Pts',(5.09102775500046,-0.611807095947689,
31.7315482922051));
#54238=CARTESIAN_POINT('Ctrl Pts',(4.7617083952635,1.90236817764437,31.8707217496271));
#54239=CARTESIAN_POINT('Ctrl Pts',(3.26798445418964,3.95134776146213,32.009895207049));
#54240=CARTESIAN_POINT('Ctrl Pts',(0.975123784377534,5.03408433878279,32.149068664471));
#54241=CARTESIAN_POINT('Ctrl Pts',(-1.5561888248749,4.8858108708966,32.2882421218929));
#54242=CARTESIAN_POINT('Ctrl Pts',(-3.70695872829678,3.5427854170894,32.4274155793149));
#54243=CARTESIAN_POINT('Ctrl Pts',(-4.75484390387066,1.6821589453014,32.5446213506808));
#54244=CARTESIAN_POINT('Ctrl Pts',(-4.91776906138271,0.431356812812067,
32.6154359695728));
#54245=CARTESIAN_POINT('Ctrl Pts',(-4.91783086310991,-2.02920551998012E-5,
32.6398594359908));
#54246=CARTESIAN_POINT('Ctrl Pts',(-4.91786460607134,-5.61405901617837E-5,
31.2351405640093));
#54247=CARTESIAN_POINT('Ctrl Pts',(-4.91800366546841,-0.347980646584003,
31.2548395446199));
#54248=CARTESIAN_POINT('Ctrl Pts',(-4.79588397241455,-1.51517210046812,
31.3209296777045));
#54249=CARTESIAN_POINT('Ctrl Pts',(-3.882368363373,-3.34963990424751,31.4334109632632));
#54250=CARTESIAN_POINT('Ctrl Pts',(-1.80269742761279,-4.80032848683557,
31.5725844206851));
#54251=CARTESIAN_POINT('Ctrl Pts',(0.717796206480772,-5.07716852221872,
31.7117578781071));
#54252=CARTESIAN_POINT('Ctrl Pts',(3.06276351222464,-4.1124629196179,31.850931335529));
#54253=CARTESIAN_POINT('Ctrl Pts',(4.65877780170794,-2.14211600791371,31.990104792951));
#54254=CARTESIAN_POINT('Ctrl Pts',(5.11555764728126,0.352053340261175,32.1292782503729));
#54255=CARTESIAN_POINT('Ctrl Pts',(4.32140436840864,2.760133308691,32.2684517077949));
#54256=CARTESIAN_POINT('Ctrl Pts',(2.47051627364734,4.49326395159359,32.4076251652168));
#54257=CARTESIAN_POINT('Ctrl Pts',(0.0155003683372346,5.12763408753279,
32.5467986226388));
#54258=CARTESIAN_POINT('Ctrl Pts',(-2.44330592025679,4.50811798615397,32.6859720800608));
#54259=CARTESIAN_POINT('Ctrl Pts',(-4.30463828331925,2.78620904578768,32.8251455374827));
#54260=CARTESIAN_POINT('Ctrl Pts',(-4.88409932027737,1.06420425567212,32.9248683654655));
#54261=CARTESIAN_POINT('Ctrl Pts',(-4.91857528747368,0.122649576681999,
32.9782000409744));
#54262=CARTESIAN_POINT('Ctrl Pts',(-4.91845769753216,0.000108139753099545,
32.9851405640093));
#54263=CARTESIAN_POINT('Origin',(0.,0.,-3.23514056400933));
#54264=CARTESIAN_POINT('',(-4.91792510490206,8.60427107810521E-5,29.1398594359908));
#54265=CARTESIAN_POINT('',(-4.91867551204664,9.95602900351817E-7,29.4851405640093));
#54266=CARTESIAN_POINT('',(-4.91825,1.47989506776076E-12,-3.23514056400933));
#54267=CARTESIAN_POINT('Ctrl Pts',(-4.91792510490206,8.60427107807205E-5,
29.1398594359908));
#54268=CARTESIAN_POINT('Ctrl Pts',(-4.91760801436112,-0.509544199604375,
29.1687149768638));
#54269=CARTESIAN_POINT('Ctrl Pts',(-4.71209097325018,-1.83875860727307,
29.2439616702109));
#54270=CARTESIAN_POINT('Ctrl Pts',(-3.5336719345399,-3.71564720928695,29.3655995160319));
#54271=CARTESIAN_POINT('Ctrl Pts',(-1.3212624743179,-4.95450673617428,29.5047729734539));
#54272=CARTESIAN_POINT('Ctrl Pts',(1.21424196580137,-4.98181573056689,29.6439464308758));
#54273=CARTESIAN_POINT('Ctrl Pts',(3.45282169099331,-3.79089618626559,29.7831198882978));
#54274=CARTESIAN_POINT('Ctrl Pts',(4.84706550524806,-1.67296966878402,29.9222933457197));
#54275=CARTESIAN_POINT('Ctrl Pts',(5.05603193335185,0.854056563561975,30.0614668031417));
#54276=CARTESIAN_POINT('Ctrl Pts',(4.02862136020189,3.17223603487539,30.2006402605636));
#54277=CARTESIAN_POINT('Ctrl Pts',(2.01607167753466,4.71469262156925,30.3398137179856));
#54278=CARTESIAN_POINT('Ctrl Pts',(-0.48947818547963,5.10424163130788,30.4789871754075));
#54279=CARTESIAN_POINT('Ctrl Pts',(-2.87533347790578,4.24562467908683,30.6181606328295));
#54280=CARTESIAN_POINT('Ctrl Pts',(-4.53127503174689,2.37900648499639,30.7551180530239));
#54281=CARTESIAN_POINT('Ctrl Pts',(-4.91830457435893,0.779824678331975,
30.8456843207443));
#54282=CARTESIAN_POINT('Ctrl Pts',(-4.91864785516252,-4.10080702073533E-5,
30.8898594359907));
#54283=CARTESIAN_POINT('Ctrl Pts',(-4.91867550406428,9.95584223391723E-7,
29.4851405640093));
#54284=CARTESIAN_POINT('Ctrl Pts',(-4.91866563344334,-0.818043332890193,
29.5314790482654));
#54285=CARTESIAN_POINT('Ctrl Pts',(-4.50145125695214,-2.45507147256078,
29.6242086849956));
#54286=CARTESIAN_POINT('Ctrl Pts',(-2.77563018347832,-4.31146711475466,
29.7633294741997));
#54287=CARTESIAN_POINT('Ctrl Pts',(-0.370416895766376,-5.11426074035902,
29.9025029316217));
#54288=CARTESIAN_POINT('Ctrl Pts',(2.1253763045803,-4.66643838071129,30.0416763890436));
#54289=CARTESIAN_POINT('Ctrl Pts',(4.10144051258044,-3.07750829711484,30.1808498464656));
#54290=CARTESIAN_POINT('Ctrl Pts',(5.07455877628885,-0.736019580606846,
30.3200233038876));
#54291=CARTESIAN_POINT('Ctrl Pts',(4.8067695763542,1.7854517178805,30.4591967613095));
#54292=CARTESIAN_POINT('Ctrl Pts',(3.36355675709311,3.87031749845671,30.5983702187315));
#54293=CARTESIAN_POINT('Ctrl Pts',(1.09783643160968,5.00875501162488,30.7375436761534));
#54294=CARTESIAN_POINT('Ctrl Pts',(-1.43634337614621,4.92237638776717,30.8767171335754));
#54295=CARTESIAN_POINT('Ctrl Pts',(-3.61928689038582,3.63230422763955,31.0158905909973));
#54296=CARTESIAN_POINT('Ctrl Pts',(-4.7334795615999,1.76232844516563,31.1353650678086));
#54297=CARTESIAN_POINT('Ctrl Pts',(-4.9176761802132,0.47138250352112,31.208448392146));
#54298=CARTESIAN_POINT('Ctrl Pts',(-4.91786460607134,-5.61405901617837E-5,
31.2351405640093));
#54299=CARTESIAN_POINT('Origin',(0.,0.,-3.23514056400933));
#54300=CARTESIAN_POINT('',(-4.91833988482916,-0.000123980294687707,27.3898594359908));
#54301=CARTESIAN_POINT('',(-4.91786234455194,5.45566455475988E-5,27.7351405640093));
#54302=CARTESIAN_POINT('',(-4.91825,1.47989506776076E-12,-3.23514056400933));
#54303=CARTESIAN_POINT('Ctrl Pts',(-4.91833988482916,-0.000123980294688027,
27.3898594359908));
#54304=CARTESIAN_POINT('Ctrl Pts',(-4.91850603363977,-0.160872832603585,
27.3989633280354));
#54305=CARTESIAN_POINT('Ctrl Pts',(-4.87141522988022,-1.14066063085594,
27.454458372554));
#54306=CARTESIAN_POINT('Ctrl Pts',(-4.23855121493717,-2.88575035704607,
27.5563445695465));
#54307=CARTESIAN_POINT('Ctrl Pts',(-2.33760383332739,-4.56382294170687,
27.6955180269685));
#54308=CARTESIAN_POINT('Ctrl Pts',(0.134969609127406,-5.12588087351325,
27.8346914843905));
#54309=CARTESIAN_POINT('Ctrl Pts',(2.57453825200954,-4.43448129027247,27.9738649418124));
#54310=CARTESIAN_POINT('Ctrl Pts',(4.38454206508205,-2.65869562085676,28.1130383992344));
#54311=CARTESIAN_POINT('Ctrl Pts',(5.12237168270734,-0.232765695571575,
28.2522118566563));
#54312=CARTESIAN_POINT('Ctrl Pts',(4.60760190542052,2.25008359978071,28.3913853140782));
#54313=CARTESIAN_POINT('Ctrl Pts',(2.96611198437499,4.18270859862171,28.5305587715002));
#54314=CARTESIAN_POINT('Ctrl Pts',(0.59930373287477,5.09251475801487,28.6697322289221));
#54315=CARTESIAN_POINT('Ctrl Pts',(-1.91405528449465,4.75702258694817,28.8089056863441));
#54316=CARTESIAN_POINT('Ctrl Pts',(-3.95936070487888,3.25827167889634,28.948079143766));
#54317=CARTESIAN_POINT('Ctrl Pts',(-4.81314243584705,1.43869944420298,29.058397060315));
#54318=CARTESIAN_POINT('Ctrl Pts',(-4.91811780191622,0.309790096730312,
29.1223238243899));
#54319=CARTESIAN_POINT('Ctrl Pts',(-4.91792510490206,8.60427107807205E-5,
29.1398594359908));
#54320=CARTESIAN_POINT('Ctrl Pts',(-4.91786234455194,5.455664554746E-5,
27.7351405640093));
#54321=CARTESIAN_POINT('Ctrl Pts',(-4.91768006061354,-0.469524247219173,
27.761727399437));
#54322=CARTESIAN_POINT('Ctrl Pts',(-4.73449557411608,-1.75860652475638,
27.8347053873387));
#54323=CARTESIAN_POINT('Ctrl Pts',(-3.62340576199759,-3.62819545793354,
27.9540745277144));
#54324=CARTESIAN_POINT('Ctrl Pts',(-1.44192736471906,-4.92074354868461,
28.0932479851363));
#54325=CARTESIAN_POINT('Ctrl Pts',(1.09215280697808,-5.0099973895459,28.2324214425583));
#54326=CARTESIAN_POINT('Ctrl Pts',(3.35916334181333,-3.8741312884393,28.3715948999802));
#54327=CARTESIAN_POINT('Ctrl Pts',(4.80474071443369,-1.79090431461596,28.5107683574022));
#54328=CARTESIAN_POINT('Ctrl Pts',(5.0753905955706,0.730261528111896,28.6499418148241));
#54329=CARTESIAN_POINT('Ctrl Pts',(4.10492960409817,3.07285283449196,28.7891152722461));
#54330=CARTESIAN_POINT('Ctrl Pts',(2.1306694631793,4.66402393172698,28.928288729668));
#54331=CARTESIAN_POINT('Ctrl Pts',(-0.36461403286742,5.11467772240667,29.06746218709));
#54332=CARTESIAN_POINT('Ctrl Pts',(-2.77073661962518,4.31461356111005,29.2066356445119));
#54333=CARTESIAN_POINT('Ctrl Pts',(-4.49931699972899,2.45947517429971,29.3458091019339));
#54334=CARTESIAN_POINT('Ctrl Pts',(-4.9184479131161,0.820834680615058,29.4386440750997));
#54335=CARTESIAN_POINT('Ctrl Pts',(-4.91867551528321,0.000930782942780498,
29.4850878957915));
#54336=CARTESIAN_POINT('Ctrl Pts',(-4.91867550406428,9.95584223391723E-7,
29.4851405640093));
#54337=CARTESIAN_POINT('Origin',(0.,0.,-3.23514056400933));
#54338=CARTESIAN_POINT('',(-4.91825297823531,0.000128629553767107,25.6398594359908));
#54339=CARTESIAN_POINT('',(-4.91846315696893,-0.00010709994074265,25.9851405640093));
#54340=CARTESIAN_POINT('',(-4.91825,1.47989506776076E-12,-3.23514056400933));
#54341=CARTESIAN_POINT('Ctrl Pts',(-4.91825297823531,0.000128629553767055,
25.6398594359908));
#54342=CARTESIAN_POINT('Ctrl Pts',(-4.91760082664806,-0.631030237377122,
25.6756028316809));
#54343=CARTESIAN_POINT('Ctrl Pts',(-4.63725911016808,-2.08192918048296,
25.757737379845));
#54344=CARTESIAN_POINT('Ctrl Pts',(-3.24853925631766,-3.96734977346339,
25.8862630804831));
#54345=CARTESIAN_POINT('Ctrl Pts',(-0.950388722330458,-5.03881263804321,
26.0254365379051));
#54346=CARTESIAN_POINT('Ctrl Pts',(1.58016516156227,-4.87810922253918,26.164609995327));
#54347=CARTESIAN_POINT('Ctrl Pts',(3.72431328503039,-3.52453714404928,26.303783452749));
#54348=CARTESIAN_POINT('Ctrl Pts',(4.95773628813266,-1.30909221301232,26.4429569101709));
#54349=CARTESIAN_POINT('Ctrl Pts',(4.97881902010364,1.22647164251408,26.5821303675929));
#54350=CARTESIAN_POINT('Ctrl Pts',(3.78240601411158,3.462120198556,26.7213038250149));
#54351=CARTESIAN_POINT('Ctrl Pts',(1.66106217957725,4.85115903268642,26.8604772824368));
#54352=CARTESIAN_POINT('Ctrl Pts',(-0.866469571400946,5.05391946974555,
26.9996507398587));
#54353=CARTESIAN_POINT('Ctrl Pts',(-3.182119145904,4.02081947693602,27.1388241972807));
#54354=CARTESIAN_POINT('Ctrl Pts',(-4.61905440019765,2.13638449485411,27.268893762658));
#54355=CARTESIAN_POINT('Ctrl Pts',(-4.9176593809369,0.658263035982611,27.3525721755614));
#54356=CARTESIAN_POINT('Ctrl Pts',(-4.91833988482916,-0.000123980294688027,
27.3898594359908));
#54357=CARTESIAN_POINT('Ctrl Pts',(-4.91846315696893,-0.000107099940742945,
25.9851405640093));
#54358=CARTESIAN_POINT('Ctrl Pts',(-4.91857823666502,-0.120788336375971,
25.9919757506085));
#54359=CARTESIAN_POINT('Ctrl Pts',(-4.88469360351122,-1.06048172000503,
26.0452020896818));
#54360=CARTESIAN_POINT('Ctrl Pts',(-4.30779673681465,-2.7813232230965,26.144819581229));
#54361=CARTESIAN_POINT('Ctrl Pts',(-2.44841924438686,-4.50534291711108,
26.2839930386509));
#54362=CARTESIAN_POINT('Ctrl Pts',(0.00968256052368256,-5.12764837377413,
26.4231664960729));
#54363=CARTESIAN_POINT('Ctrl Pts',(2.46541664005145,-4.49606409963251,26.5623399534948));
#54364=CARTESIAN_POINT('Ctrl Pts',(4.31826994816623,-2.76503458419805,26.7015134109168));
#54365=CARTESIAN_POINT('Ctrl Pts',(5.11515491599038,-0.357857209604937,
26.8406868683387));
#54366=CARTESIAN_POINT('Ctrl Pts',(4.66120524128334,2.13682879419003,26.9798603257607));
#54367=CARTESIAN_POINT('Ctrl Pts',(3.06742752861815,4.10898527056527,27.1190337831826));
#54368=CARTESIAN_POINT('Ctrl Pts',(0.723556284229189,5.07635084490811,27.2582072406046));
#54369=CARTESIAN_POINT('Ctrl Pts',(-1.79724982938647,4.80237073202571,27.3973806980266));
#54370=CARTESIAN_POINT('Ctrl Pts',(-3.87856537335147,3.35404267141695,27.5365541554485));
#54371=CARTESIAN_POINT('Ctrl Pts',(-4.79501921332612,1.51889555036017,27.6491407774428));
#54372=CARTESIAN_POINT('Ctrl Pts',(-4.91799812637216,0.349839980910759,
27.715336246963));
#54373=CARTESIAN_POINT('Ctrl Pts',(-4.91786234455194,5.455664554746E-5,
27.7351405640093));
#54374=CARTESIAN_POINT('Origin',(0.,0.,-3.23514056400933));
#54375=CARTESIAN_POINT('',(-4.91798336942312,-0.000103487961194405,23.8898594359907));
#54376=CARTESIAN_POINT('',(-4.91812910911164,0.000125410111702917,24.2351405640093));
#54377=CARTESIAN_POINT('',(-4.91825,1.47989506776076E-12,-3.23514056400933));
#54378=CARTESIAN_POINT('Ctrl Pts',(-4.91798336942312,-0.000103487961194554,
23.8898594359907));
#54379=CARTESIAN_POINT('Ctrl Pts',(-4.91819811111129,-0.282531091654608,
23.9058511828524));
#54380=CARTESIAN_POINT('Ctrl Pts',(-4.82487700658905,-1.38412483582262,
23.9682340821881));
#54381=CARTESIAN_POINT('Ctrl Pts',(-4.01299334824328,-3.19198306884484,
24.0770081339978));
#54382=CARTESIAN_POINT('Ctrl Pts',(-1.99289265244315,-4.72453705675752,
24.2161815914197));
#54383=CARTESIAN_POINT('Ctrl Pts',(0.514540139737736,-5.10177615830366,
24.3553550488417));
#54384=CARTESIAN_POINT('Ctrl Pts',(2.89614983519387,-4.23145219244452,24.4945285062636));
#54385=CARTESIAN_POINT('Ctrl Pts',(4.56954939756152,-2.32638987018126,24.6337019636856));
#54386=CARTESIAN_POINT('Ctrl Pts',(5.12553398792908,0.147556305933546,24.7728754211075));
#54387=CARTESIAN_POINT('Ctrl Pts',(4.42814588893175,2.58541979399356,24.9120488785295));
#54388=CARTESIAN_POINT('Ctrl Pts',(2.64792093141759,4.39105753387467,25.0512223359514));
#54389=CARTESIAN_POINT('Ctrl Pts',(0.220186507211287,5.12292781784782,25.1903957933734));
#54390=CARTESIAN_POINT('Ctrl Pts',(-2.26139123465815,4.60206271237672,25.3295692507953));
#54391=CARTESIAN_POINT('Ctrl Pts',(-4.18997956700173,2.95583198997252,25.4687427082172));
#54392=CARTESIAN_POINT('Ctrl Pts',(-4.86180231945706,1.19522716609489,25.5721727699491));
#54393=CARTESIAN_POINT('Ctrl Pts',(-4.91844725052962,0.188147310411823,
25.6292116792069));
#54394=CARTESIAN_POINT('Ctrl Pts',(-4.91825297823531,0.000128629553767055,
25.6398594359908));
#54395=CARTESIAN_POINT('Ctrl Pts',(-4.91812910911164,0.000125410111702882,
24.2351405640093));
#54396=CARTESIAN_POINT('Ctrl Pts',(-4.91755969077297,-0.591015325586734,
24.2686152542541));
#54397=CARTESIAN_POINT('Ctrl Pts',(-4.66305203111981,-2.00186995761876,
24.3484810969728));
#54398=CARTESIAN_POINT('Ctrl Pts',(-3.34450836095903,-3.8867898606076,24.4747380921655));
#54399=CARTESIAN_POINT('Ctrl Pts',(-1.07322428658152,-5.01408628044417,
24.6139115495875));
#54400=CARTESIAN_POINT('Ctrl Pts',(1.46050073805254,-4.91526288118904,24.7530850070094));
#54401=CARTESIAN_POINT('Ctrl Pts',(3.63708214756602,-3.61448544732211,24.8922584644314));
#54402=CARTESIAN_POINT('Ctrl Pts',(4.92426950692363,-1.42983964843226,25.0314319218533));
#54403=CARTESIAN_POINT('Ctrl Pts',(5.0073003960314,1.10445205461833,25.1706053792753));
#54404=CARTESIAN_POINT('Ctrl Pts',(3.86587085260431,3.36866652371991,25.3097788366973));
#54405=CARTESIAN_POINT('Ctrl Pts',(1.77910040251715,4.80912396958221,25.4489522941192));
#54406=CARTESIAN_POINT('Ctrl Pts',(-0.742722446286816,5.07358206446181,
25.5881257515412));
#54407=CARTESIAN_POINT('Ctrl Pts',(-3.08292362754424,4.0973715359699,25.7272992089631));
#54408=CARTESIAN_POINT('Ctrl Pts',(-4.59133353590126,2.2163629543867,25.8596374797858));
#54409=CARTESIAN_POINT('Ctrl Pts',(-4.9177971782915,0.698288298756671,25.9455845981345));
#54410=CARTESIAN_POINT('Ctrl Pts',(-4.91846315696893,-0.000107099940742945,
25.9851405640093));
#54411=CARTESIAN_POINT('Origin',(0.,0.,-3.23514056400933));
#54412=CARTESIAN_POINT('',(-4.91860118447858,6.69814320594633E-5,22.1398594359908));
#54413=CARTESIAN_POINT('',(-4.91808775011422,-0.000121504406732365,22.4851405640093));
#54414=CARTESIAN_POINT('',(-4.91825,1.47989506776076E-12,-3.23514056400933));
#54415=CARTESIAN_POINT('Ctrl Pts',(-4.91860118447858,6.69814320593525E-5,
22.1398594359908));
#54416=CARTESIAN_POINT('Ctrl Pts',(-4.91809758575849,-0.752564123265761,
22.182490686498));
#54417=CARTESIAN_POINT('Ctrl Pts',(-4.55189348730661,-2.32467849421272,
22.2715130894791));
#54418=CARTESIAN_POINT('Ctrl Pts',(-2.94553417198737,-4.19722526992435,
22.4069266449343));
#54419=CARTESIAN_POINT('Ctrl Pts',(-0.57428624079235,-5.09539663210565,
22.5461001023563));
#54420=CARTESIAN_POINT('Ctrl Pts',(1.93739480269542,-4.74756494461378,22.6852735597782));
#54421=CARTESIAN_POINT('Ctrl Pts',(3.97531491904182,-3.23878724513983,22.8244470172002));
#54422=CARTESIAN_POINT('Ctrl Pts',(5.04113121891057,-0.938012557784862,
22.9636204746221));
#54423=CARTESIAN_POINT('Ctrl Pts',(4.87421426441648,1.59213907350953,23.1027939320441));
#54424=CARTESIAN_POINT('Ctrl Pts',(3.51538110070013,3.73295690327082,23.241967389466));
#54425=CARTESIAN_POINT('Ctrl Pts',(1.29691405791799,4.9609359450825,23.381140846888));
#54426=CARTESIAN_POINT('Ctrl Pts',(-1.23869392363774,4.97579228750355,23.52031430431));
#54427=CARTESIAN_POINT('Ctrl Pts',(-3.47139782963254,3.77389303415709,23.6594877617318));
#54428=CARTESIAN_POINT('Ctrl Pts',(-4.69621463502052,1.89328920109618,23.7826694722922));
#54429=CARTESIAN_POINT('Ctrl Pts',(-4.91757515762881,0.536775400570982,
23.8594600303784));
#54430=CARTESIAN_POINT('Ctrl Pts',(-4.91798336942312,-0.000103487961194554,
23.8898594359907));
#54431=CARTESIAN_POINT('Ctrl Pts',(-4.91808775011422,-0.000121504406732746,
22.4851405640093));
#54432=CARTESIAN_POINT('Ctrl Pts',(-4.91831091521774,-0.242467126595803,
22.4988636054256));
#54433=CARTESIAN_POINT('Ctrl Pts',(-4.84124936173334,-1.30392870955655,
22.5589777993159));
#54434=CARTESIAN_POINT('Ctrl Pts',(-4.089788760808,-3.09297583065489,22.6654831456802));
#54435=CARTESIAN_POINT('Ctrl Pts',(-2.10773789918185,-4.67443178850642,
22.8046566031021));
#54436=CARTESIAN_POINT('Ctrl Pts',(0.389728746515864,-5.11282535406657,
22.9438300605241));
#54437=CARTESIAN_POINT('Ctrl Pts',(2.79189305526804,-4.30095393662765,23.083003517946));
#54438=CARTESIAN_POINT('Ctrl Pts',(4.51134166740374,-2.43734855057574,23.222176975368));
#54439=CARTESIAN_POINT('Ctrl Pts',(5.12760913750936,0.0222739753389076,
23.3613504327899));
#54440=CARTESIAN_POINT('Ctrl Pts',(4.48999647145208,2.47644973367009,23.5005238902119));
#54441=CARTESIAN_POINT('Ctrl Pts',(2.75442231183803,4.32504674253304,23.6396973476338));
#54442=CARTESIAN_POINT('Ctrl Pts',(0.345295365574717,5.11601824738336,23.7788708050558));
#54443=CARTESIAN_POINT('Ctrl Pts',(-2.14826839878302,4.65594399492059,23.9180442624777));
#54444=CARTESIAN_POINT('Ctrl Pts',(-4.11650525148601,3.05732826362086,24.0572177198997));
#54445=CARTESIAN_POINT('Ctrl Pts',(-4.8468218058486,1.27541781951381,24.1629164870769));
#54446=CARTESIAN_POINT('Ctrl Pts',(-4.91834882348122,0.228221530761836,
24.2222241017801));
#54447=CARTESIAN_POINT('Ctrl Pts',(-4.91812910911164,0.000125410111702882,
24.2351405640093));
#54448=CARTESIAN_POINT('Origin',(0.,0.,-3.23514056400933));
#54449=CARTESIAN_POINT('',(-4.91782637975552,-5.24142894187958E-6,20.3898594359907));
#54450=CARTESIAN_POINT('',(-4.91850368862107,9.83542250791031E-5,20.7351405640093));
#54451=CARTESIAN_POINT('',(-4.91825,1.47989506776076E-12,-3.23514056400933));
#54452=CARTESIAN_POINT('Ctrl Pts',(-4.91782637975553,-5.24142894198221E-6,
20.3898594359907));
#54453=CARTESIAN_POINT('Ctrl Pts',(-4.91784131778503,-0.404115038784516,
20.4127390376695));
#54454=CARTESIAN_POINT('Ctrl Pts',(-4.76876465270878,-1.627595371266,20.4820097918222));
#54455=CARTESIAN_POINT('Ctrl Pts',(-3.76535729773513,-3.48065452827909,
20.5976716984489));
#54456=CARTESIAN_POINT('Ctrl Pts',(-1.63721722455307,-4.85925830600346,
20.7368451558709));
#54457=CARTESIAN_POINT('Ctrl Pts',(0.891279837899838,-5.04960313048365,
20.8760186132929));
#54458=CARTESIAN_POINT('Ctrl Pts',(3.20182774421876,-4.00514302131496,21.0151920707148));
#54459=CARTESIAN_POINT('Ctrl Pts',(4.72941655591346,-1.98128507930803,21.1543655281368));
#54460=CARTESIAN_POINT('Ctrl Pts',(5.10049727269117,0.527066500649415,21.2935389855586));
#54461=CARTESIAN_POINT('Ctrl Pts',(4.22432765441569,2.9065318496407,21.4327124429807));
#54462=CARTESIAN_POINT('Ctrl Pts',(2.3151618789705,4.57524829916352,21.5718859004026));
#54463=CARTESIAN_POINT('Ctrl Pts',(-0.160142112979361,5.12515619552101,
21.7110593578246));
#54464=CARTESIAN_POINT('Ctrl Pts',(-2.5962857459699,4.4217837859975,21.8502328152465));
#54465=CARTESIAN_POINT('Ctrl Pts',(-4.39754652471548,2.63713027509066,21.9894062726684));
#54466=CARTESIAN_POINT('Ctrl Pts',(-4.90109526461051,0.951811533492146,
22.0859484795832));
#54467=CARTESIAN_POINT('Ctrl Pts',(-4.91864559982637,0.0664459672029366,
22.136099534024));
#54468=CARTESIAN_POINT('Ctrl Pts',(-4.91860118447858,6.69814320593525E-5,
22.1398594359908));
#54469=CARTESIAN_POINT('Ctrl Pts',(-4.91850368862107,9.83542250790163E-5,
20.7351405640093));
#54470=CARTESIAN_POINT('Ctrl Pts',(-4.91786254178827,-0.712520933069854,
20.7755031090711));
#54471=CARTESIAN_POINT('Ctrl Pts',(-4.5811979304639,-2.24478329879145,20.8622568066069));
#54472=CARTESIAN_POINT('Ctrl Pts',(-3.04721056302127,-4.12400040999737,
20.9954016566167));
#54473=CARTESIAN_POINT('Ctrl Pts',(-0.698616677582171,-5.07984314077225,
21.1345751140387));
#54474=CARTESIAN_POINT('Ctrl Pts',(1.82081346922569,-4.79348619559222,21.2737485714606));
#54475=CARTESIAN_POINT('Ctrl Pts',(3.89499091063157,-3.33495388321102,21.4129220288826));
#54476=CARTESIAN_POINT('Ctrl Pts',(5.01670657064901,-1.06090846968716,21.5520954863046));
#54477=CARTESIAN_POINT('Ctrl Pts',(4.91166165878904,1.47256624524283,21.6912689437265));
#54478=CARTESIAN_POINT('Ctrl Pts',(3.6055433374024,3.6459469056968,21.8304424011485));
#54479=CARTESIAN_POINT('Ctrl Pts',(1.41774331025312,4.92776577195785,21.9696158585704));
#54480=CARTESIAN_POINT('Ctrl Pts',(-1.11674464244417,5.00457320863818,22.1087893159924));
#54481=CARTESIAN_POINT('Ctrl Pts',(-3.37814939266335,3.85758710567824,22.2479627734143));
#54482=CARTESIAN_POINT('Ctrl Pts',(-4.67194924907029,1.97339756309458,22.3734131894199));
#54483=CARTESIAN_POINT('Ctrl Pts',(-4.91755649890211,0.576789506777712,
22.4524724529516));
#54484=CARTESIAN_POINT('Ctrl Pts',(-4.91808775011422,-0.000121504406732746,
22.4851405640093));
#54485=CARTESIAN_POINT('Origin',(0.,0.,-3.23514056400933));
#54486=CARTESIAN_POINT('',(-4.91862258429063,-5.67213663493321E-5,18.6398594359907));
#54487=CARTESIAN_POINT('',(-4.91784723885709,-4.2125959418271E-5,18.9851405640093));
#54488=CARTESIAN_POINT('',(-4.91825,1.47989506776076E-12,-3.23514056400933));
#54489=CARTESIAN_POINT('Ctrl Pts',(-4.91862258429063,-5.67213663495159E-5,
18.6398594359907));
#54490=CARTESIAN_POINT('Ctrl Pts',(-4.91865476642852,-0.0552782982130806,
18.642987388841));
#54491=CARTESIAN_POINT('Ctrl Pts',(-4.90423951910381,-0.929482791963975,
18.6925064941653));
#54492=CARTESIAN_POINT('Ctrl Pts',(-4.41539501983301,-2.60713604241717,
18.7884167519636));
#54493=CARTESIAN_POINT('Ctrl Pts',(-2.62632371694331,-4.40400899847605,
18.9275902093855));
#54494=CARTESIAN_POINT('Ctrl Pts',(-0.195024223195767,-5.12394741163527,
19.0667636668075));
#54495=CARTESIAN_POINT('Ctrl Pts',(2.28396552793643,-4.59090110893657,19.2059371242294));
#54496=CARTESIAN_POINT('Ctrl Pts',(4.2044456636982,-2.9352185925151,19.3451105816514));
#54497=CARTESIAN_POINT('Ctrl Pts',(5.09679148580437,-0.561772262637615,
19.4842840390733));
#54498=CARTESIAN_POINT('Ctrl Pts',(4.74279316762406,1.94904707330927,19.6234574964953));
#54499=CARTESIAN_POINT('Ctrl Pts',(3.22901570416719,3.98325609358456,19.7626309539172));
#54500=CARTESIAN_POINT('Ctrl Pts',(0.925630737050274,5.04341940190033,19.9018044113392));
#54501=CARTESIAN_POINT('Ctrl Pts',(-1.60410338490353,4.87028991492066,20.0409778687611));
#54502=CARTESIAN_POINT('Ctrl Pts',(-3.7415780118875,3.5062038597031,20.1801513261831));
#54503=CARTESIAN_POINT('Ctrl Pts',(-4.76312665923809,1.64993048430327,20.2964451819263));
#54504=CARTESIAN_POINT('Ctrl Pts',(-4.91781102912816,0.415266324955308,
20.3663478851955));
#54505=CARTESIAN_POINT('Ctrl Pts',(-4.91782637975553,-5.24142894198221E-6,
20.3898594359907));
#54506=CARTESIAN_POINT('Ctrl Pts',(-4.91784723885709,-4.21259594185139E-5,
18.9851405640093));
#54507=CARTESIAN_POINT('Ctrl Pts',(-4.91795594482061,-0.364076614836121,
19.0057514602427));
#54508=CARTESIAN_POINT('Ctrl Pts',(-4.78832206838964,-1.54740630006116,
19.07275350895));
#54509=CARTESIAN_POINT('Ctrl Pts',(-3.84928009761185,-3.3876118914622,19.1861467101313));
#54510=CARTESIAN_POINT('Ctrl Pts',(-1.75546046578727,-4.8178034569817,19.3253201675533));
#54511=CARTESIAN_POINT('Ctrl Pts',(0.767630771739118,-5.06987323266825,
19.4644936249752));
#54512=CARTESIAN_POINT('Ctrl Pts',(3.10300938320942,-4.08218132433643,19.6036670823972));
#54513=CARTESIAN_POINT('Ctrl Pts',(4.67959345250773,-2.09625301819547,19.7428405398192));
#54514=CARTESIAN_POINT('Ctrl Pts',(5.11185292177081,0.402282616117053,19.8820139972411));
#54515=CARTESIAN_POINT('Ctrl Pts',(4.29408520181098,2.80244605240401,20.0211874546631));
#54516=CARTESIAN_POINT('Ctrl Pts',(2.4262631596223,4.5173132144347,20.160360912085));
#54517=CARTESIAN_POINT('Ctrl Pts',(-0.0348652558426957,5.12753898190759,
20.299534369507));
#54518=CARTESIAN_POINT('Ctrl Pts',(-2.4874678943674,4.48390176872088,20.4387078269289));
#54519=CARTESIAN_POINT('Ctrl Pts',(-4.33179745699125,2.74379343038994,20.5778812843509));
#54520=CARTESIAN_POINT('Ctrl Pts',(-4.88917263131133,1.03197826464391,20.676692196711));
#54521=CARTESIAN_POINT('Ctrl Pts',(-4.91859945122828,0.106536189372549,
20.7291119565971));
#54522=CARTESIAN_POINT('Ctrl Pts',(-4.91850368862107,9.83542250790163E-5,
20.7351405640093));
#54523=CARTESIAN_POINT('Origin',(0.,0.,-3.23514056400933));
#54524=CARTESIAN_POINT('',(-4.91795812443448,9.68028131021826E-5,16.8898594359907));
#54525=CARTESIAN_POINT('',(-4.91867111326921,-1.61887755736889E-5,17.2351405640093));
#54526=CARTESIAN_POINT('',(-4.91825,1.47989506776076E-12,-3.23514056400933));
#54527=CARTESIAN_POINT('Ctrl Pts',(-4.91795812443448,9.68028131020232E-5,
16.8898594359907));
#54528=CARTESIAN_POINT('Ctrl Pts',(-4.91758682380195,-0.525629068321328,
16.9196268924865));
#54529=CARTESIAN_POINT('Ctrl Pts',(-4.70277528584012,-1.87096968829015,
16.9957855014563));
#54530=CARTESIAN_POINT('Ctrl Pts',(-3.4970054763967,-3.75017655889538,17.1183352629001));
#54531=CARTESIAN_POINT('Ctrl Pts',(-1.27253436014598,-4.96724549696155,
17.2575087203221));
#54532=CARTESIAN_POINT('Ctrl Pts',(1.2631160043629,-4.96964882907829,17.3966821777441));
#54533=CARTESIAN_POINT('Ctrl Pts',(3.48989023867801,-3.75679885631596,17.535855635166));
#54534=CARTESIAN_POINT('Ctrl Pts',(4.86326400304377,-1.62527990252007,17.675029092588));
#54535=CARTESIAN_POINT('Ctrl Pts',(5.04739928085542,0.903676946954519,17.8142025500099));
#54536=CARTESIAN_POINT('Ctrl Pts',(3.9972685434884,3.21165311266256,17.9533760074318));
#54537=CARTESIAN_POINT('Ctrl Pts',(1.96966555908043,4.73426753682229,18.0925494648538));
#54538=CARTESIAN_POINT('Ctrl Pts',(-0.539589683365057,5.09918763122548,
18.2317229222758));
#54539=CARTESIAN_POINT('Ctrl Pts',(-2.91689633778329,4.21717764381148,18.3708963796977));
#54540=CARTESIAN_POINT('Ctrl Pts',(-4.5435203376001,2.34692079867374,18.5069418842694));
#54541=CARTESIAN_POINT('Ctrl Pts',(-4.91817746816439,0.763721448255779,
18.596596236367));
#54542=CARTESIAN_POINT('Ctrl Pts',(-4.91862258429063,-5.67213663495159E-5,
18.6398594359907));
#54543=CARTESIAN_POINT('Ctrl Pts',(-4.91867111326921,-1.61887755739448E-5,
17.2351405640093));
#54544=CARTESIAN_POINT('Ctrl Pts',(-4.91867394862149,-0.0151850987544867,
17.2359998114142));
#54545=CARTESIAN_POINT('Ctrl Pts',(-4.91489622429265,-0.849328838714203,
17.2832502112931));
#54546=CARTESIAN_POINT('Ctrl Pts',(-4.47778002818978,-2.49847105570419,
17.376891763646));
#54547=CARTESIAN_POINT('Ctrl Pts',(-2.73314800394566,-4.33852205083421,
17.5160652210679));
#54548=CARTESIAN_POINT('Ctrl Pts',(-0.320165506910762,-5.11765235681669,
17.6552386784899));
#54549=CARTESIAN_POINT('Ctrl Pts',(2.17110867707493,-4.64533730846069,17.7944121359119));
#54550=CARTESIAN_POINT('Ctrl Pts',(4.13147070090376,-3.0370744878288,17.9335855933338));
#54551=CARTESIAN_POINT('Ctrl Pts',(5.08154334695868,-0.686140517697928,
18.0727590507557));
#54552=CARTESIAN_POINT('Ctrl Pts',(4.78900055706072,1.83257885547087,18.2119325081777));
#54553=CARTESIAN_POINT('Ctrl Pts',(3.3253792957861,3.90316847397136,18.3511059655996));
#54554=CARTESIAN_POINT('Ctrl Pts',(1.04858625554496,5.01929661025616,18.4902794230216));
#54555=CARTESIAN_POINT('Ctrl Pts',(-1.4846228729006,4.90803081920919,18.6294528804436));
#54556=CARTESIAN_POINT('Ctrl Pts',(-3.6547896788716,3.5965794861591,18.7686263378655));
#54557=CARTESIAN_POINT('Ctrl Pts',(-4.74219752133363,1.7301058879693,18.8871888990541));
#54558=CARTESIAN_POINT('Ctrl Pts',(-4.91771126866139,0.455294813171815,
18.9593603077687));
#54559=CARTESIAN_POINT('Ctrl Pts',(-4.91784723885709,-4.21259594185139E-5,
18.9851405640093));
#54560=CARTESIAN_POINT('Origin',(0.,0.,-3.23514056400933));
#54561=CARTESIAN_POINT('',(-4.91828854462098,-0.000127404755611427,15.1398594359907));
#54562=CARTESIAN_POINT('',(-4.91788408102176,6.79148635503168E-5,15.4851405640093));
#54563=CARTESIAN_POINT('',(-4.91825,1.47989506776076E-12,-3.23514056400933));
#54564=CARTESIAN_POINT('Ctrl Pts',(-4.91828854462098,-0.000127404755611727,
15.1398594359907));
#54565=CARTESIAN_POINT('Ctrl Pts',(-4.91847218829568,-0.176983412021483,
15.1498752436581));
#54566=CARTESIAN_POINT('Ctrl Pts',(-4.86579387478643,-1.17289109012218,
15.2062822037994));
#54567=CARTESIAN_POINT('Ctrl Pts',(-4.21000220374625,-2.92724323712408,
15.3090803164148));
#54568=CARTESIAN_POINT('Ctrl Pts',(-2.29266408325714,-4.58656330231903,
15.4482537738367));
#54569=CARTESIAN_POINT('Ctrl Pts',(0.185310754227624,-5.12430789953185,
15.5874272312587));
#54570=CARTESIAN_POINT('Ctrl Pts',(2.6179706179084,-4.40897962896238,15.7266006886806));
#54571=CARTESIAN_POINT('Ctrl Pts',(4.41044491618784,-2.61550132213878,15.8657741461026));
#54572=CARTESIAN_POINT('Ctrl Pts',(5.12441086413413,-0.182441279268398,
16.0049476035245));
#54573=CARTESIAN_POINT('Ctrl Pts',(4.58527876584435,2.29523205021492,16.1441210609465));
#54574=CARTESIAN_POINT('Ctrl Pts',(2.92488531375835,4.21164070478449,16.2832945183684));
#54575=CARTESIAN_POINT('Ctrl Pts',(0.549254897012139,5.09815560599567,16.4224679757903));
#54576=CARTESIAN_POINT('Ctrl Pts',(-1.96068759122481,4.73799279172668,16.5616414332123));
#54577=CARTESIAN_POINT('Ctrl Pts',(-3.99117324920656,3.21922469232187,16.7008148906343));
#54578=CARTESIAN_POINT('Ctrl Pts',(-4.82013201349797,1.40646381671154,16.8102208915604));
#54579=CARTESIAN_POINT('Ctrl Pts',(-4.91816547801985,0.293689473413913,
16.8732357400126));
#54580=CARTESIAN_POINT('Ctrl Pts',(-4.91795812443448,9.68028131020232E-5,
16.8898594359907));
#54581=CARTESIAN_POINT('Ctrl Pts',(-4.91788408102176,6.79148635503515E-5,
15.4851405640093));
#54582=CARTESIAN_POINT('Ctrl Pts',(-4.91764809163557,-0.485611072828922,
15.5126393150597));
#54583=CARTESIAN_POINT('Ctrl Pts',(-4.72562172430427,-1.7908264783202,15.5865292185841));
#54584=CARTESIAN_POINT('Ctrl Pts',(-3.587593947644,-3.66361041376876,15.7068102745826));
#54585=CARTESIAN_POINT('Ctrl Pts',(-1.39352506003175,-4.93466913826148,
15.8459837320045));
#54586=CARTESIAN_POINT('Ctrl Pts',(1.1413095421973,-4.99902831817707,15.9851571894265));
#54587=CARTESIAN_POINT('Ctrl Pts',(3.39705396305783,-3.8409498784962,16.1243306468484));
#54588=CARTESIAN_POINT('Ctrl Pts',(4.82209963689558,-1.74362458370441,16.2635041042704));
#54589=CARTESIAN_POINT('Ctrl Pts',(5.06797295434764,0.780078028819932,16.4026775616923));
#54590=CARTESIAN_POINT('Ctrl Pts',(4.07454927242783,3.11302422470575,16.5418510191143));
#54591=CARTESIAN_POINT('Ctrl Pts',(2.08475549686315,4.68472689869385,16.6810244765362));
#54592=CARTESIAN_POINT('Ctrl Pts',(-0.414834059965531,5.1108496651476,16.8201979339582));
#54593=CARTESIAN_POINT('Ctrl Pts',(-2.81298215087013,4.28719057378289,16.9593713913801));
#54594=CARTESIAN_POINT('Ctrl Pts',(-4.51269839905733,2.42672090768734,17.0976856013972));
#54595=CARTESIAN_POINT('Ctrl Pts',(-4.91852086668098,0.803791149140066,
17.1896086589402));
#54596=CARTESIAN_POINT('Ctrl Pts',(-4.91867111326921,-1.61887755739448E-5,
17.2351405640093));
#54597=CARTESIAN_POINT('Origin',(0.,0.,-3.23514056400933));
#54598=CARTESIAN_POINT('',(-4.91830432977965,0.000126561679052736,13.3898594359907));
#54599=CARTESIAN_POINT('',(-4.91841486112574,-0.000115290859867556,13.7351405640093));
#54600=CARTESIAN_POINT('',(-4.91825,1.47989506776076E-12,-3.23514056400933));
#54601=CARTESIAN_POINT('Ctrl Pts',(-4.91830432977965,0.000126561679052607,
13.3898594359907));
#54602=CARTESIAN_POINT('Ctrl Pts',(-4.91763218604279,-0.64711550896179,
13.4265147473036));
#54603=CARTESIAN_POINT('Ctrl Pts',(-4.62657036081707,-2.11409703197736,
13.5095612110905));
#54604=CARTESIAN_POINT('Ctrl Pts',(-3.20941426864339,-3.99906633816759,
13.6389988273513));
#54605=CARTESIAN_POINT('Ctrl Pts',(-0.900850425695856,-5.04790451923969,
13.7781722847733));
#54606=CARTESIAN_POINT('Ctrl Pts',(1.62800291751233,-4.86235313664159,13.9173457421952));
#54607=CARTESIAN_POINT('Ctrl Pts',(3.75875249244549,-3.4877860062469,14.0565191996172));
#54608=CARTESIAN_POINT('Ctrl Pts',(4.97035535384435,-1.26033296447714,14.1956926570391));
#54609=CARTESIAN_POINT('Ctrl Pts',(4.96653214029797,1.27531565669998,14.3348661144611));
#54610=CARTESIAN_POINT('Ctrl Pts',(3.7482177615067,3.49910490513827,14.474039571883));
#54611=CARTESIAN_POINT('Ctrl Pts',(1.61333278009552,4.86724037474072,14.613213029305));
#54612=CARTESIAN_POINT('Ctrl Pts',(-0.916068606863061,5.04516499555335,
14.7523864867269));
#54613=CARTESIAN_POINT('Ctrl Pts',(-3.22145911492965,3.98936996224636,14.8915599441489));
#54614=CARTESIAN_POINT('Ctrl Pts',(-4.62987159599441,2.10422201302728,15.0207175939035));
#54615=CARTESIAN_POINT('Ctrl Pts',(-4.91762158872381,0.642177086213023,
15.1034840911841));
#54616=CARTESIAN_POINT('Ctrl Pts',(-4.91828854462098,-0.000127404755611727,
15.1398594359907));
#54617=CARTESIAN_POINT('Ctrl Pts',(-4.91841486112574,-0.000115290859867678,
13.7351405640093));
#54618=CARTESIAN_POINT('Ctrl Pts',(-4.9185513730654,-0.136901079078092,
13.7428876662313));
#54619=CARTESIAN_POINT('Ctrl Pts',(-4.87947714473731,-1.09270897128707,
13.7970259209272));
#54620=CARTESIAN_POINT('Ctrl Pts',(-4.28027009411781,-2.82350128713404,
13.8975553280972));
#54621=CARTESIAN_POINT('Ctrl Pts',(-2.40404855375509,-4.52917455484274,
14.0367287855191));
#54622=CARTESIAN_POINT('Ctrl Pts',(0.06004711021698,-5.12730591457165,14.1759022429411));
#54623=CARTESIAN_POINT('Ctrl Pts',(2.5094591513317,-4.47163128677269,14.315075700363));
#54624=CARTESIAN_POINT('Ctrl Pts',(4.34522048351284,-2.72248609669679,14.454249157785));
#54625=CARTESIAN_POINT('Ctrl Pts',(5.11842312500342,-0.307597643809348,
14.5934226152069));
#54626=CARTESIAN_POINT('Ctrl Pts',(4.63999193232155,2.18250921304762,14.7325960726289));
#54627=CARTESIAN_POINT('Ctrl Pts',(3.02692009916372,4.13891607915956,14.8717695300508));
#54628=CARTESIAN_POINT('Ctrl Pts',(0.673660220405915,5.08321291158352,15.0109429874728));
#54629=CARTESIAN_POINT('Ctrl Pts',(-1.84433319131777,4.78448604099233,15.1501164448947));
#54630=CARTESIAN_POINT('Ctrl Pts',(-3.91132250131647,3.31578465641879,15.2892899023167));
#54631=CARTESIAN_POINT('Ctrl Pts',(-4.80243024213341,1.4866607259055,15.4009646086882));
#54632=CARTESIAN_POINT('Ctrl Pts',(-4.91804621224755,0.333742792738227,
15.4662481625857));
#54633=CARTESIAN_POINT('Ctrl Pts',(-4.91788408102176,6.79148635503515E-5,
15.4851405640093));
#54634=CARTESIAN_POINT('Origin',(0.,0.,-3.23514056400933));
#54635=CARTESIAN_POINT('',(-4.91794754609162,-9.36338042964645E-5,11.6398594359907));
#54636=CARTESIAN_POINT('',(-4.91817784002761,0.000128112752882797,11.9851405640093));
#54637=CARTESIAN_POINT('',(-4.91825,1.47989506776076E-12,-3.23514056400933));
#54638=CARTESIAN_POINT('Ctrl Pts',(-4.91794754609163,-9.36338042967569E-5,
11.6398594359907));
#54639=CARTESIAN_POINT('Ctrl Pts',(-4.91815090375448,-0.298632658744152,
11.6567630984751));
#54640=CARTESIAN_POINT('Ctrl Pts',(-4.81800407439185,-1.41636045649421,
11.7200579134335));
#54641=CARTESIAN_POINT('Ctrl Pts',(-3.98144732521719,-3.23124569189002,
11.829743880866));
#54642=CARTESIAN_POINT('Ctrl Pts',(-1.94639095768057,-4.74388382706577,
11.9689173382879));
#54643=CARTESIAN_POINT('Ctrl Pts',(0.564626212170274,-5.09647611250825,
12.1080907957099));
#54644=CARTESIAN_POINT('Ctrl Pts',(2.93757248527155,-4.20280137748769,12.2472642531318));
#54645=CARTESIAN_POINT('Ctrl Pts',(4.59217933564339,-2.28139441441562,12.3864377105538));
#54646=CARTESIAN_POINT('Ctrl Pts',(5.12383740106595,0.197893436663885,12.5256111679757));
#54647=CARTESIAN_POINT('Ctrl Pts',(4.40253765207021,2.62878940711139,12.6647846253977));
#54648=CARTESIAN_POINT('Ctrl Pts',(2.60466315593581,4.41685423904247,12.8039580828196));
#54649=CARTESIAN_POINT('Ctrl Pts',(0.169857235225308,5.12484341658148,12.9431315402416));
#54650=CARTESIAN_POINT('Ctrl Pts',(-2.30648473230954,4.57962877365185,13.0823049976635));
#54651=CARTESIAN_POINT('Ctrl Pts',(-4.21881034979734,2.9145343980265,13.2214784550854));
#54652=CARTESIAN_POINT('Ctrl Pts',(-4.86753707266041,1.16299591758168,13.3239966011945));
#54653=CARTESIAN_POINT('Ctrl Pts',(-4.9184828546489,0.172037418983138,13.3801235948296));
#54654=CARTESIAN_POINT('Ctrl Pts',(-4.91830432977965,0.000126561679052607,
13.3898594359907));
#54655=CARTESIAN_POINT('Ctrl Pts',(-4.91817784002761,0.000128112752882659,
11.9851405640093));
#54656=CARTESIAN_POINT('Ctrl Pts',(-4.91757026063081,-0.607099161997894,
12.0195271698768));
#54657=CARTESIAN_POINT('Ctrl Pts',(-4.65282093162953,-2.03405502531225,
12.1003049282183));
#54658=CARTESIAN_POINT('Ctrl Pts',(-3.30617002296448,-3.91945294349836,
12.2274738390338));
#54659=CARTESIAN_POINT('Ctrl Pts',(-1.02392293276547,-5.02438587538853,
12.3666472964557));
#54660=CARTESIAN_POINT('Ctrl Pts',(1.50870919886821,-4.90068037626382,12.5058207538777));
#54661=CARTESIAN_POINT('Ctrl Pts',(3.67240905719958,-3.57858677603957,12.6449942112996));
#54662=CARTESIAN_POINT('Ctrl Pts',(4.93807619790383,-1.38140329402478,12.7841676687216));
#54663=CARTESIAN_POINT('Ctrl Pts',(4.99621064854467,1.15358170599905,12.9233411261435));
#54664=CARTESIAN_POINT('Ctrl Pts',(3.83259649856215,3.40647555051493,13.0625145835655));
#54665=CARTESIAN_POINT('Ctrl Pts',(1.7317781876149,4.82636673968609,13.2016880409874));
#54666=CARTESIAN_POINT('Ctrl Pts',(-0.792520582052584,5.06604211629452,
13.3408614984094));
#54667=CARTESIAN_POINT('Ctrl Pts',(-3.12302029475477,4.06689265110314,13.4800349558313));
#54668=CARTESIAN_POINT('Ctrl Pts',(-4.60261538530517,2.18422194630641,13.6114613110313));
#54669=CARTESIAN_POINT('Ctrl Pts',(-4.91773391306217,0.68219878247996,13.6964965137573));
#54670=CARTESIAN_POINT('Ctrl Pts',(-4.91841486112574,-0.000115290859867678,
13.7351405640093));
#54671=CARTESIAN_POINT('Origin',(0.,0.,-3.23514056400933));
#54672=CARTESIAN_POINT('',(-4.91863108450388,5.20022792591365E-5,9.88985943599073));
#54673=CARTESIAN_POINT('',(-4.91804344864283,-0.000115457371072658,10.2351405640093));
#54674=CARTESIAN_POINT('',(-4.91825,1.47989506776076E-12,-3.23514056400933));
#54675=CARTESIAN_POINT('Ctrl Pts',(-4.91863108450388,5.20022792590506E-5,
9.88985943599073));
#54676=CARTESIAN_POINT('Ctrl Pts',(-4.91821498045426,-0.768664899305898,
9.93340260212068));
#54677=CARTESIAN_POINT('Ctrl Pts',(-4.53978139223194,-2.35677273363979,
10.0233369207246));
#54678=CARTESIAN_POINT('Ctrl Pts',(-2.90416590773529,-4.225954555504,10.1596623918025));
#54679=CARTESIAN_POINT('Ctrl Pts',(-0.524210305286386,-5.10079161313893,
10.2988358492245));
#54680=CARTESIAN_POINT('Ctrl Pts',(1.98393308826428,-4.72830635916573,10.4380093066464));
#54681=CARTESIAN_POINT('Ctrl Pts',(4.00693531287256,-3.1995844922883,10.5771827640684));
#54682=CARTESIAN_POINT('Ctrl Pts',(5.05010142654417,-0.888452084500591,
10.7163562214903));
#54683=CARTESIAN_POINT('Ctrl Pts',(4.85834075571687,1.63993799461361,10.8555296789123));
#54684=CARTESIAN_POINT('Ctrl Pts',(3.47854550484689,3.76730576082515,10.9947031363342));
#54685=CARTESIAN_POINT('Ctrl Pts',(1.24812396903648,4.97343523962598,11.1338765937562));
#54686=CARTESIAN_POINT('Ctrl Pts',(-1.28750761891996,4.96338550347039,11.2730500511781));
#54687=CARTESIAN_POINT('Ctrl Pts',(-3.5082984720956,3.73961406505117,11.4122235086001));
#54688=CARTESIAN_POINT('Ctrl Pts',(-4.70565429318266,1.86108102271416,11.5344933035376));
#54689=CARTESIAN_POINT('Ctrl Pts',(-4.9175928000682,0.520690930932643,11.6103719460012));
#54690=CARTESIAN_POINT('Ctrl Pts',(-4.91794754609163,-9.36338042967569E-5,
11.6398594359907));
#54691=CARTESIAN_POINT('Ctrl Pts',(-4.91804344864283,-0.000115457371073178,
10.2351405640093));
#54692=CARTESIAN_POINT('Ctrl Pts',(-4.91826654662029,-0.258571969827967,
10.2497755210483));
#54693=CARTESIAN_POINT('Ctrl Pts',(-4.83479258826795,-1.33616357645592,
10.3108016305613));
#54694=CARTESIAN_POINT('Ctrl Pts',(-4.05921150653168,-3.13299753308037,
10.4182188925484));
#54695=CARTESIAN_POINT('Ctrl Pts',(-2.06172281055525,-4.69490901397279,
10.5573923499703));
#54696=CARTESIAN_POINT('Ctrl Pts',(0.439929367680037,-5.10875070330306,
10.6965658073923));
#54697=CARTESIAN_POINT('Ctrl Pts',(2.83400339776564,-4.27332380454602,10.8357392648142));
#54698=CARTESIAN_POINT('Ctrl Pts',(4.53506427669625,-2.39291947279475,10.9749127222362));
#54699=CARTESIAN_POINT('Ctrl Pts',(5.12714300424288,0.0726375322416105,
11.1140861796581));
#54700=CARTESIAN_POINT('Ctrl Pts',(4.46545558154636,2.52043211499204,11.2532596370801));
#54701=CARTESIAN_POINT('Ctrl Pts',(2.71180777293433,4.35189271463576,11.392433094502));
#54702=CARTESIAN_POINT('Ctrl Pts',(0.295027925902909,5.11916302924455,11.531606551924));
#54703=CARTESIAN_POINT('Ctrl Pts',(-2.19389658855195,4.63461857716327,11.6707800093459));
#54704=CARTESIAN_POINT('Ctrl Pts',(-4.14633649986933,3.01674745825668,11.8099534667679));
#54705=CARTESIAN_POINT('Ctrl Pts',(-4.85296596667775,1.24318419508919,11.9147403183223));
#54706=CARTESIAN_POINT('Ctrl Pts',(-4.91838994921961,0.212114377071997,
11.9731360174028));
#54707=CARTESIAN_POINT('Ctrl Pts',(-4.91817784002761,0.000128112752882659,
11.9851405640093));
#54708=CARTESIAN_POINT('Origin',(0.,0.,-3.23514056400933));
#54709=CARTESIAN_POINT('',(-4.91782719367126,9.87882777895753E-6,8.13985943599073));
#54710=CARTESIAN_POINT('',(-4.91854624166208,8.68734550606501E-5,8.48514056400926));
#54711=CARTESIAN_POINT('',(-4.91825,1.47989506776076E-12,-3.23514056400933));
#54712=CARTESIAN_POINT('Ctrl Pts',(-4.91782719367126,9.87882777886417E-6,
8.13985943599073));
#54713=CARTESIAN_POINT('Ctrl Pts',(-4.91779791116503,-0.420206382800527,
8.16365095329221));
#54714=CARTESIAN_POINT('Ctrl Pts',(-4.76060227876805,-1.65982512688071,
8.23383362306768));
#54715=CARTESIAN_POINT('Ctrl Pts',(-3.73098781882938,-3.51747088411314,
8.35040744531713));
#54716=CARTESIAN_POINT('Ctrl Pts',(-1.58940942229392,-4.87510504637185,
8.48958090273909));
#54717=CARTESIAN_POINT('Ctrl Pts',(0.940835280389158,-5.04060517200187,
8.62875436016105));
#54718=CARTESIAN_POINT('Ctrl Pts',(3.24101278453099,-3.97350068017404,8.76792781758299));
#54719=CARTESIAN_POINT('Ctrl Pts',(4.74864907841449,-1.93473601685351,8.90710127500494));
#54720=CARTESIAN_POINT('Ctrl Pts',(5.09507425160708,0.577139407290319,9.04627473242689));
#54721=CARTESIAN_POINT('Ctrl Pts',(4.19557520845658,2.94788401994064,9.18544818984885));
#54722=CARTESIAN_POINT('Ctrl Pts',(2.27011098883077,4.59776767825721,9.3246216472708));
#54723=CARTESIAN_POINT('Ctrl Pts',(-0.210474925808355,5.12333600600652,
9.46379510469275));
#54724=CARTESIAN_POINT('Ctrl Pts',(-2.63959234478916,4.39606912800144,9.60296856211471));
#54725=CARTESIAN_POINT('Ctrl Pts',(-4.42323692839189,2.59380928368822,9.74214201953665));
#54726=CARTESIAN_POINT('Ctrl Pts',(-4.90560794918632,0.919590948282322,
9.83777231082867));
#54727=CARTESIAN_POINT('Ctrl Pts',(-4.91865830022465,0.0503307356082542,
9.88701144964669));
#54728=CARTESIAN_POINT('Ctrl Pts',(-4.91863108450388,5.20022792590506E-5,
9.88985943599073));
#54729=CARTESIAN_POINT('Ctrl Pts',(-4.91854624166208,8.68734550606501E-5,
8.48514056400926));
#54730=CARTESIAN_POINT('Ctrl Pts',(-4.91794764432125,-0.728614457117709,
8.52641502469384));
#54731=CARTESIAN_POINT('Ctrl Pts',(-4.56956039415971,-2.27690562510606,
8.6140806378524));
#54732=CARTESIAN_POINT('Ctrl Pts',(-3.00655662644843,-4.15373191828816,
8.74813740348495));
#54733=CARTESIAN_POINT('Ctrl Pts',(-0.648687514646424,-5.08646007606358,
8.88731086090689));
#54734=CARTESIAN_POINT('Ctrl Pts',(1.86780842837057,-4.77537048530841,9.02648431832885));
#54735=CARTESIAN_POINT('Ctrl Pts',(3.92755975149067,-3.29653545339913,9.1656577757508));
#54736=CARTESIAN_POINT('Ctrl Pts',(5.0268850702256,-1.01158197284738,9.30483123317275));
#54737=CARTESIAN_POINT('Ctrl Pts',(4.89696081722127,1.52073875193816,9.44400469059471));
#54738=CARTESIAN_POINT('Ctrl Pts',(3.56955802565887,3.68118555610841,9.58317814801665));
#54739=CARTESIAN_POINT('Ctrl Pts',(1.36927319819533,4.9414534810874,9.72235160543861));
#54740=CARTESIAN_POINT('Ctrl Pts',(-1.16584691373595,4.99336285190443,9.86152506286056));
#54741=CARTESIAN_POINT('Ctrl Pts',(-3.41587659702151,3.82422000818044,10.0006985202825));
#54742=CARTESIAN_POINT('Ctrl Pts',(-4.68183725211151,1.94120147697101,10.1252370206654));
#54743=CARTESIAN_POINT('Ctrl Pts',(-4.91755935135749,0.560705835039386,
10.2033843685743));
#54744=CARTESIAN_POINT('Ctrl Pts',(-4.91804344864283,-0.000115457371073178,
10.2351405640093));
#54745=CARTESIAN_POINT('Origin',(0.,0.,-3.23514056400933));
#54746=CARTESIAN_POINT('',(-4.91859079181753,-7.13374654231665E-5,6.38985943599073));
#54747=CARTESIAN_POINT('',(-4.91783496857819,-2.75488291934245E-5,6.73514056400926));
#54748=CARTESIAN_POINT('',(-4.91825,1.47989506776076E-12,-3.23514056400933));
#54749=CARTESIAN_POINT('Ctrl Pts',(-4.91859079181753,-7.13374654238812E-5,
6.38985943599073));
#54750=CARTESIAN_POINT('Ctrl Pts',(-4.91864101597956,-0.0713934139407059,
6.39389930446375));
#54751=CARTESIAN_POINT('Ctrl Pts',(-4.89967772397134,-0.96170387456932,
6.44433032541076));
#54752=CARTESIAN_POINT('Ctrl Pts',(-4.3895740957611,-2.65037936580031,6.54115249883176));
#54753=CARTESIAN_POINT('Ctrl Pts',(-2.58293977084456,-4.42959294574867,
6.68032595625371));
#54754=CARTESIAN_POINT('Ctrl Pts',(-0.14468615032387,-5.12561581107493,
6.81949941367566));
#54755=CARTESIAN_POINT('Ctrl Pts',(2.32894830461766,-4.5682459784096,6.95867287109761));
#54756=CARTESIAN_POINT('Ctrl Pts',(4.2330732788251,-2.89377990540639,7.09784632851956));
#54757=CARTESIAN_POINT('Ctrl Pts',(5.10206348419584,-0.51168323020428,7.23701978594152));
#54758=CARTESIAN_POINT('Ctrl Pts',(4.72342036091109,1.9955379272185,7.37619324336347));
#54759=CARTESIAN_POINT('Ctrl Pts',(3.18973542252992,4.01478012587175,7.51536670078542));
#54760=CARTESIAN_POINT('Ctrl Pts',(0.876048385964622,5.05226788188094,7.65454015820737));
#54761=CARTESIAN_POINT('Ctrl Pts',(-1.65186318293549,4.85429907913586,7.79371361562932));
#54762=CARTESIAN_POINT('Ctrl Pts',(-3.77583631245843,3.46928402791661,7.93288707305128));
#54763=CARTESIAN_POINT('Ctrl Pts',(-4.77123581750181,1.61770020117239,8.04826901317175));
#54764=CARTESIAN_POINT('Ctrl Pts',(-4.91785500921365,0.39917459312526,8.11725980081823));
#54765=CARTESIAN_POINT('Ctrl Pts',(-4.91782719367126,9.87882777886417E-6,
8.13985943599073));
#54766=CARTESIAN_POINT('Ctrl Pts',(-4.91783496857819,-2.75488291934939E-5,
6.73514056400926));
#54767=CARTESIAN_POINT('Ctrl Pts',(-4.91790898066783,-0.380171218459799,
6.75666337586538));
#54768=CARTESIAN_POINT('Ctrl Pts',(-4.78058891259536,-1.5796395597185,6.82457734019548));
#54769=CARTESIAN_POINT('Ctrl Pts',(-3.81582045786105,-3.42525704588953,
6.93888245699957));
#54770=CARTESIAN_POINT('Ctrl Pts',(-1.70805413921296,-4.83481361115031,
7.07805591442152));
#54771=CARTESIAN_POINT('Ctrl Pts',(0.817391276888771,-5.06208880774656,
7.21722937184347));
#54772=CARTESIAN_POINT('Ctrl Pts',(3.1429558795201,-4.05150588503051,7.35640282926542));
#54773=CARTESIAN_POINT('Ctrl Pts',(4.69995762166771,-2.05018778446619,7.49557628668737));
#54774=CARTESIAN_POINT('Ctrl Pts',(5.10765501073841,0.452473080222043,7.63474974410933));
#54775=CARTESIAN_POINT('Ctrl Pts',(4.26635174695346,2.84448841943749,7.77392320153127));
#54776=CARTESIAN_POINT('Ctrl Pts',(2.3817759625982,4.5409266522414,7.91309665895324));
#54777=CARTESIAN_POINT('Ctrl Pts',(-0.085227516263993,5.12694917738788,
8.05227011637518));
#54778=CARTESIAN_POINT('Ctrl Pts',(-2.53138988051854,4.45925294975012,8.19144357379713));
#54779=CARTESIAN_POINT('Ctrl Pts',(-4.35853870396961,2.70111309704827,8.33061703121909));
#54780=CARTESIAN_POINT('Ctrl Pts',(-4.89408458761665,0.999753759990778,
8.42851602795646));
#54781=CARTESIAN_POINT('Ctrl Pts',(-4.91862044827915,0.0904221571445439,
8.48002387221985));
#54782=CARTESIAN_POINT('Ctrl Pts',(-4.91854624166208,8.68734550606501E-5,
8.48514056400926));
#54783=CARTESIAN_POINT('Origin',(0.,0.,-3.23514056400933));
#54784=CARTESIAN_POINT('',(-4.91799513380959,0.000106232428033744,4.63985943599073));
#54785=CARTESIAN_POINT('',(-4.9186575077129,-3.3023661052678E-5,4.98514056400926));
#54786=CARTESIAN_POINT('',(-4.91825,1.47989506776076E-12,-3.23514056400933));
#54787=CARTESIAN_POINT('Ctrl Pts',(-4.91799513380959,0.000106232428033724,
4.63985943599073));
#54788=CARTESIAN_POINT('Ctrl Pts',(-4.91757083151256,-0.541713384096372,
4.67053880810928));
#54789=CARTESIAN_POINT('Ctrl Pts',(-4.69328057951372,-1.90317651775494,
4.74760933270181));
#54790=CARTESIAN_POINT('Ctrl Pts',(-3.46000163130249,-3.78434409590636,
4.87107100976833));
#54791=CARTESIAN_POINT('Ctrl Pts',(-1.22368347336451,-4.9795050237801,5.01024446719028));
#54792=CARTESIAN_POINT('Ctrl Pts',(1.31186817898678,-4.95700246175034,5.14941792461223));
#54793=CARTESIAN_POINT('Ctrl Pts',(3.52662208588147,-3.72233907485736,5.28859138203419));
#54794=CARTESIAN_POINT('Ctrl Pts',(4.87899329888229,-1.57743333117398,5.42776483945614));
#54795=CARTESIAN_POINT('Ctrl Pts',(5.03827966124805,0.953210144664441,5.56693829687808));
#54796=CARTESIAN_POINT('Ctrl Pts',(3.96553007503505,3.25076033395718,5.70611175430005));
#54797=CARTESIAN_POINT('Ctrl Pts',(1.92306940962342,4.75338569554455,5.84528521172199));
#54798=CARTESIAN_POINT('Ctrl Pts',(-0.589649122276164,5.09364166755337,
5.98445866914395));
#54799=CARTESIAN_POINT('Ctrl Pts',(-2.9581777789531,4.18832374022651,6.1236321265659));
#54800=CARTESIAN_POINT('Ctrl Pts',(-4.55557356052274,2.31482287380865,6.25876571551483));
#54801=CARTESIAN_POINT('Ctrl Pts',(-4.91806427523321,0.747621696728937,
6.34750815198977));
#54802=CARTESIAN_POINT('Ctrl Pts',(-4.91859079181753,-7.13374654238812E-5,
6.38985943599073));
#54803=CARTESIAN_POINT('Ctrl Pts',(-4.9186575077129,-3.30236610529425E-5,
4.98514056400926));
#54804=CARTESIAN_POINT('Ctrl Pts',(-4.91866884723753,-0.0313008852961278,
4.98691172703692));
#54805=CARTESIAN_POINT('Ctrl Pts',(-4.91073115346834,-0.881545817767002,
5.03507404253856));
#54806=CARTESIAN_POINT('Ctrl Pts',(-4.45302342878565,-2.54233238183619,
5.12962751051419));
#54807=CARTESIAN_POINT('Ctrl Pts',(-2.69040213352721,-4.36515841143928,
5.26880096793613));
#54808=CARTESIAN_POINT('Ctrl Pts',(-0.269883228865836,-5.12055022822975,
5.40797442535809));
#54809=CARTESIAN_POINT('Ctrl Pts',(2.21663158357308,-4.62378805956254,5.54714788278004));
#54810=CARTESIAN_POINT('Ctrl Pts',(4.16110228982188,-2.99634766518939,5.686321340202));
#54811=CARTESIAN_POINT('Ctrl Pts',(5.08803765633847,-0.636195256763649,
5.82549479762394));
#54812=CARTESIAN_POINT('Ctrl Pts',(4.77076950065945,1.87952918802142,5.9646682550459));
#54813=CARTESIAN_POINT('Ctrl Pts',(3.28688100581895,3.93564287640957,6.10384171246786));
#54814=CARTESIAN_POINT('Ctrl Pts',(0.999234913118859,5.02935395308892,6.2430151698898));
#54815=CARTESIAN_POINT('Ctrl Pts',(-1.53275913499672,4.89321172964454,6.38218862731175));
#54816=CARTESIAN_POINT('Ctrl Pts',(-3.68993985757321,3.56050775094501,6.52136208473371));
#54817=CARTESIAN_POINT('Ctrl Pts',(-4.75073997281743,1.69788071323429,6.63901273029954));
#54818=CARTESIAN_POINT('Ctrl Pts',(-4.91774945197063,0.439206057044297,
6.71027222339139));
#54819=CARTESIAN_POINT('Ctrl Pts',(-4.91783496857819,-2.75488291934939E-5,
6.73514056400926));
#54820=CARTESIAN_POINT('Origin',(0.,0.,-3.23514056400933));
#54821=CARTESIAN_POINT('',(-4.91823729647676,-0.000128872636838075,2.88985943599072));
#54822=CARTESIAN_POINT('',(-4.91791055468647,8.03577796647248E-5,3.23514056400926));
#54823=CARTESIAN_POINT('',(-4.91825,1.47989506776076E-12,-3.23514056400933));
#54824=CARTESIAN_POINT('Ctrl Pts',(-4.91823729647676,-0.000128872636838643,
2.88985943599072));
#54825=CARTESIAN_POINT('Ctrl Pts',(-4.91843583389124,-0.193092987687688,
2.90078715928082));
#54826=CARTESIAN_POINT('Ctrl Pts',(-4.86000879587966,-1.20512267208922,
2.95810603504489));
#54827=CARTESIAN_POINT('Ctrl Pts',(-4.18104701653603,-2.96845369999834,
3.06181606328295));
#54828=CARTESIAN_POINT('Ctrl Pts',(-2.24750313966228,-4.60886115685302,
3.2009895207049));
#54829=CARTESIAN_POINT('Ctrl Pts',(0.235634020762259,-5.12224053832399,
3.34016297812685));
#54830=CARTESIAN_POINT('Ctrl Pts',(2.66115040510108,-4.38305259454633,3.47933643554881));
#54831=CARTESIAN_POINT('Ctrl Pts',(4.43592225278534,-2.57205468293112,3.61850989297076));
#54832=CARTESIAN_POINT('Ctrl Pts',(5.12595564846396,-0.132099261254929,
3.75768335039271));
#54833=CARTESIAN_POINT('Ctrl Pts',(4.56251324399756,2.34015905938081,3.89685680781466));
#54834=CARTESIAN_POINT('Ctrl Pts',(2.88337645366723,4.24016647683272,4.03603026523662));
#54835=CARTESIAN_POINT('Ctrl Pts',(0.499153069686797,5.10330458995647,4.17520372265857));
#54836=CARTESIAN_POINT('Ctrl Pts',(-2.00713073313589,4.71850588056565,4.31437718008052));
#54837=CARTESIAN_POINT('Ctrl Pts',(-4.02260072986122,3.17986711875809,4.45355063750247));
#54838=CARTESIAN_POINT('Ctrl Pts',(-4.82695337161777,1.37422822879704,4.56204472280588));
#54839=CARTESIAN_POINT('Ctrl Pts',(-4.91821243110203,0.277587491633778,
4.62414765563529));
#54840=CARTESIAN_POINT('Ctrl Pts',(-4.91799513380959,0.000106232428033724,
4.63985943599073));
#54841=CARTESIAN_POINT('Ctrl Pts',(-4.91791055468647,8.03577796646554E-5,
3.23514056400926));
#54842=CARTESIAN_POINT('Ctrl Pts',(-4.91762009358936,-0.501697021057008,
3.26355123068244));
#54843=CARTESIAN_POINT('Ctrl Pts',(-4.71657087607217,-1.8230431477797,3.33835304982961));
#54844=CARTESIAN_POINT('Ctrl Pts',(-3.55143600647059,-3.69867190880361,
3.45954602145075));
#54845=CARTESIAN_POINT('Ctrl Pts',(-1.34498830969541,-4.94811863679935,
3.59871947887272));
#54846=CARTESIAN_POINT('Ctrl Pts',(1.19035616522235,-4.98757694646994,3.73789293629466));
#54847=CARTESIAN_POINT('Ctrl Pts',(3.43461684055513,-3.80739789825333,3.87706639371662));
#54848=CARTESIAN_POINT('Ctrl Pts',(4.83899332888966,-1.69617662995569,4.01623985113857));
#54849=CARTESIAN_POINT('Ctrl Pts',(5.06006636109004,0.829819268522708,4.15541330856052));
#54850=CARTESIAN_POINT('Ctrl Pts',(4.04377583306429,3.15289527402549,4.29458676598247));
#54851=CARTESIAN_POINT('Ctrl Pts',(2.03864039580317,4.7049778887521,4.43376022340442));
#54852=CARTESIAN_POINT('Ctrl Pts',(-0.4650140643643,5.1065285191596,4.57293368082638));
#54853=CARTESIAN_POINT('Ctrl Pts',(-2.85495628892523,4.25935396338143,4.71210713824833));
#54854=CARTESIAN_POINT('Ctrl Pts',(-4.52523122535563,2.3946547077534,4.84950943264262));
#54855=CARTESIAN_POINT('Ctrl Pts',(-4.91837183696364,0.787681960436565,
4.94052057456294));
#54856=CARTESIAN_POINT('Ctrl Pts',(-4.9186575077129,-3.30236610529425E-5,
4.98514056400926));
#54857=CARTESIAN_POINT('Origin',(0.,0.,-3.23514056400933));
#54858=CARTESIAN_POINT('',(-4.91835559909507,0.00012341875379533,1.13985943599073));
#54859=CARTESIAN_POINT('',(-4.91836475234218,-0.000121599733085009,1.48514056400926));
#54860=CARTESIAN_POINT('',(-4.91825,1.47989506776076E-12,-3.23514056400933));
#54861=CARTESIAN_POINT('Ctrl Pts',(-4.91835559909507,0.00012341875379537,
1.13985943599073));
#54862=CARTESIAN_POINT('Ctrl Pts',(-4.917672964651,-0.663200925352557,1.17742666292634));
#54863=CARTESIAN_POINT('Ctrl Pts',(-4.6156960583571,-2.14625832956755,1.26138504233594));
#54864=CARTESIAN_POINT('Ctrl Pts',(-3.16997967797153,-4.03039635294118,
1.39173457421952));
#54865=CARTESIAN_POINT('Ctrl Pts',(-0.85122519685208,-5.05650975620884,
1.53090803164147));
#54866=CARTESIAN_POINT('Ctrl Pts',(1.67568359580848,-4.84612774610485,1.67008148906343));
#54867=CARTESIAN_POINT('Ctrl Pts',(3.79282906492235,-3.45069846869191,1.80925494648538));
#54868=CARTESIAN_POINT('Ctrl Pts',(4.98249488295983,-1.21145207040314,1.94842840390733));
#54869=CARTESIAN_POINT('Ctrl Pts',(4.95376609667662,1.32403660424732,2.08760186132928));
#54870=CARTESIAN_POINT('Ctrl Pts',(3.71366788460521,3.5357520353937,2.22677531875123));
#54871=CARTESIAN_POINT('Ctrl Pts',(1.56544772852549,4.88285212444658,2.36594877617319));
#54872=CARTESIAN_POINT('Ctrl Pts',(-0.965579261288932,5.03592377327551,
2.50512223359514));
#54873=CARTESIAN_POINT('Ctrl Pts',(-3.26048828129931,3.9575355560864,2.6442956910171));
#54874=CARTESIAN_POINT('Ctrl Pts',(-4.64050357659391,2.07205186532311,2.77254142514895));
#54875=CARTESIAN_POINT('Ctrl Pts',(-4.91759298865968,0.62609207453369,2.85439600680683));
#54876=CARTESIAN_POINT('Ctrl Pts',(-4.91823729647676,-0.000128872636838643,
2.88985943599072));
#54877=CARTESIAN_POINT('Ctrl Pts',(-4.91836475234218,-0.000121599733084975,
1.48514056400926));
#54878=CARTESIAN_POINT('Ctrl Pts',(-4.91852158624276,-0.153013008821408,
1.49379958185398));
#54879=CARTESIAN_POINT('Ctrl Pts',(-4.87409834135891,-1.12493756164979,
1.54884975217269));
#54880=CARTESIAN_POINT('Ctrl Pts',(-4.25233049755791,-2.86540695615602,
1.65029107496538));
#54881=CARTESIAN_POINT('Ctrl Pts',(-2.35944592257799,-4.55256921648261,
1.78946453238733));
#54882=CARTESIAN_POINT('Ctrl Pts',(0.110405866233583,-5.12646878239007,
1.92863798980928));
#54883=CARTESIAN_POINT('Ctrl Pts',(2.55325955316838,-4.44676705445871,2.06781144723124));
#54884=CARTESIAN_POINT('Ctrl Pts',(4.37175179702231,-2.67967494785925,2.20698490465319));
#54885=CARTESIAN_POINT('Ctrl Pts',(5.12119751466329,-0.257308400894945,
2.34615836207514));
#54886=CARTESIAN_POINT('Ctrl Pts',(4.61833096239999,2.22797906576163,2.48533181949709));
#54887=CARTESIAN_POINT('Ctrl Pts',(2.98612063605357,4.1684475701488,2.62450527691905));
#54888=CARTESIAN_POINT('Ctrl Pts',(0.623699162634292,5.08958455582901,2.763678734341));
#54889=CARTESIAN_POINT('Ctrl Pts',(-1.8912386141611,4.76613974843824,2.90285219176295));
#54890=CARTESIAN_POINT('Ctrl Pts',(-3.94370226951601,3.27720673842359,3.04202564918491));
#54891=CARTESIAN_POINT('Ctrl Pts',(-4.80967135409758,1.45442541578736,3.15278843993367));
#54892=CARTESIAN_POINT('Ctrl Pts',(-4.91809438112364,0.317644219941786,
3.21716007820846));
#54893=CARTESIAN_POINT('Ctrl Pts',(-4.91791055468647,8.03577796646554E-5,
3.23514056400926));
#54894=CARTESIAN_POINT('Origin',(2.3094010767585,4.,91.));
#54895=CARTESIAN_POINT('',(2.3094010767585,4.,91.));
#54896=CARTESIAN_POINT('',(4.61880215351701,0.,91.));
#54897=CARTESIAN_POINT('',(2.88675134594813,3.,91.));
#54898=CARTESIAN_POINT('',(2.3094010767585,4.,86.));
#54899=CARTESIAN_POINT('',(2.3094010767585,4.,91.));
#54900=CARTESIAN_POINT('',(4.61880215351701,0.,86.));
#54901=CARTESIAN_POINT('',(4.61880215351701,0.,86.));
#54902=CARTESIAN_POINT('',(4.61880215351701,0.,91.));
#54903=CARTESIAN_POINT('Origin',(-2.3094010767585,4.,91.));
#54904=CARTESIAN_POINT('',(-2.3094010767585,4.,91.));
#54905=CARTESIAN_POINT('',(-1.15470053837925,4.,91.));
#54906=CARTESIAN_POINT('',(-2.3094010767585,4.,86.));
#54907=CARTESIAN_POINT('',(-2.3094010767585,4.,91.));
#54908=CARTESIAN_POINT('',(2.3094010767585,4.,86.));
#54909=CARTESIAN_POINT('Origin',(-4.61880215351701,5.55111512312578E-16,
91.));
#54910=CARTESIAN_POINT('',(-4.61880215351701,5.6564012731995E-16,91.));
#54911=CARTESIAN_POINT('',(-4.04145188432738,1.,91.));
#54912=CARTESIAN_POINT('',(-4.61880215351701,5.55111512312578E-16,86.));
#54913=CARTESIAN_POINT('',(-4.61880215351701,5.6564012731995E-16,91.));
#54914=CARTESIAN_POINT('',(-2.3094010767585,4.,86.));
#54915=CARTESIAN_POINT('Origin',(-2.30940107675851,-4.,91.));
#54916=CARTESIAN_POINT('',(-2.30940107675851,-4.,91.));
#54917=CARTESIAN_POINT('',(-2.88675134594813,-3.,91.));
#54918=CARTESIAN_POINT('',(-2.30940107675851,-4.,86.));
#54919=CARTESIAN_POINT('',(-2.30940107675851,-4.,91.));
#54920=CARTESIAN_POINT('',(-4.61880215351701,5.6564012731995E-16,86.));
#54921=CARTESIAN_POINT('Origin',(2.3094010767585,-4.,91.));
#54922=CARTESIAN_POINT('',(2.3094010767585,-4.,91.));
#54923=CARTESIAN_POINT('',(1.15470053837925,-4.,91.));
#54924=CARTESIAN_POINT('',(2.3094010767585,-4.,86.));
#54925=CARTESIAN_POINT('',(2.3094010767585,-4.,91.));
#54926=CARTESIAN_POINT('',(-2.30940107675851,-4.,86.));
#54927=CARTESIAN_POINT('Origin',(4.61880215351701,0.,91.));
#54928=CARTESIAN_POINT('',(4.04145188432738,-1.,91.));
#54929=CARTESIAN_POINT('',(2.3094010767585,-4.,86.));
#54930=CARTESIAN_POINT('Origin',(0.,0.,86.));
#54931=CARTESIAN_POINT('Origin',(0.,0.,66.5));
#54932=CARTESIAN_POINT('',(-5.,-6.12323399573677E-16,66.));
#54933=CARTESIAN_POINT('Origin',(0.,0.,66.));
#54934=CARTESIAN_POINT('',(-5.,-6.12323399573677E-16,67.));
#54935=CARTESIAN_POINT('',(-5.,-6.12323399573677E-16,66.5));
#54936=CARTESIAN_POINT('Origin',(0.,0.,67.));
#54937=CARTESIAN_POINT('Origin',(9.,0.,66.));
#54938=CARTESIAN_POINT('Origin',(5.,0.,67.));
#54939=CARTESIAN_POINT('',(-5.91675,-7.2459289488551E-16,67.));
#54940=CARTESIAN_POINT('Origin',(0.,0.,67.));
#54941=CARTESIAN_POINT('Origin',(0.,0.,0.));
#54942=CARTESIAN_POINT('',(-5.91675,7.2459289488551E-16,79.));
#54943=CARTESIAN_POINT('Origin',(0.,0.,79.));
#54944=CARTESIAN_POINT('',(-5.91675,-7.2459289488551E-16,0.));
#54945=CARTESIAN_POINT('Origin',(7.01450167938425E-16,2.84304068604708E-16,
64.));
#54946=CARTESIAN_POINT('Ctrl Pts',(-4.31134524531358,2.36723698448015,64.));
#54947=CARTESIAN_POINT('Ctrl Pts',(-4.37780531290395,2.27027384935843,64.));
#54948=CARTESIAN_POINT('Ctrl Pts',(-4.44067228193355,2.17102449251108,64.));
#54949=CARTESIAN_POINT('Ctrl Pts',(-4.49981011185718,2.0696792768666,64.));
#54950=CARTESIAN_POINT('Ctrl Pts',(-4.57274167435655,1.94469557458442,64.));
#54951=CARTESIAN_POINT('Ctrl Pts',(-4.64000323337925,1.81652518433702,64.));
#54952=CARTESIAN_POINT('Ctrl Pts',(-4.70155965673999,1.68560383988636,64.));
#54953=CARTESIAN_POINT('Ctrl Pts',(-4.7408839899757,1.60196683994773,64.));
#54954=CARTESIAN_POINT('Ctrl Pts',(-4.77787928239261,1.51720632798493,64.));
#54955=CARTESIAN_POINT('Ctrl Pts',(-4.81252800330284,1.4314287333935,64.));
#54956=CARTESIAN_POINT('Ctrl Pts',(-4.83227826388887,1.38253429223898,64.));
#54957=CARTESIAN_POINT('Ctrl Pts',(-4.85126596242407,1.33330929126607,64.));
#54958=CARTESIAN_POINT('Ctrl Pts',(-4.86948683348219,1.28377278855725,64.));
#54959=CARTESIAN_POINT('Ctrl Pts',(-4.87821226202323,1.26005124345768,64.));
#54960=CARTESIAN_POINT('Ctrl Pts',(-4.88676183322489,1.23625825950357,64.));
#54961=CARTESIAN_POINT('Ctrl Pts',(-4.89513501616439,1.2123958965766,64.));
#54962=CARTESIAN_POINT('Ctrl Pts',(-4.90245405282655,1.19153769840151,64.));
#54963=CARTESIAN_POINT('Ctrl Pts',(-4.90963706645259,1.17062994477078,64.));
#54964=CARTESIAN_POINT('Ctrl Pts',(-4.91668120130263,1.1496821616254,64.));
#54965=CARTESIAN_POINT('Ctrl Pts',(-4.96416649792232,1.00847082519322,64.));
#54966=CARTESIAN_POINT('Ctrl Pts',(-5.00538204512764,0.865335696509366,
64.));
#54967=CARTESIAN_POINT('Ctrl Pts',(-5.04029027971585,0.720733498032987,
64.));
#54968=CARTESIAN_POINT('Ctrl Pts',(-5.07541418696244,0.575237907469583,
64.));
#54969=CARTESIAN_POINT('Ctrl Pts',(-5.10415294561491,0.428256357527027,
64.));
#54970=CARTESIAN_POINT('Ctrl Pts',(-5.12642409992174,0.280225006492737,
64.));
#54971=CARTESIAN_POINT('Ctrl Pts',(-5.1422597967598,0.17496869309234,64.));
#54972=CARTESIAN_POINT('Ctrl Pts',(-5.15482469765586,0.069180988940228,
64.));
#54973=CARTESIAN_POINT('Ctrl Pts',(-5.16407425049376,-0.0369871404655844,
64.));
#54974=CARTESIAN_POINT('Ctrl Pts',(-5.16596772707835,-0.0587208253888005,
64.));
#54975=CARTESIAN_POINT('Ctrl Pts',(-5.16772222652803,-0.080470463857156,
64.));
#54976=CARTESIAN_POINT('Ctrl Pts',(-5.16933729871037,-0.10223477637485,
64.));
#54977=CARTESIAN_POINT('Ctrl Pts',(-5.17106601869474,-0.125530578511035,
64.));
#54978=CARTESIAN_POINT('Ctrl Pts',(-5.17263441131894,-0.148835747470043,
64.));
#54979=CARTESIAN_POINT('Ctrl Pts',(-5.17404184458105,-0.172141022243276,
64.));
#54980=CARTESIAN_POINT('Ctrl Pts',(-5.17774276994364,-0.233423560330576,
64.));
#54981=CARTESIAN_POINT('Ctrl Pts',(-5.18033204032176,-0.294723109481203,
64.));
#54982=CARTESIAN_POINT('Ctrl Pts',(-5.18180770735793,-0.356009398655015,
64.));
#54983=CARTESIAN_POINT('Ctrl Pts',(-5.18539797672768,-0.505117755359866,
64.));
#54984=CARTESIAN_POINT('Ctrl Pts',(-5.18239996117048,-0.654146301806263,
64.));
#54985=CARTESIAN_POINT('Ctrl Pts',(-5.17302423201139,-0.802695070252512,
64.));
#54986=CARTESIAN_POINT('Ctrl Pts',(-5.16350202633312,-0.953564608226403,
64.));
#54987=CARTESIAN_POINT('Ctrl Pts',(-5.14740132458846,-1.10393992393194,
64.));
#54988=CARTESIAN_POINT('Ctrl Pts',(-5.12489097487864,-1.25341711880026,
64.));
#54989=CARTESIAN_POINT('Ctrl Pts',(-5.10217125158059,-1.40428463310164,
64.));
#54990=CARTESIAN_POINT('Ctrl Pts',(-5.07292209013945,-1.55423798988641,
64.));
#54991=CARTESIAN_POINT('Ctrl Pts',(-5.03726447997022,-1.70286643658769,
64.));
#54992=CARTESIAN_POINT('Ctrl Pts',(-5.01186088094471,-1.8087540001643,64.));
#54993=CARTESIAN_POINT('Ctrl Pts',(-4.98320351689797,-1.91396921865827,
64.));
#54994=CARTESIAN_POINT('Ctrl Pts',(-4.95132011278482,-2.01836169389923,
64.));
#54995=CARTESIAN_POINT('Ctrl Pts',(-4.94086691439713,-2.05258750146991,
64.));
#54996=CARTESIAN_POINT('Ctrl Pts',(-4.93006684271935,-2.08672484833539,
64.));
#54997=CARTESIAN_POINT('Ctrl Pts',(-4.91892056737488,-2.12076835091139,
64.));
#54998=CARTESIAN_POINT('Ctrl Pts',(-4.91265900654528,-2.13989271807844,
64.));
#54999=CARTESIAN_POINT('Ctrl Pts',(-4.90629102097233,-2.15897878249012,
64.));
#55000=CARTESIAN_POINT('Ctrl Pts',(-4.89981802721649,-2.1780227675418,64.));
#55001=CARTESIAN_POINT('Ctrl Pts',(-4.84938469026562,-2.32640105295769,
64.));
#55002=CARTESIAN_POINT('Ctrl Pts',(-4.79256264059072,-2.47228090596256,
64.));
#55003=CARTESIAN_POINT('Ctrl Pts',(-4.72954803993235,-2.61523817290472,
64.));
#55004=CARTESIAN_POINT('Ctrl Pts',(-4.68330907578958,-2.72013760686169,
64.));
#55005=CARTESIAN_POINT('Ctrl Pts',(-4.63373470382308,-2.82346372059285,
64.));
#55006=CARTESIAN_POINT('Ctrl Pts',(-4.58088461958618,-2.92504945063106,
64.));
#55007=CARTESIAN_POINT('Ctrl Pts',(-4.50929622970348,-3.06265299381362,
64.));
#55008=CARTESIAN_POINT('Ctrl Pts',(-4.43169950814481,-3.19706421366866,
64.));
#55009=CARTESIAN_POINT('Ctrl Pts',(-4.34843690979793,-3.3280078311807,64.));
#55010=CARTESIAN_POINT('Ctrl Pts',(-4.26448354412519,-3.46003778967061,
64.));
#55011=CARTESIAN_POINT('Ctrl Pts',(-4.17476954614258,-3.58854300641687,
64.));
#55012=CARTESIAN_POINT('Ctrl Pts',(-4.07959689883012,-3.71322134423231,
64.));
#55013=CARTESIAN_POINT('Ctrl Pts',(-4.03277217929074,-3.77456279438319,
64.));
#55014=CARTESIAN_POINT('Ctrl Pts',(-3.98462541634808,-3.83497754023627,
64.));
#55015=CARTESIAN_POINT('Ctrl Pts',(-3.93518868011867,-3.89442711707548,
64.));
#55016=CARTESIAN_POINT('Ctrl Pts',(-3.92030576236725,-3.91232439812471,
64.));
#55017=CARTESIAN_POINT('Ctrl Pts',(-3.90530591656096,-3.93013419211438,
64.));
#55018=CARTESIAN_POINT('Ctrl Pts',(-3.89018997578744,-3.94785541510478,
64.));
#55019=CARTESIAN_POINT('Ctrl Pts',(-3.87616481471958,-3.96429785891188,
64.));
#55020=CARTESIAN_POINT('Ctrl Pts',(-3.86204436309214,-3.98065855108264,
64.));
#55021=CARTESIAN_POINT('Ctrl Pts',(-3.84783458724206,-3.99693104286356,
64.));
#55022=CARTESIAN_POINT('Ctrl Pts',(-3.74279515441396,-4.11721818358982,
64.));
#55023=CARTESIAN_POINT('Ctrl Pts',(-3.63279501364812,-4.23278568191491,
64.));
#55024=CARTESIAN_POINT('Ctrl Pts',(-3.51822087870055,-4.34336190163689,
64.));
#55025=CARTESIAN_POINT('Ctrl Pts',(-3.39739720559283,-4.45996959002389,
64.));
#55026=CARTESIAN_POINT('Ctrl Pts',(-3.2714868962383,-4.57102756026343,64.));
#55027=CARTESIAN_POINT('Ctrl Pts',(-3.14088626174176,-4.67619358286374,
64.));
#55028=CARTESIAN_POINT('Ctrl Pts',(-3.01028562724523,-4.78135960546406,
64.));
#55029=CARTESIAN_POINT('Ctrl Pts',(-2.87499408109108,-4.88063446711579,
64.));
#55030=CARTESIAN_POINT('Ctrl Pts',(-2.73535787325043,-4.97364013837371,
64.));
#55031=CARTESIAN_POINT('Ctrl Pts',(-2.63476045962855,-5.04064374814942,
64.));
#55032=CARTESIAN_POINT('Ctrl Pts',(-2.5319070344886,-5.10439284622974,64.));
#55033=CARTESIAN_POINT('Ctrl Pts',(-2.42697062082297,-5.16484032452088,
64.));
#55034=CARTESIAN_POINT('Ctrl Pts',(-2.38106093984425,-5.19128609627326,
64.));
#55035=CARTESIAN_POINT('Ctrl Pts',(-2.33475243107453,-5.21709974137731,
64.));
#55036=CARTESIAN_POINT('Ctrl Pts',(-2.28805902581717,-5.24227646698602,
64.));
#55037=CARTESIAN_POINT('Ctrl Pts',(-2.25858405339635,-5.25816914581022,
64.));
#55038=CARTESIAN_POINT('Ctrl Pts',(-2.2289557048792,-5.27380802074749,64.));
#55039=CARTESIAN_POINT('Ctrl Pts',(-2.19917742481413,-5.28919177522327,
64.));
#55040=CARTESIAN_POINT('Ctrl Pts',(-2.18038129925631,-5.2989020398875,64.));
#55041=CARTESIAN_POINT('Ctrl Pts',(-2.16152483404981,-5.30851090345271,
64.));
#55042=CARTESIAN_POINT('Ctrl Pts',(-2.14262330943649,-5.31801094329774,
64.));
#55043=CARTESIAN_POINT('Ctrl Pts',(-1.99828519502283,-5.39055629961888,
64.));
#55044=CARTESIAN_POINT('Ctrl Pts',(-1.85112559185448,-5.45686153661499,
64.));
#55045=CARTESIAN_POINT('Ctrl Pts',(-1.70160748689977,-5.51689175397447,
64.));
#55046=CARTESIAN_POINT('Ctrl Pts',(-1.54897259072225,-5.57817333587356,
64.));
#55047=CARTESIAN_POINT('Ctrl Pts',(-1.3938793092164,-5.63291598043752,64.));
#55048=CARTESIAN_POINT('Ctrl Pts',(-1.23678212836632,-5.6810439753599,64.));
#55049=CARTESIAN_POINT('Ctrl Pts',(-1.07907796720142,-5.72935792362245,
64.));
#55050=CARTESIAN_POINT('Ctrl Pts',(-0.919353717236846,-5.77100635051268,
64.));
#55051=CARTESIAN_POINT('Ctrl Pts',(-0.758040484974843,-5.80586855253193,
64.));
#55052=CARTESIAN_POINT('Ctrl Pts',(-0.597977648513776,-5.84046052531825,
64.));
#55053=CARTESIAN_POINT('Ctrl Pts',(-0.436349656242937,-5.86837132847252,
64.));
#55054=CARTESIAN_POINT('Ctrl Pts',(-0.273559922641045,-5.88943535634351,
64.));
#55055=CARTESIAN_POINT('Ctrl Pts',(-0.18886669624301,-5.90039415848576,
64.));
#55056=CARTESIAN_POINT('Ctrl Pts',(-0.10385879111916,-5.9094989197477,64.));
#55057=CARTESIAN_POINT('Ctrl Pts',(-0.018592070832216,-5.91672078920428,
64.));
#55058=CARTESIAN_POINT('Ctrl Pts',(4.63776713187094,-3.67456288307058,64.));
#55059=CARTESIAN_POINT('Ctrl Pts',(4.71578553900881,-3.55794368649718,64.));
#55060=CARTESIAN_POINT('Ctrl Pts',(4.78951444896037,-3.43867724387658,64.));
#55061=CARTESIAN_POINT('Ctrl Pts',(4.85875509456031,-3.31693895956287,64.));
#55062=CARTESIAN_POINT('Ctrl Pts',(4.94085947644668,-3.17258376906917,64.));
#55063=CARTESIAN_POINT('Ctrl Pts',(5.01665430968009,-3.02475279858741,64.));
#55064=CARTESIAN_POINT('Ctrl Pts',(5.08600617178006,-2.87388851250663,64.));
#55065=CARTESIAN_POINT('Ctrl Pts',(5.15507978373619,-2.72362951672421,64.));
#55066=CARTESIAN_POINT('Ctrl Pts',(5.21776212770692,-2.57036072742675,64.));
#55067=CARTESIAN_POINT('Ctrl Pts',(5.2738704289044,-2.41451223998073,64.));
#55068=CARTESIAN_POINT('Ctrl Pts',(5.28458676255205,-2.3847461562764,64.));
#55069=CARTESIAN_POINT('Ctrl Pts',(5.29506313174358,-2.35488596754356,64.));
#55070=CARTESIAN_POINT('Ctrl Pts',(5.30529804539234,-2.3249346767927,64.));
#55071=CARTESIAN_POINT('Ctrl Pts',(5.31418295674338,-2.29893401158895,64.));
#55072=CARTESIAN_POINT('Ctrl Pts',(5.32288630842342,-2.27286324727078,64.));
#55073=CARTESIAN_POINT('Ctrl Pts',(5.33140150285065,-2.24674211170248,64.));
#55074=CARTESIAN_POINT('Ctrl Pts',(5.38204436598286,-2.09139050995696,64.));
#55075=CARTESIAN_POINT('Ctrl Pts',(5.42608483565498,-1.93411836332475,64.));
#55076=CARTESIAN_POINT('Ctrl Pts',(5.46339533915538,-1.77535137306523,64.));
#55077=CARTESIAN_POINT('Ctrl Pts',(5.50043436992127,-1.61773957785674,64.));
#55078=CARTESIAN_POINT('Ctrl Pts',(5.53084106778903,-1.45865387817275,64.));
#55079=CARTESIAN_POINT('Ctrl Pts',(5.55443968683482,-1.29850913579728,64.));
#55080=CARTESIAN_POINT('Ctrl Pts',(5.5724596467274,-1.17622224142378,64.));
#55081=CARTESIAN_POINT('Ctrl Pts',(5.58650888091475,-1.05331771709944,64.));
#55082=CARTESIAN_POINT('Ctrl Pts',(5.59648856647768,-0.929983589607728,
64.));
#55083=CARTESIAN_POINT('Ctrl Pts',(5.59871377260605,-0.902483338763021,
64.));
#55084=CARTESIAN_POINT('Ctrl Pts',(5.60073658073746,-0.8749617478155,64.));
#55085=CARTESIAN_POINT('Ctrl Pts',(5.60255577183255,-0.847420936734302,
64.));
#55086=CARTESIAN_POINT('Ctrl Pts',(5.60426136527795,-0.821599885285683,
64.));
#55087=CARTESIAN_POINT('Ctrl Pts',(5.60578799465812,-0.795760150203196,
64.));
#55088=CARTESIAN_POINT('Ctrl Pts',(5.60713372452998,-0.769924994464162,
64.));
#55089=CARTESIAN_POINT('Ctrl Pts',(5.6107899878593,-0.699732503006053,64.));
#55090=CARTESIAN_POINT('Ctrl Pts',(5.61311362363577,-0.629538426216335,
64.));
#55091=CARTESIAN_POINT('Ctrl Pts',(5.61409507354281,-0.559376451480223,
64.));
#55092=CARTESIAN_POINT('Ctrl Pts',(5.6163226971518,-0.400127904759795,64.));
#55093=CARTESIAN_POINT('Ctrl Pts',(5.61163937877799,-0.241044294874839,
64.));
#55094=CARTESIAN_POINT('Ctrl Pts',(5.60017586715559,-0.0825479907627651,
64.));
#55095=CARTESIAN_POINT('Ctrl Pts',(5.5886705938214,0.0765257173061029,64.));
#55096=CARTESIAN_POINT('Ctrl Pts',(5.57033540063889,0.235008590310874,64.));
#55097=CARTESIAN_POINT('Ctrl Pts',(5.54525152574663,0.392461691483428,64.));
#55098=CARTESIAN_POINT('Ctrl Pts',(5.52050581985309,0.547792084031498,64.));
#55099=CARTESIAN_POINT('Ctrl Pts',(5.48919182491573,0.702120940243903,64.));
#55100=CARTESIAN_POINT('Ctrl Pts',(5.45134258839387,0.855004798823976,64.));
#55101=CARTESIAN_POINT('Ctrl Pts',(5.42448368941834,0.96349555028783,64.));
#55102=CARTESIAN_POINT('Ctrl Pts',(5.39433288585167,1.07125820303177,64.));
#55103=CARTESIAN_POINT('Ctrl Pts',(5.36088933597902,1.17812470068103,64.));
#55104=CARTESIAN_POINT('Ctrl Pts',(5.34772509504774,1.22019010127083,64.));
#55105=CARTESIAN_POINT('Ctrl Pts',(5.33405056167791,1.26211655112641,64.));
#55106=CARTESIAN_POINT('Ctrl Pts',(5.31986526294901,1.30389338831185,64.));
#55107=CARTESIAN_POINT('Ctrl Pts',(5.31288626186537,1.32444710364491,64.));
#55108=CARTESIAN_POINT('Ctrl Pts',(5.30578589639194,1.34495781344142,64.));
#55109=CARTESIAN_POINT('Ctrl Pts',(5.29856707862928,1.36541680688513,64.));
#55110=CARTESIAN_POINT('Ctrl Pts',(5.24687903771558,1.51190690054584,64.));
#55111=CARTESIAN_POINT('Ctrl Pts',(5.1890807996147,1.65586906246907,64.));
#55112=CARTESIAN_POINT('Ctrl Pts',(5.12526319108892,1.79690248233301,64.));
#55113=CARTESIAN_POINT('Ctrl Pts',(5.07803955192826,1.90126413867048,64.));
#55114=CARTESIAN_POINT('Ctrl Pts',(5.02751886787974,2.00402182099969,64.));
#55115=CARTESIAN_POINT('Ctrl Pts',(4.97372199207057,2.10500394192546,64.));
#55116=CARTESIAN_POINT('Ctrl Pts',(4.90071000480305,2.24205475047863,64.));
#55117=CARTESIAN_POINT('Ctrl Pts',(4.82166453854399,2.37583674945006,64.));
#55118=CARTESIAN_POINT('Ctrl Pts',(4.73686704330111,2.50599898911507,64.));
#55119=CARTESIAN_POINT('Ctrl Pts',(4.6526636823959,2.63524924599295,64.));
#55120=CARTESIAN_POINT('Ctrl Pts',(4.56278799724779,2.76093077356813,64.));
#55121=CARTESIAN_POINT('Ctrl Pts',(4.4674852282392,2.88265881474064,64.));
#55122=CARTESIAN_POINT('Ctrl Pts',(4.42323218722205,2.93918220912867,64.));
#55123=CARTESIAN_POINT('Ctrl Pts',(4.37780862316338,2.99485255318148,64.));
#55124=CARTESIAN_POINT('Ctrl Pts',(4.33123740110862,3.04962783433613,64.));
#55125=CARTESIAN_POINT('Ctrl Pts',(4.31630796020963,3.06718726882472,64.));
#55126=CARTESIAN_POINT('Ctrl Pts',(4.30126057146792,3.08465470260554,64.));
#55127=CARTESIAN_POINT('Ctrl Pts',(4.28609596941756,3.1020286992127,64.));
#55128=CARTESIAN_POINT('Ctrl Pts',(4.27208612364491,3.11807969825063,64.));
#55129=CARTESIAN_POINT('Ctrl Pts',(4.25798072796444,3.13404575090414,64.));
#55130=CARTESIAN_POINT('Ctrl Pts',(4.24378617175793,3.14991972152872,64.));
#55131=CARTESIAN_POINT('Ctrl Pts',(4.14263165658703,3.26304222983437,64.));
#55132=CARTESIAN_POINT('Ctrl Pts',(4.0368652620674,3.37159127598299,64.));
#55133=CARTESIAN_POINT('Ctrl Pts',(3.92677488831619,3.47526252928417,64.));
#55134=CARTESIAN_POINT('Ctrl Pts',(3.81533679383097,3.58020292077459,64.));
#55135=CARTESIAN_POINT('Ctrl Pts',(3.69946764495016,3.68014597296354,64.));
#55136=CARTESIAN_POINT('Ctrl Pts',(3.57943412821498,3.77473182718883,64.));
#55137=CARTESIAN_POINT('Ctrl Pts',(3.4594006114798,3.86931768141412,64.));
#55138=CARTESIAN_POINT('Ctrl Pts',(3.33520211173227,3.9585468624312,64.));
#55139=CARTESIAN_POINT('Ctrl Pts',(3.20708253874238,4.04200713373791,64.));
#55140=CARTESIAN_POINT('Ctrl Pts',(3.11885047720282,4.09948368960047,64.));
#55141=CARTESIAN_POINT('Ctrl Pts',(3.02875820280347,4.15422301877539,64.));
#55142=CARTESIAN_POINT('Ctrl Pts',(2.93694146408057,4.20615325321952,64.));
#55143=CARTESIAN_POINT('Ctrl Pts',(2.88917182567783,4.23317107759523,64.));
#55144=CARTESIAN_POINT('Ctrl Pts',(2.84093538421679,4.2594283266899,64.));
#55145=CARTESIAN_POINT('Ctrl Pts',(2.79225122260655,4.28491353726207,64.));
#55146=CARTESIAN_POINT('Ctrl Pts',(2.76158313515809,4.30096768383909,64.));
#55147=CARTESIAN_POINT('Ctrl Pts',(2.73073738177846,4.31671544847069,64.));
#55148=CARTESIAN_POINT('Ctrl Pts',(2.69971874557491,4.33215377415929,64.));
#55149=CARTESIAN_POINT('Ctrl Pts',(2.6819646151136,4.34099020547693,64.));
#55150=CARTESIAN_POINT('Ctrl Pts',(2.6641624621708,4.34972096085384,64.));
#55151=CARTESIAN_POINT('Ctrl Pts',(2.6463156374621,4.35834466861521,64.));
#55152=CARTESIAN_POINT('Ctrl Pts',(2.51371120616726,4.42242003675576,64.));
#55153=CARTESIAN_POINT('Ctrl Pts',(2.37859978023243,4.48061070952557,64.));
#55154=CARTESIAN_POINT('Ctrl Pts',(2.24138104291238,4.53280614111679,64.));
#55155=CARTESIAN_POINT('Ctrl Pts',(2.10421785117505,4.58498044421114,64.));
#55156=CARTESIAN_POINT('Ctrl Pts',(1.96494827442017,4.63116450492661,64.));
#55157=CARTESIAN_POINT('Ctrl Pts',(1.82395999692009,4.67119766109615,64.));
#55158=CARTESIAN_POINT('Ctrl Pts',(1.68432383228183,4.71084688928022,64.));
#55159=CARTESIAN_POINT('Ctrl Pts',(1.54300104255641,4.74446268902098,64.));
#55160=CARTESIAN_POINT('Ctrl Pts',(1.40036822577045,4.77183822748119,64.));
#55161=CARTESIAN_POINT('Ctrl Pts',(1.26083360159048,4.79861912935809,64.));
#55162=CARTESIAN_POINT('Ctrl Pts',(1.12004462305474,4.81942787543702,64.));
#55163=CARTESIAN_POINT('Ctrl Pts',(0.978363735010218,4.83402204168757,64.));
#55164=CARTESIAN_POINT('Ctrl Pts',(0.931389872203962,4.8388606926354,64.));
#55165=CARTESIAN_POINT('Ctrl Pts',(0.884318089179114,4.84301581405944,64.));
#55166=CARTESIAN_POINT('Ctrl Pts',(0.837162017642518,4.84647736182856,64.));
#55167=CARTESIAN_POINT('Ctrl Pts',(-2.14786219406452,4.42446279878228,-0.576484243785856));
#55168=CARTESIAN_POINT('Ctrl Pts',(-2.8848113557746,4.06670970753236,-0.530093091311872));
#55169=CARTESIAN_POINT('Ctrl Pts',(-4.17573600431334,2.97619823210191,-0.437310786363904));
#55170=CARTESIAN_POINT('Ctrl Pts',(-5.09111818072895,0.611045927560412,
-0.298137328941951));
#55171=CARTESIAN_POINT('Ctrl Pts',(-4.76147221760645,-1.90285915103548,
-0.15896387152));
#55172=CARTESIAN_POINT('Ctrl Pts',(-3.26751735403169,-3.9517774964877,-0.0197904140980472));
#55173=CARTESIAN_POINT('Ctrl Pts',(-0.97452041004599,-5.03418042523659,
0.119383043323905));
#55174=CARTESIAN_POINT('Ctrl Pts',(1.5567708799336,-4.88563546465558,0.258556500745857));
#55175=CARTESIAN_POINT('Ctrl Pts',(3.70738228326065,-3.54233751270576,0.39772995816781));
#55176=CARTESIAN_POINT('Ctrl Pts',(4.95140614815209,-1.33283639810976,0.536903415589762));
#55177=CARTESIAN_POINT('Ctrl Pts',(4.98463903712129,1.20260146313003,0.676076873011714));
#55178=CARTESIAN_POINT('Ctrl Pts',(3.79895229578282,3.44395520585394,0.815250330433666));
#55179=CARTESIAN_POINT('Ctrl Pts',(1.68428893605082,4.84314423609996,0.954423787855619));
#55180=CARTESIAN_POINT('Ctrl Pts',(-0.842242278542283,5.05801321348077,
1.09359724527757));
#55181=CARTESIAN_POINT('Ctrl Pts',(-3.16281564529539,4.03602149408518,1.23277070269952));
#55182=CARTESIAN_POINT('Ctrl Pts',(-4.70996979078121,2.02708066455042,1.37194416012147));
#55183=CARTESIAN_POINT('Ctrl Pts',(-5.10537123237187,-0.477552219033277,
1.51111761754343));
#55184=CARTESIAN_POINT('Ctrl Pts',(-4.25233049755791,-2.86540695615602,
1.65029107496538));
#55185=CARTESIAN_POINT('Ctrl Pts',(-2.35944592257799,-4.55256921648261,
1.78946453238733));
#55186=CARTESIAN_POINT('Ctrl Pts',(0.110405866233583,-5.12646878239007,
1.92863798980928));
#55187=CARTESIAN_POINT('Ctrl Pts',(2.55325955316838,-4.44676705445871,2.06781144723124));
#55188=CARTESIAN_POINT('Ctrl Pts',(4.37175179702231,-2.67967494785925,2.20698490465319));
#55189=CARTESIAN_POINT('Ctrl Pts',(5.12119751466329,-0.257308400894945,
2.34615836207514));
#55190=CARTESIAN_POINT('Ctrl Pts',(4.61833096239999,2.22797906576163,2.48533181949709));
#55191=CARTESIAN_POINT('Ctrl Pts',(2.98612063605357,4.1684475701488,2.62450527691905));
#55192=CARTESIAN_POINT('Ctrl Pts',(0.623699162634292,5.08958455582901,2.763678734341));
#55193=CARTESIAN_POINT('Ctrl Pts',(-1.8912386141611,4.76613974843824,2.90285219176295));
#55194=CARTESIAN_POINT('Ctrl Pts',(-3.94370226951601,3.27720673842359,3.04202564918491));
#55195=CARTESIAN_POINT('Ctrl Pts',(-5.03179250909024,0.986881828040634,
3.18119910660685));
#55196=CARTESIAN_POINT('Ctrl Pts',(-4.88943313614101,-1.54477027556571,
3.32037256402881));
#55197=CARTESIAN_POINT('Ctrl Pts',(-3.55143600647059,-3.69867190880361,
3.45954602145075));
#55198=CARTESIAN_POINT('Ctrl Pts',(-1.34498830969541,-4.94811863679935,
3.59871947887272));
#55199=CARTESIAN_POINT('Ctrl Pts',(1.19035616522235,-4.98757694646994,3.73789293629466));
#55200=CARTESIAN_POINT('Ctrl Pts',(3.43461684055513,-3.80739789825333,3.87706639371662));
#55201=CARTESIAN_POINT('Ctrl Pts',(4.83899332888966,-1.69617662995569,4.01623985113857));
#55202=CARTESIAN_POINT('Ctrl Pts',(5.06006636109004,0.829819268522708,4.15541330856052));
#55203=CARTESIAN_POINT('Ctrl Pts',(4.04377583306429,3.15289527402549,4.29458676598247));
#55204=CARTESIAN_POINT('Ctrl Pts',(2.03864039580317,4.7049778887521,4.43376022340442));
#55205=CARTESIAN_POINT('Ctrl Pts',(-0.4650140643643,5.1065285191596,4.57293368082638));
#55206=CARTESIAN_POINT('Ctrl Pts',(-2.85495628892523,4.25935396338143,4.71210713824833));
#55207=CARTESIAN_POINT('Ctrl Pts',(-4.54676164612823,2.37061809036044,4.85128059567028));
#55208=CARTESIAN_POINT('Ctrl Pts',(-5.12672443517544,-0.0978169863668739,
4.99045405309224));
#55209=CARTESIAN_POINT('Ctrl Pts',(-4.45302342878565,-2.54233238183619,
5.12962751051419));
#55210=CARTESIAN_POINT('Ctrl Pts',(-2.69040213352721,-4.36515841143928,
5.26880096793613));
#55211=CARTESIAN_POINT('Ctrl Pts',(-0.269883228865836,-5.12055022822975,
5.40797442535809));
#55212=CARTESIAN_POINT('Ctrl Pts',(2.21663158357308,-4.62378805956254,5.54714788278004));
#55213=CARTESIAN_POINT('Ctrl Pts',(4.16110228982188,-2.99634766518939,5.686321340202));
#55214=CARTESIAN_POINT('Ctrl Pts',(5.08803765633847,-0.636195256763649,
5.82549479762394));
#55215=CARTESIAN_POINT('Ctrl Pts',(4.77076950065945,1.87952918802142,5.9646682550459));
#55216=CARTESIAN_POINT('Ctrl Pts',(3.28688100581895,3.93564287640957,6.10384171246786));
#55217=CARTESIAN_POINT('Ctrl Pts',(0.999234913118859,5.02935395308892,6.2430151698898));
#55218=CARTESIAN_POINT('Ctrl Pts',(-1.53275913499672,4.89321172964454,6.38218862731175));
#55219=CARTESIAN_POINT('Ctrl Pts',(-3.68993985757321,3.56050775094501,6.52136208473371));
#55220=CARTESIAN_POINT('Ctrl Pts',(-4.94480096744728,1.35713484568753,6.66053554215565));
#55221=CARTESIAN_POINT('Ctrl Pts',(-4.99048494542848,-1.17810509144919,
6.79970899957761));
#55222=CARTESIAN_POINT('Ctrl Pts',(-3.81582045786105,-3.42525704588953,
6.93888245699957));
#55223=CARTESIAN_POINT('Ctrl Pts',(-1.70805413921296,-4.83481361115031,
7.07805591442152));
#55224=CARTESIAN_POINT('Ctrl Pts',(0.817391276888771,-5.06208880774656,
7.21722937184347));
#55225=CARTESIAN_POINT('Ctrl Pts',(3.1429558795201,-4.05150588503051,7.35640282926542));
#55226=CARTESIAN_POINT('Ctrl Pts',(4.69995762166771,-2.05018778446619,7.49557628668737));
#55227=CARTESIAN_POINT('Ctrl Pts',(5.10765501073841,0.452473080222043,7.63474974410933));
#55228=CARTESIAN_POINT('Ctrl Pts',(4.26635174695346,2.84448841943749,7.77392320153127));
#55229=CARTESIAN_POINT('Ctrl Pts',(2.3817759625982,4.5409266522414,7.91309665895324));
#55230=CARTESIAN_POINT('Ctrl Pts',(-0.085227516263993,5.12694917738788,
8.05227011637518));
#55231=CARTESIAN_POINT('Ctrl Pts',(-2.53138988051854,4.45925294975012,8.19144357379713));
#55232=CARTESIAN_POINT('Ctrl Pts',(-4.35853870396961,2.70111309704827,8.33061703121909));
#55233=CARTESIAN_POINT('Ctrl Pts',(-5.11987206507848,0.282456428986481,
8.46979048864104));
#55234=CARTESIAN_POINT('Ctrl Pts',(-4.62921727538704,-2.20527073492236,
8.60896394606299));
#55235=CARTESIAN_POINT('Ctrl Pts',(-3.00655662644843,-4.15373191828816,
8.74813740348495));
#55236=CARTESIAN_POINT('Ctrl Pts',(-0.648687514646424,-5.08646007606358,
8.88731086090689));
#55237=CARTESIAN_POINT('Ctrl Pts',(1.86780842837057,-4.77537048530841,9.02648431832885));
#55238=CARTESIAN_POINT('Ctrl Pts',(3.92755975149067,-3.29653545339913,9.1656577757508));
#55239=CARTESIAN_POINT('Ctrl Pts',(5.0268850702256,-1.01158197284738,9.30483123317275));
#55240=CARTESIAN_POINT('Ctrl Pts',(4.89696081722127,1.52073875193816,9.44400469059471));
#55241=CARTESIAN_POINT('Ctrl Pts',(3.56955802565887,3.68118555610841,9.58317814801665));
#55242=CARTESIAN_POINT('Ctrl Pts',(1.36927319819533,4.9414534810874,9.72235160543861));
#55243=CARTESIAN_POINT('Ctrl Pts',(-1.16584691373595,4.99336285190443,9.86152506286056));
#55244=CARTESIAN_POINT('Ctrl Pts',(-3.41587659702151,3.82422000818044,10.0006985202825));
#55245=CARTESIAN_POINT('Ctrl Pts',(-4.83060473962267,1.71992134895229,10.1398719777045));
#55246=CARTESIAN_POINT('Ctrl Pts',(-5.06408073015179,-0.804958356408661,
10.2790454351264));
#55247=CARTESIAN_POINT('Ctrl Pts',(-4.05921150653168,-3.13299753308037,
10.4182188925484));
#55248=CARTESIAN_POINT('Ctrl Pts',(-2.06172281055525,-4.69490901397279,
10.5573923499703));
#55249=CARTESIAN_POINT('Ctrl Pts',(0.439929367680037,-5.10875070330306,
10.6965658073923));
#55250=CARTESIAN_POINT('Ctrl Pts',(2.83400339776564,-4.27332380454602,10.8357392648142));
#55251=CARTESIAN_POINT('Ctrl Pts',(4.53506427669625,-2.39291947279475,10.9749127222362));
#55252=CARTESIAN_POINT('Ctrl Pts',(5.12714300424288,0.0726375322416105,
11.1140861796581));
#55253=CARTESIAN_POINT('Ctrl Pts',(4.46545558154636,2.52043211499204,11.2532596370801));
#55254=CARTESIAN_POINT('Ctrl Pts',(2.71180777293433,4.35189271463576,11.392433094502));
#55255=CARTESIAN_POINT('Ctrl Pts',(0.295027925902909,5.11916302924455,11.531606551924));
#55256=CARTESIAN_POINT('Ctrl Pts',(-2.19389658855195,4.63461857716327,11.6707800093459));
#55257=CARTESIAN_POINT('Ctrl Pts',(-4.14633649986933,3.01674745825668,11.8099534667679));
#55258=CARTESIAN_POINT('Ctrl Pts',(-5.08485182457936,0.661175860961971,
11.9491269241898));
#55259=CARTESIAN_POINT('Ctrl Pts',(-4.77994267460943,-1.8560764058881,12.0883003816118));
#55260=CARTESIAN_POINT('Ctrl Pts',(-3.30617002296448,-3.91945294349836,
12.2274738390338));
#55261=CARTESIAN_POINT('Ctrl Pts',(-1.02392293276547,-5.02438587538853,
12.3666472964557));
#55262=CARTESIAN_POINT('Ctrl Pts',(1.50870919886821,-4.90068037626382,12.5058207538777));
#55263=CARTESIAN_POINT('Ctrl Pts',(3.67240905719958,-3.57858677603957,12.6449942112996));
#55264=CARTESIAN_POINT('Ctrl Pts',(4.93807619790383,-1.38140329402478,12.7841676687216));
#55265=CARTESIAN_POINT('Ctrl Pts',(4.99621064854467,1.15358170599905,12.9233411261435));
#55266=CARTESIAN_POINT('Ctrl Pts',(3.83259649856215,3.40647555051493,13.0625145835655));
#55267=CARTESIAN_POINT('Ctrl Pts',(1.7317781876149,4.82636673968609,13.2016880409874));
#55268=CARTESIAN_POINT('Ctrl Pts',(-0.792520582052584,5.06604211629452,
13.3408614984094));
#55269=CARTESIAN_POINT('Ctrl Pts',(-3.12302029475477,4.06689265110314,13.4800349558313));
#55270=CARTESIAN_POINT('Ctrl Pts',(-4.68983209611028,2.07324540451455,13.6192084132533));
#55271=CARTESIAN_POINT('Ctrl Pts',(-5.10981559024654,-0.427383002376447,
13.7583818706752));
#55272=CARTESIAN_POINT('Ctrl Pts',(-4.28027009411781,-2.82350128713404,
13.8975553280972));
#55273=CARTESIAN_POINT('Ctrl Pts',(-2.40404855375509,-4.52917455484274,
14.0367287855191));
#55274=CARTESIAN_POINT('Ctrl Pts',(0.06004711021698,-5.12730591457165,14.1759022429411));
#55275=CARTESIAN_POINT('Ctrl Pts',(2.5094591513317,-4.47163128677269,14.315075700363));
#55276=CARTESIAN_POINT('Ctrl Pts',(4.34522048351284,-2.72248609669679,14.454249157785));
#55277=CARTESIAN_POINT('Ctrl Pts',(5.11842312500342,-0.307597643809348,
14.5934226152069));
#55278=CARTESIAN_POINT('Ctrl Pts',(4.63999193232155,2.18250921304762,14.7325960726289));
#55279=CARTESIAN_POINT('Ctrl Pts',(3.02692009916372,4.13891607915956,14.8717695300508));
#55280=CARTESIAN_POINT('Ctrl Pts',(0.673660220405915,5.08321291158352,15.0109429874728));
#55281=CARTESIAN_POINT('Ctrl Pts',(-1.84433319131777,4.78448604099233,15.1501164448947));
#55282=CARTESIAN_POINT('Ctrl Pts',(-3.91132250131647,3.31578465641879,15.2892899023167));
#55283=CARTESIAN_POINT('Ctrl Pts',(-5.02185638364779,1.0362577184575,15.4284633597386));
#55284=CARTESIAN_POINT('Ctrl Pts',(-4.90437038434335,-1.49667054832476,
15.5676368171606));
#55285=CARTESIAN_POINT('Ctrl Pts',(-3.587593947644,-3.66361041376876,15.7068102745826));
#55286=CARTESIAN_POINT('Ctrl Pts',(-1.39352506003175,-4.93466913826148,
15.8459837320045));
#55287=CARTESIAN_POINT('Ctrl Pts',(1.1413095421973,-4.99902831817707,15.9851571894265));
#55288=CARTESIAN_POINT('Ctrl Pts',(3.39705396305783,-3.8409498784962,16.1243306468484));
#55289=CARTESIAN_POINT('Ctrl Pts',(4.82209963689558,-1.74362458370441,16.2635041042704));
#55290=CARTESIAN_POINT('Ctrl Pts',(5.06797295434764,0.780078028819932,16.4026775616923));
#55291=CARTESIAN_POINT('Ctrl Pts',(4.07454927242783,3.11302422470575,16.5418510191143));
#55292=CARTESIAN_POINT('Ctrl Pts',(2.08475549686315,4.68472689869385,16.6810244765362));
#55293=CARTESIAN_POINT('Ctrl Pts',(-0.414834059965531,5.1108496651476,16.8201979339582));
#55294=CARTESIAN_POINT('Ctrl Pts',(-2.81298215087013,4.28719057378289,16.9593713913801));
#55295=CARTESIAN_POINT('Ctrl Pts',(-4.52325752219571,2.41516313837115,17.0985448488021));
#55296=CARTESIAN_POINT('Ctrl Pts',(-5.12743790739186,-0.0474563261099836,
17.237718306224));
#55297=CARTESIAN_POINT('Ctrl Pts',(-4.47778002818978,-2.49847105570419,
17.376891763646));
#55298=CARTESIAN_POINT('Ctrl Pts',(-2.73314800394566,-4.33852205083421,
17.5160652210679));
#55299=CARTESIAN_POINT('Ctrl Pts',(-0.320165506910762,-5.11765235681669,
17.6552386784899));
#55300=CARTESIAN_POINT('Ctrl Pts',(2.17110867707493,-4.64533730846069,17.7944121359119));
#55301=CARTESIAN_POINT('Ctrl Pts',(4.13147070090376,-3.0370744878288,17.9335855933338));
#55302=CARTESIAN_POINT('Ctrl Pts',(5.08154334695868,-0.686140517697928,
18.0727590507557));
#55303=CARTESIAN_POINT('Ctrl Pts',(4.78900055706072,1.83257885547087,18.2119325081777));
#55304=CARTESIAN_POINT('Ctrl Pts',(3.3253792957861,3.90316847397136,18.3511059655996));
#55305=CARTESIAN_POINT('Ctrl Pts',(1.04858625554496,5.01929661025616,18.4902794230216));
#55306=CARTESIAN_POINT('Ctrl Pts',(-1.4846228729006,4.90803081920919,18.6294528804436));
#55307=CARTESIAN_POINT('Ctrl Pts',(-3.6547896788716,3.5965794861591,18.7686263378655));
#55308=CARTESIAN_POINT('Ctrl Pts',(-4.93123232270488,1.40563842312223,18.9077997952874));
#55309=CARTESIAN_POINT('Ctrl Pts',(-5.00181584381112,-1.12903049633163,
19.0469732527094));
#55310=CARTESIAN_POINT('Ctrl Pts',(-3.84928009761185,-3.3876118914622,19.1861467101313));
#55311=CARTESIAN_POINT('Ctrl Pts',(-1.75546046578727,-4.8178034569817,19.3253201675533));
#55312=CARTESIAN_POINT('Ctrl Pts',(0.767630771739118,-5.06987323266825,
19.4644936249752));
#55313=CARTESIAN_POINT('Ctrl Pts',(3.10300938320942,-4.08218132433643,19.6036670823972));
#55314=CARTESIAN_POINT('Ctrl Pts',(4.67959345250773,-2.09625301819547,19.7428405398192));
#55315=CARTESIAN_POINT('Ctrl Pts',(5.11185292177081,0.402282616117053,19.8820139972411));
#55316=CARTESIAN_POINT('Ctrl Pts',(4.29408520181098,2.80244605240401,20.0211874546631));
#55317=CARTESIAN_POINT('Ctrl Pts',(2.4262631596223,4.5173132144347,20.160360912085));
#55318=CARTESIAN_POINT('Ctrl Pts',(-0.0348652558426957,5.12753898190759,
20.299534369507));
#55319=CARTESIAN_POINT('Ctrl Pts',(-2.4874678943674,4.48390176872088,20.4387078269289));
#55320=CARTESIAN_POINT('Ctrl Pts',(-4.33179745699125,2.74379343038994,20.5778812843509));
#55321=CARTESIAN_POINT('Ctrl Pts',(-5.11685072933207,0.33273143942329,20.7170547417728));
#55322=CARTESIAN_POINT('Ctrl Pts',(-4.65065467334822,-2.15969504937878,
20.8562281991948));
#55323=CARTESIAN_POINT('Ctrl Pts',(-3.04721056302127,-4.12400040999737,
20.9954016566167));
#55324=CARTESIAN_POINT('Ctrl Pts',(-0.698616677582171,-5.07984314077225,
21.1345751140387));
#55325=CARTESIAN_POINT('Ctrl Pts',(1.82081346922569,-4.79348619559222,21.2737485714606));
#55326=CARTESIAN_POINT('Ctrl Pts',(3.89499091063157,-3.33495388321102,21.4129220288826));
#55327=CARTESIAN_POINT('Ctrl Pts',(5.01670657064901,-1.06090846968716,21.5520954863046));
#55328=CARTESIAN_POINT('Ctrl Pts',(4.91166165878904,1.47256624524283,21.6912689437265));
#55329=CARTESIAN_POINT('Ctrl Pts',(3.6055433374024,3.6459469056968,21.8304424011485));
#55330=CARTESIAN_POINT('Ctrl Pts',(1.41774331025312,4.92776577195785,21.9696158585704));
#55331=CARTESIAN_POINT('Ctrl Pts',(-1.11674464244417,5.00457320863818,22.1087893159924));
#55332=CARTESIAN_POINT('Ctrl Pts',(-3.37814939266335,3.85758710567824,22.2479627734143));
#55333=CARTESIAN_POINT('Ctrl Pts',(-4.81347822585022,1.76728576249361,22.3871362308363));
#55334=CARTESIAN_POINT('Ctrl Pts',(-5.07174293979774,-0.755178885866551,
22.5263096882582));
#55335=CARTESIAN_POINT('Ctrl Pts',(-4.089788760808,-3.09297583065489,22.6654831456802));
#55336=CARTESIAN_POINT('Ctrl Pts',(-2.10773789918185,-4.67443178850642,
22.8046566031021));
#55337=CARTESIAN_POINT('Ctrl Pts',(0.389728746515864,-5.11282535406657,
22.9438300605241));
#55338=CARTESIAN_POINT('Ctrl Pts',(2.79189305526804,-4.30095393662765,23.083003517946));
#55339=CARTESIAN_POINT('Ctrl Pts',(4.51134166740374,-2.43734855057574,23.222176975368));
#55340=CARTESIAN_POINT('Ctrl Pts',(5.12760913750936,0.0222739753389076,
23.3613504327899));
#55341=CARTESIAN_POINT('Ctrl Pts',(4.48999647145208,2.47644973367009,23.5005238902119));
#55342=CARTESIAN_POINT('Ctrl Pts',(2.75442231183803,4.32504674253304,23.6396973476338));
#55343=CARTESIAN_POINT('Ctrl Pts',(0.345295365574717,5.11601824738336,23.7788708050558));
#55344=CARTESIAN_POINT('Ctrl Pts',(-2.14826839878302,4.65594399492059,23.9180442624777));
#55345=CARTESIAN_POINT('Ctrl Pts',(-4.11650525148601,3.05732826362086,24.0572177198997));
#55346=CARTESIAN_POINT('Ctrl Pts',(-5.07811230327642,0.711088624827749,
24.1963911773216));
#55347=CARTESIAN_POINT('Ctrl Pts',(-4.79794292953853,-1.80903710352717,
24.3355646347436));
#55348=CARTESIAN_POINT('Ctrl Pts',(-3.34450836095903,-3.8867898606076,24.4747380921655));
#55349=CARTESIAN_POINT('Ctrl Pts',(-1.07322428658152,-5.01408628044417,
24.6139115495875));
#55350=CARTESIAN_POINT('Ctrl Pts',(1.46050073805254,-4.91526288118904,24.7530850070094));
#55351=CARTESIAN_POINT('Ctrl Pts',(3.63708214756602,-3.61448544732211,24.8922584644314));
#55352=CARTESIAN_POINT('Ctrl Pts',(4.92426950692363,-1.42983964843226,25.0314319218533));
#55353=CARTESIAN_POINT('Ctrl Pts',(5.0073003960314,1.10445205461833,25.1706053792753));
#55354=CARTESIAN_POINT('Ctrl Pts',(3.86587085260431,3.36866652371991,25.3097788366973));
#55355=CARTESIAN_POINT('Ctrl Pts',(1.77910040251715,4.80912396958221,25.4489522941192));
#55356=CARTESIAN_POINT('Ctrl Pts',(-0.742722446286816,5.07358206446181,
25.5881257515412));
#55357=CARTESIAN_POINT('Ctrl Pts',(-3.08292362754424,4.0973715359699,25.7272992089631));
#55358=CARTESIAN_POINT('Ctrl Pts',(-4.66924193781462,2.11921007056874,25.8664726663851));
#55359=CARTESIAN_POINT('Ctrl Pts',(-5.11376695617113,-0.377172526861437,
26.005646123807));
#55360=CARTESIAN_POINT('Ctrl Pts',(-4.30779673681465,-2.7813232230965,26.144819581229));
#55361=CARTESIAN_POINT('Ctrl Pts',(-2.44841924438686,-4.50534291711108,
26.2839930386509));
#55362=CARTESIAN_POINT('Ctrl Pts',(0.00968256052368256,-5.12764837377413,
26.4231664960729));
#55363=CARTESIAN_POINT('Ctrl Pts',(2.46541664005145,-4.49606409963251,26.5623399534948));
#55364=CARTESIAN_POINT('Ctrl Pts',(4.31826994816623,-2.76503458419805,26.7015134109168));
#55365=CARTESIAN_POINT('Ctrl Pts',(5.11515491599038,-0.357857209604937,
26.8406868683387));
#55366=CARTESIAN_POINT('Ctrl Pts',(4.66120524128334,2.13682879419003,26.9798603257607));
#55367=CARTESIAN_POINT('Ctrl Pts',(3.06742752861815,4.10898527056527,27.1190337831826));
#55368=CARTESIAN_POINT('Ctrl Pts',(0.723556284229189,5.07635084490811,27.2582072406046));
#55369=CARTESIAN_POINT('Ctrl Pts',(-1.79724982938647,4.80237073202571,27.3973806980266));
#55370=CARTESIAN_POINT('Ctrl Pts',(-3.87856537335147,3.35404267141695,27.5365541554485));
#55371=CARTESIAN_POINT('Ctrl Pts',(-5.01143575544194,1.08553363196406,27.6757276128705));
#55372=CARTESIAN_POINT('Ctrl Pts',(-4.91883446469394,-1.44842642408439,
27.8149010702924));
#55373=CARTESIAN_POINT('Ctrl Pts',(-3.62340576199759,-3.62819545793354,
27.9540745277144));
#55374=CARTESIAN_POINT('Ctrl Pts',(-1.44192736471906,-4.92074354868461,
28.0932479851363));
#55375=CARTESIAN_POINT('Ctrl Pts',(1.09215280697808,-5.0099973895459,28.2324214425583));
#55376=CARTESIAN_POINT('Ctrl Pts',(3.35916334181333,-3.8741312884393,28.3715948999802));
#55377=CARTESIAN_POINT('Ctrl Pts',(4.80474071443369,-1.79090431461596,28.5107683574022));
#55378=CARTESIAN_POINT('Ctrl Pts',(5.0753905955706,0.730261528111896,28.6499418148241));
#55379=CARTESIAN_POINT('Ctrl Pts',(4.10492960409817,3.07285283449196,28.7891152722461));
#55380=CARTESIAN_POINT('Ctrl Pts',(2.1306694631793,4.66402393172698,28.928288729668));
#55381=CARTESIAN_POINT('Ctrl Pts',(-0.36461403286742,5.11467772240667,29.06746218709));
#55382=CARTESIAN_POINT('Ctrl Pts',(-2.77073661962518,4.31461356111005,29.2066356445119));
#55383=CARTESIAN_POINT('Ctrl Pts',(-4.49931699972899,2.45947517429971,29.3458091019339));
#55384=CARTESIAN_POINT('Ctrl Pts',(-5.12765669046533,0.00290891267710508,
29.4849825593558));
#55385=CARTESIAN_POINT('Ctrl Pts',(-4.50210461667452,-2.45436868004072,
29.6241560167778));
#55386=CARTESIAN_POINT('Ctrl Pts',(-2.77563018347832,-4.31146711475466,
29.7633294741997));
#55387=CARTESIAN_POINT('Ctrl Pts',(-0.370416895766376,-5.11426074035902,
29.9025029316217));
#55388=CARTESIAN_POINT('Ctrl Pts',(2.1253763045803,-4.66643838071129,30.0416763890436));
#55389=CARTESIAN_POINT('Ctrl Pts',(4.10144051258044,-3.07750829711484,30.1808498464656));
#55390=CARTESIAN_POINT('Ctrl Pts',(5.07455877628885,-0.736019580606846,
30.3200233038876));
#55391=CARTESIAN_POINT('Ctrl Pts',(4.8067695763542,1.7854517178805,30.4591967613095));
#55392=CARTESIAN_POINT('Ctrl Pts',(3.36355675709311,3.87031749845671,30.5983702187315));
#55393=CARTESIAN_POINT('Ctrl Pts',(1.09783643160968,5.00875501162488,30.7375436761534));
#55394=CARTESIAN_POINT('Ctrl Pts',(-1.43634337614621,4.92237638776717,30.8767171335754));
#55395=CARTESIAN_POINT('Ctrl Pts',(-3.61928689038582,3.63230422763955,31.0158905909973));
#55396=CARTESIAN_POINT('Ctrl Pts',(-4.91718791850219,1.45400638622494,31.1550640484193));
#55397=CARTESIAN_POINT('Ctrl Pts',(-5.0126641729189,-1.07984697368752,31.2942375058412));
#55398=CARTESIAN_POINT('Ctrl Pts',(-3.882368363373,-3.34963990424751,31.4334109632632));
#55399=CARTESIAN_POINT('Ctrl Pts',(-1.80269742761279,-4.80032848683557,
31.5725844206851));
#55400=CARTESIAN_POINT('Ctrl Pts',(0.717796206480772,-5.07716852221872,
31.7117578781071));
#55401=CARTESIAN_POINT('Ctrl Pts',(3.06276351222464,-4.1124629196179,31.850931335529));
#55402=CARTESIAN_POINT('Ctrl Pts',(4.65877780170794,-2.14211600791371,31.990104792951));
#55403=CARTESIAN_POINT('Ctrl Pts',(5.11555764728126,0.352053340261175,32.1292782503729));
#55404=CARTESIAN_POINT('Ctrl Pts',(4.32140436840864,2.760133308691,32.2684517077949));
#55405=CARTESIAN_POINT('Ctrl Pts',(2.47051627364734,4.49326395159359,32.4076251652168));
#55406=CARTESIAN_POINT('Ctrl Pts',(0.0155003683372346,5.12763408753279,
32.5467986226388));
#55407=CARTESIAN_POINT('Ctrl Pts',(-2.44330592025679,4.50811798615397,32.6859720800608));
#55408=CARTESIAN_POINT('Ctrl Pts',(-4.30463828331925,2.78620904578768,32.8251455374827));
#55409=CARTESIAN_POINT('Ctrl Pts',(-5.11333572588113,0.382974348324482,
32.9643189949047));
#55410=CARTESIAN_POINT('Ctrl Pts',(-4.67164338164879,-2.113910999012,33.1034924523266));
#55411=CARTESIAN_POINT('Ctrl Pts',(-3.0875705083242,-4.0938710230262,33.2426659097486));
#55412=CARTESIAN_POINT('Ctrl Pts',(-0.748478438807404,-5.07273610822475,
33.3818393671704));
#55413=CARTESIAN_POINT('Ctrl Pts',(1.77364284015155,-4.81113943599913,33.5210128245925));
#55414=CARTESIAN_POINT('Ctrl Pts',(3.86204628565767,-3.37305056061788,33.6601862820144));
#55415=CARTESIAN_POINT('Ctrl Pts',(5.00604406515782,-1.11013261133297,33.7993597394364));
#55416=CARTESIAN_POINT('Ctrl Pts',(4.92588862905106,1.42425166709831,33.9385331968583));
#55417=CARTESIAN_POINT('Ctrl Pts',(3.64118079059058,3.61035649864124,34.0777066542803));
#55418=CARTESIAN_POINT('Ctrl Pts',(1.4660766401138,4.91360263781672,34.2168801117022));
#55419=CARTESIAN_POINT('Ctrl Pts',(-1.06753462895041,5.01530073006979,34.3560535691242));
#55420=CARTESIAN_POINT('Ctrl Pts',(-3.34009626844846,3.89058202773615,34.4952270265461));
#55421=CARTESIAN_POINT('Ctrl Pts',(-4.79588731339343,1.81447967039556,34.6344004839681));
#55422=CARTESIAN_POINT('Ctrl Pts',(-5.07891583368533,-0.705326556558901,
34.7735739413899));
#55423=CARTESIAN_POINT('Ctrl Pts',(-4.11997143710345,-3.05265572158056,
34.912747398812));
#55424=CARTESIAN_POINT('Ctrl Pts',(-2.15354963574969,-4.65350357939147,
35.0519208562339));
#55425=CARTESIAN_POINT('Ctrl Pts',(0.339490524783248,-5.11640672548902,
35.1910943136559));
#55426=CARTESIAN_POINT('Ctrl Pts',(2.74951335423154,-4.32816911776206,35.3302677710778));
#55427=CARTESIAN_POINT('Ctrl Pts',(4.48718380920458,-2.4815424758523,35.4694412284998));
#55428=CARTESIAN_POINT('Ctrl Pts',(5.12758056511281,-0.0280917305306554,
35.6086146859217));
#55429=CARTESIAN_POINT('Ctrl Pts',(4.51410417181047,2.43222842740771,35.7477881433437));
#55430=CARTESIAN_POINT('Ctrl Pts',(2.79677110733593,4.29778349503762,35.8869616007656));
#55431=CARTESIAN_POINT('Ctrl Pts',(0.395529491558261,5.1123798781345,36.0261350581876));
#55432=CARTESIAN_POINT('Ctrl Pts',(-2.10243294662056,4.67682021270983,36.1653085156095));
#55433=CARTESIAN_POINT('Ctrl Pts',(-4.08627684754628,3.09761410157141,36.3044819730315));
#55434=CARTESIAN_POINT('Ctrl Pts',(-5.07088285170647,0.760932783704383,
36.4436554304534));
#55435=CARTESIAN_POINT('Ctrl Pts',(-4.81548028461036,-1.76182326740675,
36.5828288878754));
#55436=CARTESIAN_POINT('Ctrl Pts',(-3.38252402474393,-3.85375178482954,
36.7220023452973));
#55437=CARTESIAN_POINT('Ctrl Pts',(-1.12242209698828,-5.0033029323877,36.8611758027193));
#55438=CARTESIAN_POINT('Ctrl Pts',(1.41215136985344,-4.92937116736687,37.0003492601412));
#55439=CARTESIAN_POINT('Ctrl Pts',(3.60140433654983,-3.6500353973252,37.1395227175632));
#55440=CARTESIAN_POINT('Ctrl Pts',(4.90998772824735,-1.47813805360231,37.2786961749851));
#55441=CARTESIAN_POINT('Ctrl Pts',(5.01790704510018,1.05521584700991,37.4178696324071));
#55442=CARTESIAN_POINT('Ctrl Pts',(3.89877223200052,3.33053249196408,37.5570430898291));
#55443=CARTESIAN_POINT('Ctrl Pts',(1.82625097191763,4.79141722088745,37.696216547251));
#55444=CARTESIAN_POINT('Ctrl Pts',(-0.692852653537991,5.08063251943419,
37.835390004673));
#55445=CARTESIAN_POINT('Ctrl Pts',(-3.04252952350951,4.12745511127861,37.9745634620949));
#55446=CARTESIAN_POINT('Ctrl Pts',(-4.64820129658106,2.16497027774265,38.1137369195169));
#55447=CARTESIAN_POINT('Ctrl Pts',(-5.11722495190999,-0.326925662187272,
38.2529103769388));
#55448=CARTESIAN_POINT('Ctrl Pts',(-4.33490776837895,-2.73887682028504,
38.3920838343608));
#55449=CARTESIAN_POINT('Ctrl Pts',(-2.4925537144267,-4.48107660922512,38.5312572917828));
#55450=CARTESIAN_POINT('Ctrl Pts',(-0.0406829233315988,-5.12749612352813,
38.6704307492046));
#55451=CARTESIAN_POINT('Ctrl Pts',(2.42113626829065,-4.52006313754736,38.8096042066267));
#55452=CARTESIAN_POINT('Ctrl Pts',(4.29090279124404,-2.80731630443399,38.9487776640485));
#55453=CARTESIAN_POINT('Ctrl Pts',(5.11139320288289,-0.408082249760327,
39.0879511214706));
#55454=CARTESIAN_POINT('Ctrl Pts',(4.6819688426782,2.09094221661848,39.2271245788925));
#55455=CARTESIAN_POINT('Ctrl Pts',(3.10763901629375,4.0786580319335,39.3662980363144));
#55456=CARTESIAN_POINT('Ctrl Pts',(0.773382540198208,5.06899901790909,39.5054714937364));
#55457=CARTESIAN_POINT('Ctrl Pts',(-1.74999307091798,4.81979209601264,39.6446449511584));
#55458=CARTESIAN_POINT('Ctrl Pts',(-3.84543404598807,3.39197709234639,39.7838184085803));
#55459=CARTESIAN_POINT('Ctrl Pts',(-5.00053162984347,1.13470481447017,39.9229918660022));
#55460=CARTESIAN_POINT('Ctrl Pts',(-4.93282398171498,-1.40004255737619,
40.0621653234243));
#55461=CARTESIAN_POINT('Ctrl Pts',(-3.65886799445027,-3.59243045809301,
40.2013387808461));
#55462=CARTESIAN_POINT('Ctrl Pts',(-1.49019055396033,-4.90634321159193,
40.3405122382681));
#55463=CARTESIAN_POINT('Ctrl Pts',(1.04289070214805,-5.02048310229404,40.4796856956901));
#55464=CARTESIAN_POINT('Ctrl Pts',(3.32094863246379,-3.90693892677934,40.618859153112));
#55465=CARTESIAN_POINT('Ctrl Pts',(4.7869182362722,-1.83801126119823,40.758032610534));
#55466=CARTESIAN_POINT('Ctrl Pts',(5.0823185691137,0.680374572635465,40.8972060679559));
#55467=CARTESIAN_POINT('Ctrl Pts',(4.13491389701701,3.03238497907216,41.0363795253779));
#55468=CARTESIAN_POINT('Ctrl Pts',(2.17637786502656,4.64287098524924,41.1755529827997));
#55469=CARTESIAN_POINT('Ctrl Pts',(-0.314358828238725,5.11801232161034,
41.3147264402218));
#55470=CARTESIAN_POINT('Ctrl Pts',(-2.72822377098922,4.34162027962559,41.4538998976437));
#55471=CARTESIAN_POINT('Ctrl Pts',(-4.47494238848132,2.50354992297337,41.5930733550657));
#55472=CARTESIAN_POINT('Ctrl Pts',(-5.12738076328793,0.0532738708158156,
41.7322468124876));
#55473=CARTESIAN_POINT('Ctrl Pts',(-4.5259948474324,-2.41002950979075,41.8714202699096));
#55474=CARTESIAN_POINT('Ctrl Pts',(-2.81784457349484,-4.28399621342882,
42.0105937273315));
#55475=CARTESIAN_POINT('Ctrl Pts',(-0.420632547238203,-5.1103757060759,
42.1497671847535));
#55476=CARTESIAN_POINT('Ctrl Pts',(2.07943887829429,-4.68708924050791,42.2889406421754));
#55477=CARTESIAN_POINT('Ctrl Pts',(4.07101462212891,-3.11764519204149,42.4281140995974));
#55478=CARTESIAN_POINT('Ctrl Pts',(5.06708461819206,-0.785827633217498,
42.5672875570193));
#55479=CARTESIAN_POINT('Ctrl Pts',(4.82407484420597,1.73815232202072,42.7064610144413));
#55480=CARTESIAN_POINT('Ctrl Pts',(3.40140970642374,3.83709311928876,42.8456344718632));
#55481=CARTESIAN_POINT('Ctrl Pts',(1.14698068971451,4.99773017423599,42.9848079292852));
#55482=CARTESIAN_POINT('Ctrl Pts',(-1.38792530268207,4.93624705127506,43.1239813867072));
#55483=CARTESIAN_POINT('Ctrl Pts',(-3.58343491738278,3.66767852870569,43.2631548441291));
#55484=CARTESIAN_POINT('Ctrl Pts',(-4.90266910982671,1.50223406851191,43.4023283015511));
#55485=CARTESIAN_POINT('Ctrl Pts',(-5.02302888611788,-1.03055926868484,
43.541501758973));
#55486=CARTESIAN_POINT('Ctrl Pts',(-3.91508206282783,-3.3113447477378,43.680675216395));
#55487=CARTESIAN_POINT('Ctrl Pts',(-1.84976046732335,-4.78239038667639,
43.8198486738169));
#55488=CARTESIAN_POINT('Ctrl Pts',(0.667892389093657,-5.08397397255705,
43.9590221312389));
#55489=CARTESIAN_POINT('Ctrl Pts',(3.02222214943982,-4.14234774934242,44.0981955886608));
#55490=CARTESIAN_POINT('Ctrl Pts',(4.63751267753772,-2.18777232881387,44.2373690460827));
#55491=CARTESIAN_POINT('Ctrl Pts',(5.1187688298422,0.301790098715543,44.3765425035047));
#55492=CARTESIAN_POINT('Ctrl Pts',(4.34830661102557,2.71755427058194,44.5157159609267));
#55493=CARTESIAN_POINT('Ctrl Pts',(2.51453103518521,4.46878118396249,44.6548894183486));
#55494=CARTESIAN_POINT('Ctrl Pts',(0.0658644970599633,5.12723448508783,
44.7940628757706));
#55495=CARTESIAN_POINT('Ctrl Pts',(-2.3989082188817,4.5318992656974,44.9332363331925));
#55496=CARTESIAN_POINT('Ctrl Pts',(-4.27706380323859,2.82835585103309,45.0724097906145));
#55497=CARTESIAN_POINT('Ctrl Pts',(-5.10932739384903,0.433180308313655,
45.2115832480364));
#55498=CARTESIAN_POINT('Ctrl Pts',(-4.692181375323,-2.06792300101305,45.3507567054584));
#55499=CARTESIAN_POINT('Ctrl Pts',(-3.12763256847743,-4.06334666422225,
45.4899301628804));
#55500=CARTESIAN_POINT('Ctrl Pts',(-0.798267987718407,-5.06513966409919,
45.6291036203023));
#55501=CARTESIAN_POINT('Ctrl Pts',(1.72630109211463,-4.82832850336539,45.7682770777242));
#55502=CARTESIAN_POINT('Ctrl Pts',(3.82872905502739,-3.41082181009738,45.9074505351462));
#55503=CARTESIAN_POINT('Ctrl Pts',(4.99489858245798,-1.15924964869784,46.0466239925681));
#55504=CARTESIAN_POINT('Ctrl Pts',(4.93964035540605,1.37579967883806,46.1857974499902));
#55505=CARTESIAN_POINT('Ctrl Pts',(3.67646694696398,3.57441776866221,46.3249709074119));
#55506=CARTESIAN_POINT('Ctrl Pts',(1.51426852463472,4.89896544510649,46.4641443648341));
#55507=CARTESIAN_POINT('Ctrl Pts',(-1.01822162097875,5.02554438122063,46.6033178222559));
#55508=CARTESIAN_POINT('Ctrl Pts',(-3.30172089569737,3.92320159104299,46.7424912796779));
#55509=CARTESIAN_POINT('Ctrl Pts',(-4.77783369940276,1.86149851944559,46.8816647370998));
#55510=CARTESIAN_POINT('Ctrl Pts',(-5.08559871978225,-0.655406178179629,
47.0208381945219));
#55511=CARTESIAN_POINT('Ctrl Pts',(-4.14975662342901,-3.01204109589393,
47.1600116519437));
#55512=CARTESIAN_POINT('Ctrl Pts',(-2.19915360039652,-4.63212640575685,
47.2991851093658));
#55513=CARTESIAN_POINT('Ctrl Pts',(0.289219549406528,-5.11949447204388,
47.4383585667875));
#55514=CARTESIAN_POINT('Ctrl Pts',(2.7068683833997,-4.35496672226068,47.5775320242097));
#55515=CARTESIAN_POINT('Ctrl Pts',(4.4625930328204,-2.52549698484668,47.7167054816315));
#55516=CARTESIAN_POINT('Ctrl Pts',(5.12705728980988,-0.0784547261432202,
47.8558789390536));
#55517=CARTESIAN_POINT('Ctrl Pts',(4.53777635673904,2.38777246262433,47.9950523964754));
#55518=CARTESIAN_POINT('Ctrl Pts',(2.83885007366626,4.27010560247541,48.1342258538975));
#55519=CARTESIAN_POINT('Ctrl Pts',(0.445725457324341,5.10824827252355,48.2733993113193));
#55520=CARTESIAN_POINT('Ctrl Pts',(-2.0563946542149,4.69724521641816,48.4125727687414));
#55521=CARTESIAN_POINT('Ctrl Pts',(-4.05565420445089,3.13760108537823,48.5517462261632));
#55522=CARTESIAN_POINT('Ctrl Pts',(-5.06316416735844,0.810703528686243,
48.6909196835853));
#55523=CARTESIAN_POINT('Ctrl Pts',(-4.83255304784156,-1.714439452662,48.8300931410071));
#55524=CARTESIAN_POINT('Ctrl Pts',(-3.4202133466128,-3.8203419036388,48.9692665984293));
#55525=CARTESIAN_POINT('Ctrl Pts',(-1.17151161743895,-4.99203687158382,
49.108440055851));
#55526=CARTESIAN_POINT('Ctrl Pts',(1.36366575896105,-4.94300387364647,49.2476135132731));
#55527=CARTESIAN_POINT('Ctrl Pts',(3.56537906630424,-3.68523319623146,49.386786970695));
#55528=CARTESIAN_POINT('Ctrl Pts',(4.89523223976419,-1.52629384976162,49.5259604281169));
#55529=CARTESIAN_POINT('Ctrl Pts',(5.02802957243399,1.00587783342514,49.6651338855389));
#55530=CARTESIAN_POINT('Ctrl Pts',(3.93129746246441,3.29207713437395,49.8043073429608));
#55531=CARTESIAN_POINT('Ctrl Pts',(1.87322534678482,4.77324820192809,49.9434808003828));
#55532=CARTESIAN_POINT('Ctrl Pts',(-0.642916015185119,5.08719280099207,
50.0826542578048));
#55533=CARTESIAN_POINT('Ctrl Pts',(-3.00184187982617,4.15714047460132,50.2218277152267));
#55534=CARTESIAN_POINT('Ctrl Pts',(-4.62671220238579,2.21052161114549,50.3610011726486));
#55535=CARTESIAN_POINT('Ctrl Pts',(-5.12018924383978,-0.276647256112013,
50.5001746300706));
#55536=CARTESIAN_POINT('Ctrl Pts',(-4.36160057317046,-2.69616617387836,
50.6393480874925));
#55537=CARTESIAN_POINT('Ctrl Pts',(-2.53644770583317,-4.45637797236955,
50.7785215449146));
#55538=CARTESIAN_POINT('Ctrl Pts',(-0.0910444821465626,-5.12684917852256,
50.9176950023364));
#55539=CARTESIAN_POINT('Ctrl Pts',(2.37662230816716,-4.54362608511847,51.0568684597585));
#55540=CARTESIAN_POINT('Ctrl Pts',(4.26312165309721,-2.84932717811426,51.1960419171803));
#55541=CARTESIAN_POINT('Ctrl Pts',(5.10713834860655,-0.458267918623071,
51.3352153746024));
#55542=CARTESIAN_POINT('Ctrl Pts',(4.70228073325844,2.04485390741571,51.4743888320243));
#55543=CARTESIAN_POINT('Ctrl Pts',(3.14755068263376,4.04793728920033,51.6135622894463));
#55544=CARTESIAN_POINT('Ctrl Pts',(0.823134181134756,5.06115813988206,51.7527357468682));
#55545=CARTESIAN_POINT('Ctrl Pts',(-1.70256747518846,4.83674845216052,51.8919092042902));
#55546=CARTESIAN_POINT('Ctrl Pts',(-3.8119317156975,3.42958425933908,52.0310826617121));
#55547=CARTESIAN_POINT('Ctrl Pts',(-4.98914505886961,1.18376652199825,52.1702561191341));
#55548=CARTESIAN_POINT('Ctrl Pts',(-4.94633758571435,-1.35152361621851,
52.3094295765559));
#55549=CARTESIAN_POINT('Ctrl Pts',(-3.69397722364766,-3.5563188648122,52.448603033978));
#55550=CARTESIAN_POINT('Ctrl Pts',(-1.53830997137995,-4.891469516311,52.5877764913998));
#55551=CARTESIAN_POINT('Ctrl Pts',(0.993527980457018,-5.03048444477228,
52.7269499488219));
#55552=CARTESIAN_POINT('Ctrl Pts',(3.28241352191931,-3.93936962827405,52.8661234062438));
#55553=CARTESIAN_POINT('Ctrl Pts',(4.76863392190279,-1.88494087862853,53.0052968636658));
#55554=CARTESIAN_POINT('Ctrl Pts',(5.08875620657422,0.630421975425304,53.1444703210877));
#55555=CARTESIAN_POINT('Ctrl Pts',(4.16449925833512,2.9916245627373,53.2836437785097));
#55556=CARTESIAN_POINT('Ctrl Pts',(2.22187629251225,4.62127010007193,53.4228172359315));
#55557=CARTESIAN_POINT('Ctrl Pts',(-0.264073294642276,5.12085314104043,
53.5619906933537));
#55558=CARTESIAN_POINT('Ctrl Pts',(-2.68544770655171,4.36820812375314,53.7011641507754));
#55559=CARTESIAN_POINT('Ctrl Pts',(-4.45013604008643,2.54738313211239,53.8403376081976));
#55560=CARTESIAN_POINT('Ctrl Pts',(-5.12661015248078,0.103633689154421,
53.9795110656193));
#55561=CARTESIAN_POINT('Ctrl Pts',(-4.54944841556215,-2.36545782274508,
54.1186845230415));
#55562=CARTESIAN_POINT('Ctrl Pts',(-2.8597871012007,-4.25611199721682,54.2578579804633));
#55563=CARTESIAN_POINT('Ctrl Pts',(-0.470807616579455,-5.10599762879083,
54.3970314378853));
#55564=CARTESIAN_POINT('Ctrl Pts',(2.0333008302056,-4.70728789547995,54.5362048953072));
#55565=CARTESIAN_POINT('Ctrl Pts',(4.04019596500318,-3.15748130024849,54.6753783527292));
#55566=CARTESIAN_POINT('Ctrl Pts',(5.05912159376628,-0.835559870107751,
54.8145518101511));
#55567=CARTESIAN_POINT('Ctrl Pts',(4.84091469102418,1.69068523128142,54.9537252675731));
#55568=CARTESIAN_POINT('Ctrl Pts',(3.4389344917701,3.80349854191647,55.092898724995));
#55569=CARTESIAN_POINT('Ctrl Pts',(1.1960142884793,4.98622316175281,55.232072182417));
#55570=CARTESIAN_POINT('Ctrl Pts',(-1.33937332382694,4.94964147150757,55.3712456398389));
#55571=CARTESIAN_POINT('Ctrl Pts',(-3.54723721881863,3.70269897648656,55.5104190972609));
#55572=CARTESIAN_POINT('Ctrl Pts',(-4.88767729743601,1.55031681703309,55.6495925546829));
#55573=CARTESIAN_POINT('Ctrl Pts',(-5.03290898343272,-0.981172136543431,
55.7887660121048));
#55574=CARTESIAN_POINT('Ctrl Pts',(-3.94741803979709,-3.27273011660468,
55.9279394695267));
#55575=CARTESIAN_POINT('Ctrl Pts',(-1.89664504433241,-4.76399088715083,
56.0671129269487));
#55576=CARTESIAN_POINT('Ctrl Pts',(0.617924134239044,-5.09028892710146,
56.2062863843707));
#55577=CARTESIAN_POINT('Ctrl Pts',(2.98138920623766,-4.17183293025696,56.3454598417926));
#55578=CARTESIAN_POINT('Ctrl Pts',(4.61580013163112,-2.23321757602816,56.4846332992146));
#55579=CARTESIAN_POINT('Ctrl Pts',(5.12148615964254,0.251497740818248,56.6238067566365));
#55580=CARTESIAN_POINT('Ctrl Pts',(4.37478933416524,2.67471304605202,56.7629802140585));
#55581=CARTESIAN_POINT('Ctrl Pts',(2.55830319774378,4.44386727360986,56.9021536714803));
#55582=CARTESIAN_POINT('Ctrl Pts',(0.116222271253945,5.12634021312587,57.0413271289025));
#55583=CARTESIAN_POINT('Ctrl Pts',(-2.35427907367985,4.55524331296145,57.1805005863242));
#55584=CARTESIAN_POINT('Ctrl Pts',(-4.24907667710245,2.87022977985227,57.3196740437464));
#55585=CARTESIAN_POINT('Ctrl Pts',(-5.10482611995491,0.483344475579185,
57.4588475011681));
#55586=CARTESIAN_POINT('Ctrl Pts',(-4.71226667288952,-2.02173549224955,
57.5980209585902));
#55587=CARTESIAN_POINT('Ctrl Pts',(-3.16739287834083,-4.03243027853956,
57.7371944160121));
#55588=CARTESIAN_POINT('Ctrl Pts',(-0.847980520678397,-5.05705454129148,
57.8763678734341));
#55589=CARTESIAN_POINT('Ctrl Pts',(1.67879279259075,-4.84505173931014,58.0155413308561));
#55590=CARTESIAN_POINT('Ctrl Pts',(3.79504243314771,-3.44826398752403,58.1547147882779));
#55591=CARTESIAN_POINT('Ctrl Pts',(4.98327119785246,-1.20825484302812,58.2938882457));
#55592=CARTESIAN_POINT('Ctrl Pts',(4.95291551110372,1.32721495505253,58.4330617031219));
#55593=CARTESIAN_POINT('Ctrl Pts',(3.71139840215604,3.53813418308582,58.5722351605439));
#55594=CARTESIAN_POINT('Ctrl Pts',(1.56231431431994,4.88385560600616,58.7114086179658));
#55595=CARTESIAN_POINT('Ctrl Pts',(-0.968810376189768,5.0353031737954,58.8505820753878));
#55596=CARTESIAN_POINT('Ctrl Pts',(-3.26302697682058,3.95544264850191,58.9897555328096));
#55597=CARTESIAN_POINT('Ctrl Pts',(-4.75931912566953,1.90833777332089,59.1289289902317));
#55598=CARTESIAN_POINT('Ctrl Pts',(-5.0917909533315,-0.605422566987785,
59.2681024476536));
#55599=CARTESIAN_POINT('Ctrl Pts',(-4.17914144614525,-2.97113587204582,
59.4072759050756));
#55600=CARTESIAN_POINT('Ctrl Pts',(-2.24454539330572,-4.61030233004723,
59.5464493624975));
#55601=CARTESIAN_POINT('Ctrl Pts',(0.238920670469636,-5.12208829582852,
59.6856228199195));
#55602=CARTESIAN_POINT('Ctrl Pts',(2.6639622571092,-4.38134416472343,59.8247962773414));
#55603=CARTESIAN_POINT('Ctrl Pts',(4.43757171073933,-2.56920783687788,59.9639697347634));
#55604=CARTESIAN_POINT('Ctrl Pts',(5.12603936208722,-0.128810152540617,
60.1031431921853));
#55605=CARTESIAN_POINT('Ctrl Pts',(4.56101074237015,2.34308612838655,60.2423166496072));
#55606=CARTESIAN_POINT('Ctrl Pts',(2.88065515110656,4.24201573516153,60.3814901070293));
#55607=CARTESIAN_POINT('Ctrl Pts',(0.495878420013193,5.10362382919256,60.5206635644512));
#55608=CARTESIAN_POINT('Ctrl Pts',(-2.01015796326168,4.7172170354076,60.6598370218731));
#55609=CARTESIAN_POINT('Ctrl Pts',(-4.02464027668354,3.1772853572572,60.7990104792952));
#55610=CARTESIAN_POINT('Ctrl Pts',(-5.05495699482949,0.860396057730921,
60.9381839367169));
#55611=CARTESIAN_POINT('Ctrl Pts',(-4.84915957225241,-1.66689023039832,
61.0773573941391));
#55612=CARTESIAN_POINT('Ctrl Pts',(-3.45757268999299,-3.78656344121777,
61.2165308515608));
#55613=CARTESIAN_POINT('Ctrl Pts',(-1.22048811252045,-4.98028918333677,
61.355704308983));
#55614=CARTESIAN_POINT('Ctrl Pts',(1.31504858454702,-4.95615968794384,61.4948777664048));
#55615=CARTESIAN_POINT('Ctrl Pts',(3.52900980989584,-3.72007544198956,61.6340512238268));
#55616=CARTESIAN_POINT('Ctrl Pts',(4.8800044701548,-1.57430240300827,61.7732246812487));
#55617=CARTESIAN_POINT('Ctrl Pts',(5.0376669914975,0.956442797563212,61.9123981386707));
#55618=CARTESIAN_POINT('Ctrl Pts',(3.96344342536178,3.25330411499177,62.0515715960926));
#55619=CARTESIAN_POINT('Ctrl Pts',(1.92001895732006,4.75461875552336,62.1907450535146));
#55620=CARTESIAN_POINT('Ctrl Pts',(-0.592917275387842,5.09326210086,62.3299185109366));
#55621=CARTESIAN_POINT('Ctrl Pts',(-2.96086476568654,4.18642510396251,62.4690919683585));
#55622=CARTESIAN_POINT('Ctrl Pts',(-4.60477644817559,2.25585900886765,62.6082654257805));
#55623=CARTESIAN_POINT('Ctrl Pts',(-5.12266009271483,-0.226340858050212,
62.7474388832024));
#55624=CARTESIAN_POINT('Ctrl Pts',(-4.38787150941422,-2.6531979430407,62.8866123406244));
#55625=CARTESIAN_POINT('Ctrl Pts',(-2.5800990640586,-4.43124443783022,63.0257857980463));
#55626=CARTESIAN_POINT('Ctrl Pts',(-0.141393199236074,-5.12571725998609,
63.1649592554683));
#55627=CARTESIAN_POINT('Ctrl Pts',(2.33187113869595,-4.56673182658543,63.3041327128902));
#55628=CARTESIAN_POINT('Ctrl Pts',(4.23494465804981,-2.89109992630838,63.4433061703121));
#55629=CARTESIAN_POINT('Ctrl Pts',(5.10236059910481,-0.508337431653702,
63.5824796277342));
#55630=CARTESIAN_POINT('Ctrl Pts',(4.72219820521398,1.9984257720543,63.721653085156));
#55631=CARTESIAN_POINT('Ctrl Pts',(3.18703877163087,4.01712720269185,63.8608265425781));
#55632=CARTESIAN_POINT('Ctrl Pts',(1.64440293964314,4.70703764334184,63.953608847526));
#55633=CARTESIAN_POINT('Ctrl Pts',(0.837162017642518,4.84647736182856,64.));
#55634=CARTESIAN_POINT('Ctrl Pts',(-2.29321473482425,4.72388001049942,-0.384322829190576));
#55635=CARTESIAN_POINT('Ctrl Pts',(-3.08003554722089,4.34191665058258,-0.337931676716592));
#55636=CARTESIAN_POINT('Ctrl Pts',(-4.45832109727037,3.17760685879857,-0.245149371768623));
#55637=CARTESIAN_POINT('Ctrl Pts',(-5.43565004358383,0.652397313295008,
-0.105975914346671));
#55638=CARTESIAN_POINT('Ctrl Pts',(-5.08369590891124,-2.0316315709213,0.0331975430752808));
#55639=CARTESIAN_POINT('Ctrl Pts',(-3.48864045527025,-4.2192066179736,0.172371000497233));
#55640=CARTESIAN_POINT('Ctrl Pts',(-1.04046924885582,-5.3748591324054,0.311544457919186));
#55641=CARTESIAN_POINT('Ctrl Pts',(1.66212242595201,-5.21626167055254,0.450717915341138));
#55642=CARTESIAN_POINT('Ctrl Pts',(3.9582724176131,-3.78205855212937,0.58989137276309));
#55643=CARTESIAN_POINT('Ctrl Pts',(5.28648326155152,-1.42303359857138,0.729064830185042));
#55644=CARTESIAN_POINT('Ctrl Pts',(5.32196512387744,1.28398525892032,0.868238287606994));
#55645=CARTESIAN_POINT('Ctrl Pts',(4.05603925878376,3.67701840740235,1.00741174502895));
#55646=CARTESIAN_POINT('Ctrl Pts',(1.79827002706525,5.17089492789387,1.1465852024509));
#55647=CARTESIAN_POINT('Ctrl Pts',(-0.899239443192715,5.40030475984112,
1.28575865987285));
#55648=CARTESIAN_POINT('Ctrl Pts',(-3.37685325500269,4.30915166991622,1.4249321172948));
#55649=CARTESIAN_POINT('Ctrl Pts',(-5.02870815206118,2.16425954210186,1.56410557471676));
#55650=CARTESIAN_POINT('Ctrl Pts',(-5.4508676437325,-0.509869668716006,
1.70327903213871));
#55651=CARTESIAN_POINT('Ctrl Pts',(-4.54009897901715,-3.05931799129542,
1.84245248956066));
#55652=CARTESIAN_POINT('Ctrl Pts',(-2.51911699485592,-4.86065578946139,
1.98162594698261));
#55653=CARTESIAN_POINT('Ctrl Pts',(0.117877375912552,-5.47339293083152,
2.12079940440456));
#55654=CARTESIAN_POINT('Ctrl Pts',(2.72604659895634,-4.74769366479615,2.25997286182652));
#55655=CARTESIAN_POINT('Ctrl Pts',(4.66760189067538,-2.86101691810178,2.39914631924847));
#55656=CARTESIAN_POINT('Ctrl Pts',(5.46776493995964,-0.274721263755522,
2.53831977667042));
#55657=CARTESIAN_POINT('Ctrl Pts',(4.9308678380472,2.37875336537121,2.67749323409237));
#55658=CARTESIAN_POINT('Ctrl Pts',(3.18820074280552,4.45053943200986,2.81666669151433));
#55659=CARTESIAN_POINT('Ctrl Pts',(0.665906832292452,5.43401263349861,2.95584014893628));
#55660=CARTESIAN_POINT('Ctrl Pts',(-2.01922463603481,5.08867930612745,3.09501360635823));
#55661=CARTESIAN_POINT('Ctrl Pts',(-4.21058491518014,3.49898555055628,3.23418706378019));
#55662=CARTESIAN_POINT('Ctrl Pts',(-5.37230961851784,1.05366720260117,3.37336052120213));
#55663=CARTESIAN_POINT('Ctrl Pts',(-5.22031634232453,-1.64930970321809,
3.51253397862409));
#55664=CARTESIAN_POINT('Ctrl Pts',(-3.79177276937472,-3.94897258492089,
3.65170743604604));
#55665=CARTESIAN_POINT('Ctrl Pts',(-1.43600786795491,-5.28297327404123,
3.79088089346799));
#55666=CARTESIAN_POINT('Ctrl Pts',(1.27091128347078,-5.32510185072449,3.93005435088995));
#55667=CARTESIAN_POINT('Ctrl Pts',(3.66704808576738,-4.06505640154244,4.06922780831189));
#55668=CARTESIAN_POINT('Ctrl Pts',(5.16646311583264,-1.8109621983326,4.20840126573385));
#55669=CARTESIAN_POINT('Ctrl Pts',(5.40249685035948,0.885975729297808,4.34757472315579));
#55670=CARTESIAN_POINT('Ctrl Pts',(4.31743076922477,3.36626154123542,4.48674818057776));
#55671=CARTESIAN_POINT('Ctrl Pts',(2.17660155646045,5.02337843243596,4.62592163799969));
#55672=CARTESIAN_POINT('Ctrl Pts',(-0.49648301797377,5.45210324773045,4.76509509542167));
#55673=CARTESIAN_POINT('Ctrl Pts',(-3.04816009478389,4.54759774470171,4.9042685528436));
#55674=CARTESIAN_POINT('Ctrl Pts',(-4.85445520268865,2.53104521811412,5.04344201026558));
#55675=CARTESIAN_POINT('Ctrl Pts',(-5.47366588443908,-0.104436567240076,
5.1826154676875));
#55676=CARTESIAN_POINT('Ctrl Pts',(-4.75437342750754,-2.71437995182313,
5.32178892510947));
#55677=CARTESIAN_POINT('Ctrl Pts',(-2.87247004591648,-4.66056231010398,
5.46096238253142));
#55678=CARTESIAN_POINT('Ctrl Pts',(-0.288147069596518,-5.46707384963218,
5.60013583995337));
#55679=CARTESIAN_POINT('Ctrl Pts',(2.36663796363368,-4.93669423401298,5.73930929737533));
#55680=CARTESIAN_POINT('Ctrl Pts',(4.44269707362967,-3.19911986693394,5.87848275479727));
#55681=CARTESIAN_POINT('Ctrl Pts',(5.43236105048979,-0.679248576127037,
6.01765621221923));
#55682=CARTESIAN_POINT('Ctrl Pts',(5.09362236813656,2.00672279646893,6.15682966964118));
#55683=CARTESIAN_POINT('Ctrl Pts',(3.50931450583143,4.20198011777903,6.29600312706314));
#55684=CARTESIAN_POINT('Ctrl Pts',(1.06685625951563,5.36970603781822,6.43517658448508));
#55685=CARTESIAN_POINT('Ctrl Pts',(-1.63648573126543,5.22435064504803,6.57435004190704));
#55686=CARTESIAN_POINT('Ctrl Pts',(-3.93964960852039,3.80145842712166,6.71352349932899));
#55687=CARTESIAN_POINT('Ctrl Pts',(-5.27943108764563,1.44897639796171,6.85269695675095));
#55688=CARTESIAN_POINT('Ctrl Pts',(-5.32820664305195,-1.2578311412849,6.99187041417289));
#55689=CARTESIAN_POINT('Ctrl Pts',(-4.07404894205586,-3.65705488457347,
7.13104387159485));
#55690=CARTESIAN_POINT('Ctrl Pts',(-1.82364349572545,-5.16200054354388,
7.27021732901679));
#55691=CARTESIAN_POINT('Ctrl Pts',(0.872706696667147,-5.40465616229575,
7.40939078643876));
#55692=CARTESIAN_POINT('Ctrl Pts',(3.35564951687092,-4.32568393794243,7.5485642438607));
#55693=CARTESIAN_POINT('Ctrl Pts',(5.01801842820364,-2.18893039296773,7.68773770128266));
#55694=CARTESIAN_POINT('Ctrl Pts',(5.45330597251155,0.483093346278957,7.82691115870461));
#55695=CARTESIAN_POINT('Ctrl Pts',(4.55506909013666,3.03698383188497,7.96608461612655));
#55696=CARTESIAN_POINT('Ctrl Pts',(2.54295817840347,4.84822533654739,8.10525807354852));
#55697=CARTESIAN_POINT('Ctrl Pts',(-0.0909951283882992,5.47390583565873,
8.24443153097046));
#55698=CARTESIAN_POINT('Ctrl Pts',(-2.70269693727647,4.76102451960558,8.38360498839242));
#55699=CARTESIAN_POINT('Ctrl Pts',(-4.65349462636169,2.88390585378095,8.52277844581437));
#55700=CARTESIAN_POINT('Ctrl Pts',(-5.46634979306309,0.301571137425558,
8.66195190323632));
#55701=CARTESIAN_POINT('Ctrl Pts',(-4.9424908618235,-2.35450829088376,8.80112536065827));
#55702=CARTESIAN_POINT('Ctrl Pts',(-3.21001970047595,-4.43482792604239,
8.94029881808022));
#55703=CARTESIAN_POINT('Ctrl Pts',(-0.692586224104254,-5.43067671043215,
9.07947227550218));
#55704=CARTESIAN_POINT('Ctrl Pts',(1.99420885641777,-5.09853471578198,9.21864573292412));
#55705=CARTESIAN_POINT('Ctrl Pts',(4.19334998255961,-3.51962230002261,9.35781919034609));
#55706=CARTESIAN_POINT('Ctrl Pts',(5.36707007794315,-1.08003888332615,9.49699264776802));
#55707=CARTESIAN_POINT('Ctrl Pts',(5.22835344508653,1.62365189135507,9.63616610519));
#55708=CARTESIAN_POINT('Ctrl Pts',(3.81112116218231,3.93030287614265,9.77533956261193));
#55709=CARTESIAN_POINT('Ctrl Pts',(1.46193619068226,5.2758570664322,9.9145130200339));
#55710=CARTESIAN_POINT('Ctrl Pts',(-1.24474341441315,5.33127930644458,10.0536864774558));
#55711=CARTESIAN_POINT('Ctrl Pts',(-3.64703963144277,4.08301691617056,10.1928599348778));
#55712=CARTESIAN_POINT('Ctrl Pts',(-5.15750684453896,1.83631379659982,10.3320333922997));
#55713=CARTESIAN_POINT('Ctrl Pts',(-5.40678288430936,-0.859432401639897,
10.4712068497217));
#55714=CARTESIAN_POINT('Ctrl Pts',(-4.33391102290919,-3.34501725803552,
10.6103803071437));
#55715=CARTESIAN_POINT('Ctrl Pts',(-2.20124603028706,-5.01262816546316,
10.7495537645656));
#55716=CARTESIAN_POINT('Ctrl Pts',(0.469700761545068,-5.45447581401303,
10.8887272219876));
#55717=CARTESIAN_POINT('Ctrl Pts',(3.02578925606011,-4.56251296863476,11.0279006794095));
#55718=CARTESIAN_POINT('Ctrl Pts',(4.8419662357455,-2.55485580472747,11.1670741368315));
#55719=CARTESIAN_POINT('Ctrl Pts',(5.47411277938217,0.0775531408384875,
11.3062475942534));
#55720=CARTESIAN_POINT('Ctrl Pts',(4.76764690286142,2.6909976255443,11.4454210516754));
#55721=CARTESIAN_POINT('Ctrl Pts',(2.89532427177529,4.6463988821794,11.5845945090973));
#55722=CARTESIAN_POINT('Ctrl Pts',(0.314993386789232,5.46559277456052,11.7237679665193));
#55723=CARTESIAN_POINT('Ctrl Pts',(-2.34236442051593,4.94825768655495,11.8629414239412));
#55724=CARTESIAN_POINT('Ctrl Pts',(-4.42693203656908,3.22090017769063,12.0021148813632));
#55725=CARTESIAN_POINT('Ctrl Pts',(-5.42895962354868,0.705919695806274,
12.1412883387851));
#55726=CARTESIAN_POINT('Ctrl Pts',(-5.10341631940836,-1.98168289134401,
12.2804617962071));
#55727=CARTESIAN_POINT('Ctrl Pts',(-3.52990887099163,-4.18469456155927,
12.419635253629));
#55728=CARTESIAN_POINT('Ctrl Pts',(-1.09321499453303,-5.36440175478844,
12.558808711051));
#55729=CARTESIAN_POINT('Ctrl Pts',(1.61080826087004,-5.23232471830275,12.6979821684729));
#55730=CARTESIAN_POINT('Ctrl Pts',(3.92093244415056,-3.82076091629097,12.8371556258949));
#55731=CARTESIAN_POINT('Ctrl Pts',(5.27225123195099,-1.47488716796925,12.9763290833168));
#55732=CARTESIAN_POINT('Ctrl Pts',(5.33431982237489,1.23164818177408,13.1155025407388));
#55733=CARTESIAN_POINT('Ctrl Pts',(4.09196026980959,3.63700238676701,13.2546759981608));
#55734=CARTESIAN_POINT('Ctrl Pts',(1.84897302455433,5.15298204591473,13.3938494555827));
#55735=CARTESIAN_POINT('Ctrl Pts',(-0.846152924259742,5.40887700357624,
13.5330229130046));
#55736=CARTESIAN_POINT('Ctrl Pts',(-3.33436482884134,4.34211197451597,13.6721963704266));
#55737=CARTESIAN_POINT('Ctrl Pts',(-5.00720767671766,2.21354839415561,13.8113698278485));
#55738=CARTESIAN_POINT('Ctrl Pts',(-5.45561276518078,-0.456305344528939,
13.9505432852705));
#55739=CARTESIAN_POINT('Ctrl Pts',(-4.56992933530968,-3.01457643481222,
14.0897167426925));
#55740=CARTESIAN_POINT('Ctrl Pts',(-2.56673802534377,-4.83567793802519,
14.2288902001144));
#55741=CARTESIAN_POINT('Ctrl Pts',(0.0641106856454472,-5.47428671436153,
14.3680636575364));
#55742=CARTESIAN_POINT('Ctrl Pts',(2.67928208717311,-4.77424053734229,14.5072371149583));
#55743=CARTESIAN_POINT('Ctrl Pts',(4.63927512034426,-2.90672523104677,14.6464105723803));
#55744=CARTESIAN_POINT('Ctrl Pts',(5.46480279868925,-0.328413736751764,
14.7855840298022));
#55745=CARTESIAN_POINT('Ctrl Pts',(4.95399467343356,2.33020642575739,14.9247574872242));
#55746=CARTESIAN_POINT('Ctrl Pts',(3.23176123296902,4.41900945282172,15.0639309446461));
#55747=CARTESIAN_POINT('Ctrl Pts',(0.719248910832644,5.42720980019339,15.2031044020681));
#55748=CARTESIAN_POINT('Ctrl Pts',(-1.96914497677888,5.10826714957975,15.34227785949));
#55749=CARTESIAN_POINT('Ctrl Pts',(-4.17601390696993,3.54017415671077,15.481451316912));
#55750=CARTESIAN_POINT('Ctrl Pts',(-5.36170108444399,1.10638451368468,15.6206247743339));
#55751=CARTESIAN_POINT('Ctrl Pts',(-5.23626444075002,-1.59795491725705,
15.7597982317559));
#55752=CARTESIAN_POINT('Ctrl Pts',(-3.8303776313202,-3.91153836904752,15.8989716891778));
#55753=CARTESIAN_POINT('Ctrl Pts',(-1.48782925172868,-5.26861360594508,
16.0381451465998));
#55754=CARTESIAN_POINT('Ctrl Pts',(1.21854552233153,-5.33732817250869,16.1773186040217));
#55755=CARTESIAN_POINT('Ctrl Pts',(3.62694321107045,-4.10087894904483,16.3164920614437));
#55756=CARTESIAN_POINT('Ctrl Pts',(5.14842617495558,-1.86162110325421,16.4556655188657));
#55757=CARTESIAN_POINT('Ctrl Pts',(5.4109385074689,0.832868344601511,16.5948389762876));
#55758=CARTESIAN_POINT('Ctrl Pts',(4.35028674331132,3.32369229352223,16.7340124337096));
#55759=CARTESIAN_POINT('Ctrl Pts',(2.22583741039042,5.00175699465254,16.8731858911315));
#55760=CARTESIAN_POINT('Ctrl Pts',(-0.442907176004575,5.45671681915901,
17.0123593485535));
#55761=CARTESIAN_POINT('Ctrl Pts',(-3.00334543575433,4.57731814544092,17.1515328059754));
#55762=CARTESIAN_POINT('Ctrl Pts',(-4.82936048130468,2.57860476860292,17.2907062633974));
#55763=CARTESIAN_POINT('Ctrl Pts',(-5.474427639548,-0.0506678438667996,
17.4298797208193));
#55764=CARTESIAN_POINT('Ctrl Pts',(-4.78080538328875,-2.66755039280729,
17.5690531782413));
#55765=CARTESIAN_POINT('Ctrl Pts',(-2.91810866284794,-4.63212338381232,
17.7082266356632));
#55766=CARTESIAN_POINT('Ctrl Pts',(-0.341832106388815,-5.46397987021282,
17.8474000930852));
#55767=CARTESIAN_POINT('Ctrl Pts',(2.3180343799205,-4.95970178786544,17.9865735505071));
#55768=CARTESIAN_POINT('Ctrl Pts',(4.41106022257329,-3.24260280081925,18.1257470079291));
#55769=CARTESIAN_POINT('Ctrl Pts',(5.42542725091764,-0.732573788808574,
18.264920465351));
#55770=CARTESIAN_POINT('Ctrl Pts',(5.11308717704579,1.95659518832565,18.404093922773));
#55771=CARTESIAN_POINT('Ctrl Pts',(3.55041809528059,4.16730807113576,18.5432673801949));
#55772=CARTESIAN_POINT('Ctrl Pts',(1.1195473613692,5.35896808319478,18.6824408376169));
#55773=CARTESIAN_POINT('Ctrl Pts',(-1.58509193802151,5.24017258867191,18.8216142950388));
#55774=CARTESIAN_POINT('Ctrl Pts',(-3.90212070747964,3.8399712492814,18.9607877524608));
#55775=CARTESIAN_POINT('Ctrl Pts',(-5.26494421034928,1.50076236392,19.0999612098827));
#55776=CARTESIAN_POINT('Ctrl Pts',(-5.34030433870565,-1.20543551509431,
19.2391346673047));
#55777=CARTESIAN_POINT('Ctrl Pts',(-4.10977290009678,-3.61686216500979,
19.3783081247266));
#55778=CARTESIAN_POINT('Ctrl Pts',(-1.87425795643178,-5.14383925913332,
19.5174815821486));
#55779=CARTESIAN_POINT('Ctrl Pts',(0.819578742771026,-5.41296738355655,
19.6566550395706));
#55780=CARTESIAN_POINT('Ctrl Pts',(3.31299971643335,-4.35843528000149,19.7958284969925));
#55781=CARTESIAN_POINT('Ctrl Pts',(4.99627615213528,-2.23811300488903,19.9350019544145));
#55782=CARTESIAN_POINT('Ctrl Pts',(5.45778796929029,0.429506336762568,20.0741754118364));
#55783=CARTESIAN_POINT('Ctrl Pts',(4.58467935447419,2.99209632660904,20.2133488692584));
#55784=CARTESIAN_POINT('Ctrl Pts',(2.59045596294879,4.82301390367809,20.3525223266803));
#55785=CARTESIAN_POINT('Ctrl Pts',(-0.0372246965624955,5.47453555409178,
20.4916957841023));
#55786=CARTESIAN_POINT('Ctrl Pts',(-2.65580261318861,4.78734140111499,20.6308692415242));
#55787=CARTESIAN_POINT('Ctrl Pts',(-4.62494371570838,2.92947449853702,20.7700426989462));
#55788=CARTESIAN_POINT('Ctrl Pts',(-5.46312399409346,0.35524841478801,20.9092161563681));
#55789=CARTESIAN_POINT('Ctrl Pts',(-4.96537899543687,-2.30584835640235,
21.0483896137901));
#55790=CARTESIAN_POINT('Ctrl Pts',(-3.25342481586699,-4.4030843937574,21.187563071212));
#55791=CARTESIAN_POINT('Ctrl Pts',(-0.745894249385438,-5.42361198647016,
21.326736528634));
#55792=CARTESIAN_POINT('Ctrl Pts',(1.9440336016592,-5.11787637274183,21.4659099860559));
#55793=CARTESIAN_POINT('Ctrl Pts',(4.15857710655266,-3.56064062493046,21.6050834434779));
#55794=CARTESIAN_POINT('Ctrl Pts',(5.35620276752075,-1.132703458215,21.7442569008998));
#55795=CARTESIAN_POINT('Ctrl Pts',(5.24404913850238,1.57221940072675,21.8834303583218));
#55796=CARTESIAN_POINT('Ctrl Pts',(3.8495417123254,3.89267951623505,22.0226038157437));
#55797=CARTESIAN_POINT('Ctrl Pts',(1.51368642655711,5.26124306728988,22.1617772731657));
#55798=CARTESIAN_POINT('Ctrl Pts',(-1.19231823911521,5.34324830301965,22.3009507305877));
#55799=CARTESIAN_POINT('Ctrl Pts',(-3.60675930937326,4.11864206933528,22.4401241880096));
#55800=CARTESIAN_POINT('Ctrl Pts',(-5.13922132610689,1.88688350788735,22.5792976454316));
#55801=CARTESIAN_POINT('Ctrl Pts',(-5.41496361960511,-0.806284198903995,
22.7184711028535));
#55802=CARTESIAN_POINT('Ctrl Pts',(-4.36655753545115,-3.30228716205056,
22.8576445602755));
#55803=CARTESIAN_POINT('Ctrl Pts',(-2.25037510363002,-4.99076518221518,
22.9968180176974));
#55804=CARTESIAN_POINT('Ctrl Pts',(0.41610290760959,-5.45882620911565,23.1359914751193));
#55805=CARTESIAN_POINT('Ctrl Pts',(2.98082917520816,-4.59201291802157,23.2751649325413));
#55806=CARTESIAN_POINT('Ctrl Pts',(4.81663824341509,-2.60229153691902,23.4143383899633));
#55807=CARTESIAN_POINT('Ctrl Pts',(5.47461045734216,0.0237813247943329,
23.5535118473852));
#55808=CARTESIAN_POINT('Ctrl Pts',(4.79384855140899,2.64403881915585,23.6926853048072));
#55809=CARTESIAN_POINT('Ctrl Pts',(2.94082266957834,4.61773615932561,23.8318587622291));
#55810=CARTESIAN_POINT('Ctrl Pts',(0.368662581049387,5.46223517549209,23.9710322196511));
#55811=CARTESIAN_POINT('Ctrl Pts',(-2.29364842868432,4.97102626191444,24.110205677073));
#55812=CARTESIAN_POINT('Ctrl Pts',(-4.39508201446807,3.26422721285581,24.249379134495));
#55813=CARTESIAN_POINT('Ctrl Pts',(-5.42176401779696,0.759210212241224,
24.3885525919169));
#55814=CARTESIAN_POINT('Ctrl Pts',(-5.12263470778918,-1.93146029252551,
24.5277260493389));
#55815=CARTESIAN_POINT('Ctrl Pts',(-3.57084168401882,-4.14982106586813,
24.6668995067608));
#55816=CARTESIAN_POINT('Ctrl Pts',(-1.14585272489122,-5.35340515409665,
24.8060729641828));
#55817=CARTESIAN_POINT('Ctrl Pts',(1.5593373829938,-5.24789406686598,24.9452464216047));
#55818=CARTESIAN_POINT('Ctrl Pts',(3.88321485224389,-3.85908896274257,25.0844198790267));
#55819=CARTESIAN_POINT('Ctrl Pts',(5.25751019908472,-1.5266013617082,25.2235933364486));
#55820=CARTESIAN_POINT('Ctrl Pts',(5.34616004769862,1.1791937734911,25.3627667938706));
#55821=CARTESIAN_POINT('Ctrl Pts',(4.12748640327948,3.59663470508086,25.5019402512925));
#55822=CARTESIAN_POINT('Ctrl Pts',(1.89949768148914,5.1345724037223,25.6411137087145));
#55823=CARTESIAN_POINT('Ctrl Pts',(-0.792984793166221,5.41692720357734,
25.7802871661364));
#55824=CARTESIAN_POINT('Ctrl Pts',(-3.29155469497027,4.3746534606833,25.9194606235584));
#55825=CARTESIAN_POINT('Ctrl Pts',(-4.98522411812324,2.26262363267325,26.0586340809804));
#55826=CARTESIAN_POINT('Ctrl Pts',(-5.45983153237451,-0.402696969367929,
26.1978075384023));
#55827=CARTESIAN_POINT('Ctrl Pts',(-4.59931879186191,-2.96954404949229,
26.3369809958243));
#55828=CARTESIAN_POINT('Ctrl Pts',(-2.61411141914543,-4.81023353896073,
26.4761544532462));
#55829=CARTESIAN_POINT('Ctrl Pts',(0.0103378096254605,-5.47465234884748,
26.6153279106682));
#55830=CARTESIAN_POINT('Ctrl Pts',(2.63225908164434,-4.80032679493282,26.7545013680901));
#55831=CARTESIAN_POINT('Ctrl Pts',(4.61050075812538,-2.95215310754276,26.8936748255121));
#55832=CARTESIAN_POINT('Ctrl Pts',(5.46131341976825,-0.382074524285904,
27.032848282934));
#55833=CARTESIAN_POINT('Ctrl Pts',(4.9766435532453,2.28143467033162,27.172021740356));
#55834=CARTESIAN_POINT('Ctrl Pts',(3.27500992664753,4.38705313295944,27.3111951977779));
#55835=CARTESIAN_POINT('Ctrl Pts',(0.772521597081072,5.4198833560412,27.4503686551999));
#55836=CARTESIAN_POINT('Ctrl Pts',(-1.91887533674131,5.12736215349522,27.5895421126219));
#55837=CARTESIAN_POINT('Ctrl Pts',(-4.14104000188076,3.58102121103358,27.7287155700437));
#55838=CARTESIAN_POINT('Ctrl Pts',(-5.350575259792,1.15899508210823,27.8678890274658));
#55839=CARTESIAN_POINT('Ctrl Pts',(-5.25170735057791,-1.54644596250082,
28.0070624848877));
#55840=CARTESIAN_POINT('Ctrl Pts',(-3.86861294296327,-3.87372677257782,
28.1462359423097));
#55841=CARTESIAN_POINT('Ctrl Pts',(-1.53950709149657,-5.25374562824285,
28.2854093997316));
#55842=CARTESIAN_POINT('Ctrl Pts',(1.16606219736214,-5.34903955518484,28.4245828571536));
#55843=CARTESIAN_POINT('Ctrl Pts',(3.58648841318369,-4.13630584859827,28.5637563145755));
#55844=CARTESIAN_POINT('Ctrl Pts',(5.1298925200124,-1.91210040117403,28.7029297719975));
#55845=CARTESIAN_POINT('Ctrl Pts',(5.41885812363289,0.779680605752741,28.8421032294194));
#55846=CARTESIAN_POINT('Ctrl Pts',(4.38272300687972,3.28080237990896,28.9812766868414));
#55847=CARTESIAN_POINT('Ctrl Pts',(2.27485851816045,4.97965299327192,29.1204501442633));
#55848=CARTESIAN_POINT('Ctrl Pts',(-0.389288602875022,5.4608039330048,29.2596236016852));
#55849=CARTESIAN_POINT('Ctrl Pts',(-2.95824101751041,4.60659693194099,29.3987970591072));
#55850=CARTESIAN_POINT('Ctrl Pts',(-4.80379982893518,2.62591553835446,29.5379705165292));
#55851=CARTESIAN_POINT('Ctrl Pts',(-5.47466122835514,0.003105767880113,
29.6771439739511));
#55852=CARTESIAN_POINT('Ctrl Pts',(-4.80677609262286,-2.62046347168559,
29.8163174313731));
#55853=CARTESIAN_POINT('Ctrl Pts',(-2.96346574410807,-4.60323755573695,
29.955490888795));
#55854=CARTESIAN_POINT('Ctrl Pts',(-0.395484163623925,-5.46035873248011,
30.0946643462169));
#55855=CARTESIAN_POINT('Ctrl Pts',(2.26920715499286,-4.98223083555733,30.2338378036389));
#55856=CARTESIAN_POINT('Ctrl Pts',(4.37899779764542,-3.28577289222272,30.3730112610609));
#55857=CARTESIAN_POINT('Ctrl Pts',(5.41797001254325,-0.785828323637693,
30.5121847184828));
#55858=CARTESIAN_POINT('Ctrl Pts',(5.13205868135355,1.90627881019349,30.6513581759048));
#55859=CARTESIAN_POINT('Ctrl Pts',(3.59117914459247,4.13223396754023,30.7905316333268));
#55860=CARTESIAN_POINT('Ctrl Pts',(1.17213045061785,5.34771310167099,30.9297050907486));
#55861=CARTESIAN_POINT('Ctrl Pts',(-1.53354521698279,5.25548896664414,31.0688785481707));
#55862=CARTESIAN_POINT('Ctrl Pts',(-3.86421533444969,3.87811359555816,31.2080520055926));
#55863=CARTESIAN_POINT('Ctrl Pts',(-5.24994937746456,1.55240353810105,31.3472254630145));
#55864=CARTESIAN_POINT('Ctrl Pts',(-5.35188680811497,-1.15292358991135,
31.4863989204365));
#55865=CARTESIAN_POINT('Ctrl Pts',(-4.14510035211066,-3.57632049486357,
31.6255723778584));
#55866=CARTESIAN_POINT('Ctrl Pts',(-1.92469159094798,-5.1251817031968,31.7647458352804));
#55867=CARTESIAN_POINT('Ctrl Pts',(0.766371716887421,-5.42075636812835,
31.9039192927023));
#55868=CARTESIAN_POINT('Ctrl Pts',(3.27003028170278,-4.3907661253813,32.0430927501243));
#55869=CARTESIAN_POINT('Ctrl Pts',(4.97405184125494,-2.28707968631561,32.1822662075462));
#55870=CARTESIAN_POINT('Ctrl Pts',(5.46174340514298,0.375877888982928,32.3214396649682));
#55871=CARTESIAN_POINT('Ctrl Pts',(4.61384729437183,2.9469201474195,32.4606131223901));
#55872=CARTESIAN_POINT('Ctrl Pts',(2.63770382336763,4.79733715213355,32.5997865798121));
#55873=CARTESIAN_POINT('Ctrl Pts',(0.0165493266579919,5.47463709581159,
32.738960037234));
#55874=CARTESIAN_POINT('Ctrl Pts',(-2.60865206040676,4.81319640559002,32.8781334946561));
#55875=CARTESIAN_POINT('Ctrl Pts',(-4.59594659595723,2.97476051105938,33.0173069520779));
#55876=CARTESIAN_POINT('Ctrl Pts',(-5.45937111938441,0.408891418203707,
33.1564804094999));
#55877=CARTESIAN_POINT('Ctrl Pts',(-4.98778807515939,-2.25696595639962,
33.2956538669219));
#55878=CARTESIAN_POINT('Ctrl Pts',(-3.296516044681,-4.37091605709946,33.4348273243438));
#55879=CARTESIAN_POINT('Ctrl Pts',(-0.799130311671916,-5.4160239988405,
33.5740007817658));
#55880=CARTESIAN_POINT('Ctrl Pts',(1.89367078883877,-5.13672426304429,33.7131742391877));
#55881=CARTESIAN_POINT('Ctrl Pts',(4.12340301594658,-3.60131542344347,33.8523476966097));
#55882=CARTESIAN_POINT('Ctrl Pts',(5.34481869699234,-1.18525875121433,33.9915211540316));
#55883=CARTESIAN_POINT('Ctrl Pts',(5.25923889226169,1.5206352242307,34.1306946114536));
#55884=CARTESIAN_POINT('Ctrl Pts',(3.88759086323862,3.85468059521315,34.2698680688755));
#55885=CARTESIAN_POINT('Ctrl Pts',(1.56529062375651,5.24612146964108,34.4090415262975));
#55886=CARTESIAN_POINT('Ctrl Pts',(-1.13977803036409,5.35470178932016,34.5482149837195));
#55887=CARTESIAN_POINT('Ctrl Pts',(-3.56613101143271,4.15386986078608,34.6873884411414));
#55888=CARTESIAN_POINT('Ctrl Pts',(-5.12043998168154,1.93727117488656,34.8265618985634));
#55889=CARTESIAN_POINT('Ctrl Pts',(-5.42262192561739,-0.753058206822416,
34.9657353559852));
#55890=CARTESIAN_POINT('Ctrl Pts',(-4.39878276768831,-3.25923846530712,
35.1049088134073));
#55891=CARTESIAN_POINT('Ctrl Pts',(-2.29928706344549,-4.96842069584705,
35.2440822708292));
#55892=CARTESIAN_POINT('Ctrl Pts',(0.362464908557797,-5.46264994312406,
35.3832557282512));
#55893=CARTESIAN_POINT('Ctrl Pts',(2.935581507484,-4.62106983543499,35.5224291856731));
#55894=CARTESIAN_POINT('Ctrl Pts',(4.79084554752555,-2.64947620310197,35.6616026430951));
#55895=CARTESIAN_POINT('Ctrl Pts',(5.47457995136234,-0.0299927856439818,
35.800776100517));
#55896=CARTESIAN_POINT('Ctrl Pts',(4.81958769512005,2.59682491903027,35.939949557939));
#55897=CARTESIAN_POINT('Ctrl Pts',(2.98603734028964,4.58862792275044,36.0791230153609));
#55898=CARTESIAN_POINT('Ctrl Pts',(0.422296207179969,5.4583505864364,36.2182964727829));
#55899=CARTESIAN_POINT('Ctrl Pts',(-2.2447111483659,4.99331523854152,36.3574699302048));
#55900=CARTESIAN_POINT('Ctrl Pts',(-4.36280796005417,3.30723931924151,36.4966433876268));
#55901=CARTESIAN_POINT('Ctrl Pts',(-5.41404532666736,0.812427480973212,
36.6358168450487));
#55902=CARTESIAN_POINT('Ctrl Pts',(-5.1413588704341,-1.88105134870308,36.7749903024707));
#55903=CARTESIAN_POINT('Ctrl Pts',(-3.61142998646512,-4.1145472003502,36.9141637598926));
#55904=CARTESIAN_POINT('Ctrl Pts',(-1.19837990473434,-5.34189206320926,
37.0533372173146));
#55905=CARTESIAN_POINT('Ctrl Pts',(1.50771606209154,-5.26295710481857,37.1925106747365));
#55906=CARTESIAN_POINT('Ctrl Pts',(3.84512261236244,-3.89704468885695,37.3316841321585));
#55907=CARTESIAN_POINT('Ctrl Pts',(5.24226192785463,-1.5781682707541,37.4708575895804));
#55908=CARTESIAN_POINT('Ctrl Pts',(5.35748448182613,1.12662559798778,37.6100310470024));
#55909=CARTESIAN_POINT('Ctrl Pts',(4.16261432174461,3.55592002433348,37.7492045044243));
#55910=CARTESIAN_POINT('Ctrl Pts',(1.94983907713515,5.11566738405907,37.8883779618463));
#55911=CARTESIAN_POINT('Ctrl Pts',(-0.739740155837876,5.42445478485075,
38.0275514192682));
#55912=CARTESIAN_POINT('Ctrl Pts',(-3.24842699579643,4.40677288546053,38.1667248766902));
#55913=CARTESIAN_POINT('Ctrl Pts',(-4.962759591004,2.31148057593983,38.3058983341121));
#55914=CARTESIAN_POINT('Ctrl Pts',(-5.46352354148162,-0.349049742479761,
38.4450717915341));
#55915=CARTESIAN_POINT('Ctrl Pts',(-4.62826451157864,-2.92422516607577,
38.5842452489561));
#55916=CARTESIAN_POINT('Ctrl Pts',(-2.66123260657016,-4.7843250542555,38.723418706378));
#55917=CARTESIAN_POINT('Ctrl Pts',(-0.0434360637741723,-5.47448979535197,
38.8625921638));
#55918=CARTESIAN_POINT('Ctrl Pts',(2.58498211887365,-4.82594992267353,39.0017656212219));
#55919=CARTESIAN_POINT('Ctrl Pts',(4.58128158024812,-2.99729616379969,39.1409390786439));
#55920=CARTESIAN_POINT('Ctrl Pts',(5.4572971397899,-0.435698449721977,39.2801125360658));
#55921=CARTESIAN_POINT('Ctrl Pts',(4.99881229237497,2.23244280478805,39.4192859934878));
#55922=CARTESIAN_POINT('Ctrl Pts',(3.31794265124305,4.3546735554013,39.5584594509097));
#55923=CARTESIAN_POINT('Ctrl Pts',(0.825719751359792,5.41203400795518,39.6976329083317));
#55924=CARTESIAN_POINT('Ctrl Pts',(-1.86842056588151,5.14596247557638,39.8368063657536));
#55925=CARTESIAN_POINT('Ctrl Pts',(-4.10566657415155,3.62152277266674,39.9759798231756));
#55926=CARTESIAN_POINT('Ctrl Pts',(-5.33893321796927,1.21149383205752,40.1151532805975));
#55927=CARTESIAN_POINT('Ctrl Pts',(-5.26664358189404,-1.49478780846764,
40.2543267380195));
#55928=CARTESIAN_POINT('Ctrl Pts',(-3.90647501540673,-3.83554144353207,
40.3935001954414));
#55929=CARTESIAN_POINT('Ctrl Pts',(-1.59103640144185,-5.23837077537817,
40.5326736528633));
#55930=CARTESIAN_POINT('Ctrl Pts',(1.11346637209138,-5.3602348688533,40.6718471102854));
#55931=CARTESIAN_POINT('Ctrl Pts',(3.54568759513793,-4.17133368225729,40.8110205677072));
#55932=CARTESIAN_POINT('Ctrl Pts',(5.11086393910812,-1.96239522190952,40.9501940251292));
#55933=CARTESIAN_POINT('Ctrl Pts',(5.42625493477628,0.726417644241425,41.0893674825512));
#55934=CARTESIAN_POINT('Ctrl Pts',(4.41473643051778,3.23759593836356,41.2285409399732));
#55935=CARTESIAN_POINT('Ctrl Pts',(2.32366015027217,4.95706856086197,41.3677143973951));
#55936=CARTESIAN_POINT('Ctrl Pts',(-0.335632471641556,5.46436419494793,
41.5068878548171));
#55937=CARTESIAN_POINT('Ctrl Pts',(-2.91285119167301,4.63543127941923,41.6460613122389));
#55938=CARTESIAN_POINT('Ctrl Pts',(-4.77777571164161,2.67297296288171,41.785234769661));
#55939=CARTESIAN_POINT('Ctrl Pts',(-5.47436662832414,0.0568790799862881,
41.9244082270828));
#55940=CARTESIAN_POINT('Ctrl Pts',(-4.83228304988656,-2.57312373134837,
42.063581684505));
#55941=CARTESIAN_POINT('Ctrl Pts',(-3.00853691369941,-4.57390761274833,
42.2027551419267));
#55942=CARTESIAN_POINT('Ctrl Pts',(-0.449098065014904,-5.45621078579713,
42.3419285993489));
#55943=CARTESIAN_POINT('Ctrl Pts',(2.22016099964357,-5.00427920351281,42.4811020567706));
#55944=CARTESIAN_POINT('Ctrl Pts',(4.34651289219087,-3.32862597614506,42.6202755141927));
#55945=CARTESIAN_POINT('Ctrl Pts',(5.40999005483213,-0.839007042679954,
42.7594489716146));
#55946=CARTESIAN_POINT('Ctrl Pts',(5.15053505071161,1.85577851653701,42.8986224290366));
#55947=CARTESIAN_POINT('Ctrl Pts',(3.63159372118936,4.09676119090033,43.0377958864585));
#55948=CARTESIAN_POINT('Ctrl Pts',(1.22460045410757,5.33594217911408,43.1769693438805));
#55949=CARTESIAN_POINT('Ctrl Pts',(-1.48185054131569,5.2702983012588,43.3161428013024));
#55950=CARTESIAN_POINT('Ctrl Pts',(-3.82593714649597,3.91588178602361,43.4553162587244));
#55951=CARTESIAN_POINT('Ctrl Pts',(-5.23444803567515,1.60389493822557,43.5944897161463));
#55952=CARTESIAN_POINT('Ctrl Pts',(-5.36295293381699,-1.10030043202433,
43.7336631735683));
#55953=CARTESIAN_POINT('Ctrl Pts',(-4.18002788974679,-3.53543378554715,
43.8728366309903));
#55954=CARTESIAN_POINT('Ctrl Pts',(-1.97493953349668,-5.10602967579324,
44.0120100884122));
#55955=CARTESIAN_POINT('Ctrl Pts',(0.713090752367286,-5.42802236453917,
44.1511835458341));
#55956=CARTESIAN_POINT('Ctrl Pts',(3.22674535831947,-4.42267335484013,44.2903570032561));
#55957=CARTESIAN_POINT('Ctrl Pts',(4.95134763973783,-2.33582571299994,44.4295304606781));
#55958=CARTESIAN_POINT('Ctrl Pts',(5.46517189845383,0.322213176949267,44.5687039181));
#55959=CARTESIAN_POINT('Ctrl Pts',(4.64257009574122,2.90145965286068,44.7078773755219));
#55960=CARTESIAN_POINT('Ctrl Pts',(2.68469720124231,4.77119755917639,44.8470508329439));
#55961=CARTESIAN_POINT('Ctrl Pts',(0.0703217532190181,5.47421045102153,
44.9862242903658));
#55962=CARTESIAN_POINT('Ctrl Pts',(-2.56124982796045,4.83858703857042,45.1253977477878));
#55963=CARTESIAN_POINT('Ctrl Pts',(-4.56650606471606,3.01975952220713,45.2645712052098));
#55964=CARTESIAN_POINT('Ctrl Pts',(-5.45509153100881,0.462494972259141,
45.4037446626316));
#55965=CARTESIAN_POINT('Ctrl Pts',(-5.00971593898958,-2.20786580699166,
45.5429181200538));
#55966=CARTESIAN_POINT('Ctrl Pts',(-3.33928922952715,-4.33832601963165,
45.6820915774755));
#55967=CARTESIAN_POINT('Ctrl Pts',(-0.852289274811402,-5.40791347962323,
45.8212650348977));
#55968=CARTESIAN_POINT('Ctrl Pts',(1.84312527690108,-5.15507656826719,45.9604384923194));
#55969=CARTESIAN_POINT('Ctrl Pts',(4.08783110429599,-3.64164277130519,46.0996119497416));
#55970=CARTESIAN_POINT('Ctrl Pts',(5.33291896467962,-1.23769969185162,46.2387854071634));
#55971=CARTESIAN_POINT('Ctrl Pts',(5.27392124087496,1.46890433864736,46.3779588645854));
#55972=CARTESIAN_POINT('Ctrl Pts',(3.92526494398478,3.816309779168,46.5171323220073));
#55973=CARTESIAN_POINT('Ctrl Pts',(1.61674380356837,5.23049373239969,46.6563057794293));
#55974=CARTESIAN_POINT('Ctrl Pts',(-1.08712785717717,5.36563866032725,46.7954792368512));
#55975=CARTESIAN_POINT('Ctrl Pts',(-3.5251586573914,4.18869689178719,46.9346526942733));
#55976=CARTESIAN_POINT('Ctrl Pts',(-5.10116462326485,1.98747193625476,47.073826151695));
#55977=CARTESIAN_POINT('Ctrl Pts',(-5.4297570634819,-0.699759560576068,
47.2129996091172));
#55978=CARTESIAN_POINT('Ctrl Pts',(-4.43058361056827,-3.21587532109269,
47.3521730665389));
#55979=CARTESIAN_POINT('Ctrl Pts',(-2.34797719076535,-4.94559686212844,
47.4913465239611));
#55980=CARTESIAN_POINT('Ctrl Pts',(0.308791939320552,-5.46594664712891,
47.6305199813829));
#55981=CARTESIAN_POINT('Ctrl Pts',(2.89005061832919,-4.64968091749791,47.769693438805));
#55982=CARTESIAN_POINT('Ctrl Pts',(4.76459063652578,-2.69640525095543,47.9088668962268));
#55983=CARTESIAN_POINT('Ctrl Pts',(5.47402126438588,-0.0837640024137416,
48.0480403536489));
#55984=CARTESIAN_POINT('Ctrl Pts',(4.84486185071238,2.54936048030892,48.1872138110707));
#55985=CARTESIAN_POINT('Ctrl Pts',(3.03096392165112,4.55907698078223,48.3263872684927));
#55986=CARTESIAN_POINT('Ctrl Pts',(0.475889090672027,5.453939382174,48.4655607259146));
#55987=CARTESIAN_POINT('Ctrl Pts',(-2.19555730097171,5.01512246602204,48.6047341833367));
#55988=CARTESIAN_POINT('Ctrl Pts',(-4.33011298709005,3.34993234709049,48.7439076407585));
#55989=CARTESIAN_POINT('Ctrl Pts',(-5.40580429485011,0.865566367662955,
48.8830810981806));
#55990=CARTESIAN_POINT('Ctrl Pts',(-5.15958700085801,-1.8304609232721,49.0222545556024));
#55991=CARTESIAN_POINT('Ctrl Pts',(-3.651669862419,-4.07887636818645,49.1614280130245));
#55992=CARTESIAN_POINT('Ctrl Pts',(-1.25079146630195,-5.32986359289572,
49.3006014704464));
#55993=CARTESIAN_POINT('Ctrl Pts',(1.45594927852757,-5.27751237889635,49.4397749278683));
#55994=CARTESIAN_POINT('Ctrl Pts',(3.8066593996007,-3.93462443271029,49.5789483852903));
#55995=CARTESIAN_POINT('Ctrl Pts',(5.226507889396,-1.62958291999226,49.7181218427122));
#55996=CARTESIAN_POINT('Ctrl Pts',(5.36829203218933,1.07394872697987,49.8572953001341));
#55997=CARTESIAN_POINT('Ctrl Pts',(4.19734063610474,3.51486227262932,49.9964687575562));
#55998=CARTESIAN_POINT('Ctrl Pts',(1.99999235461371,5.09626881085917,50.135642214978));
#55999=CARTESIAN_POINT('Ctrl Pts',(-0.686424149254752,5.43145902114425,
50.2748156724001));
#56000=CARTESIAN_POINT('Ctrl Pts',(-3.20498589222948,4.43846715000337,50.4139891298219));
#56001=CARTESIAN_POINT('Ctrl Pts',(-4.93981626271097,2.36011451029508,50.553162587244));
#56002=CARTESIAN_POINT('Ctrl Pts',(-5.46668843630145,-0.295368839685396,
50.6923360446659));
#56003=CARTESIAN_POINT('Ctrl Pts',(-4.65676370181106,-2.87862415687495,
50.8315095020878));
#56004=CARTESIAN_POINT('Ctrl Pts',(-2.70809704142158,-4.75795498352946,
50.9706829595098));
#56005=CARTESIAN_POINT('Ctrl Pts',(-0.0972057465137546,-5.47379906955798,
51.1098564169317));
#56006=CARTESIAN_POINT('Ctrl Pts',(2.53745576008646,-4.85110744847536,51.2490298743538));
#56007=CARTESIAN_POINT('Ctrl Pts',(4.55162040574421,-3.04215004446889,51.3882033317756));
#56008=CARTESIAN_POINT('Ctrl Pts',(5.45275434624012,-0.489280339487104,
51.5273767891977));
#56009=CARTESIAN_POINT('Ctrl Pts',(5.02049875200887,2.18323555580393,51.6665502466195));
#56010=CARTESIAN_POINT('Ctrl Pts',(3.36055526465709,4.32187384409062,51.8057237040416));
#56011=CARTESIAN_POINT('Ctrl Pts',(0.878838241173826,5.40366251323115,51.9448971614634));
#56012=CARTESIAN_POINT('Ctrl Pts',(-1.81778553201607,5.16406632128618,52.0840706188854));
#56013=CARTESIAN_POINT('Ctrl Pts',(-4.06989703656874,3.66167493406748,52.2232440763074));
#56014=CARTESIAN_POINT('Ctrl Pts',(-5.32677608218628,1.26387569851522,52.3624175337293));
#56015=CARTESIAN_POINT('Ctrl Pts',(-5.28107169366842,-1.44298543907526,
52.5015909911513));
#56016=CARTESIAN_POINT('Ctrl Pts',(-3.94396019576248,-3.7969860659858,52.6407644485732));
#56017=CARTESIAN_POINT('Ctrl Pts',(-1.64241221007741,-5.22249053069871,
52.7799379059952));
#56018=CARTESIAN_POINT('Ctrl Pts',(1.06076312090249,-5.37091303340338,52.9191113634171));
#56019=CARTESIAN_POINT('Ctrl Pts',(3.50454469334802,-4.20595907057776,53.0582848208391));
#56020=CARTESIAN_POINT('Ctrl Pts',(5.09134226809777,-2.01250071307568,53.1974582782611));
#56021=CARTESIAN_POINT('Ctrl Pts',(5.43312822726344,0.673084598815311,53.336631735683));
#56022=CARTESIAN_POINT('Ctrl Pts',(4.44632392560814,3.19407713739254,53.475805193105));
#56023=CARTESIAN_POINT('Ctrl Pts',(2.37223759840168,4.93400587634211,53.6149786505269));
#56024=CARTESIAN_POINT('Ctrl Pts',(-0.281943958984394,5.46739726149851,
53.7541521079489));
#56025=CARTESIAN_POINT('Ctrl Pts',(-2.86718033739894,4.66381840597187,53.8933255653708));
#56026=CARTESIAN_POINT('Ctrl Pts',(-4.75129064020009,2.71977250213987,54.0324990227927));
#56027=CARTESIAN_POINT('Ctrl Pts',(-5.47354386787767,0.110646904466045,
54.1716724802147));
#56028=CARTESIAN_POINT('Ctrl Pts',(-4.85732379419873,-2.52553573907794,
54.3108459376367));
#56029=CARTESIAN_POINT('Ctrl Pts',(-3.0533178232087,-4.54413638456475,54.4500193950586));
#56030=CARTESIAN_POINT('Ctrl Pts',(-0.502668637955831,-5.45153643035289,
54.5891928524806));
#56031=CARTESIAN_POINT('Ctrl Pts',(2.17090064578782,-5.02584476453135,54.7283663099025));
#56032=CARTESIAN_POINT('Ctrl Pts',(4.31360864031496,-3.37115791817132,54.8675397673245));
#56033=CARTESIAN_POINT('Ctrl Pts',(5.40148814768119,-0.8921048153153,55.0067132247464));
#56034=CARTESIAN_POINT('Ctrl Pts',(5.16851450254163,1.80509917956493,55.1458866821683));
#56035=CARTESIAN_POINT('Ctrl Pts',(3.67165792592056,4.06089316358777,55.2850601395904));
#56036=CARTESIAN_POINT('Ctrl Pts',(1.27695230959419,5.3236564511688,55.4242335970122));
#56037=CARTESIAN_POINT('Ctrl Pts',(-1.43001289846173,5.28459916372871,55.5634070544343));
#56038=CARTESIAN_POINT('Ctrl Pts',(-3.787289836653,3.95327217684718,55.7025805118562));
#56039=CARTESIAN_POINT('Ctrl Pts',(-5.21844168053232,1.65523159646386,55.8417539692781));
#56040=CARTESIAN_POINT('Ctrl Pts',(-5.37350164816491,-1.04757111845367,
55.9809274267001));
#56041=CARTESIAN_POINT('Ctrl Pts',(-4.21455214323744,-3.49420598176206,
56.120100884122));
#56042=CARTESIAN_POINT('Ctrl Pts',(-2.02499693621566,-5.08638502468761,
56.259274341544));
#56043=CARTESIAN_POINT('Ctrl Pts',(0.659740989695028,-5.43476467177423,
56.3984477989659));
#56044=CARTESIAN_POINT('Ctrl Pts',(3.1831491223616,-4.45415389000624,56.5376212563878));
#56045=CARTESIAN_POINT('Ctrl Pts',(4.92816573805848,-2.38434638198303,56.6767947138099));
#56046=CARTESIAN_POINT('Ctrl Pts',(5.46807311844585,0.268517378169513,56.8159681712317));
#56047=CARTESIAN_POINT('Ctrl Pts',(4.6708449874405,2.85571922890732,56.9551416286539));
#56048=CARTESIAN_POINT('Ctrl Pts',(2.73143156270733,4.74459764672362,57.0943150860756));
#56049=CARTESIAN_POINT('Ctrl Pts',(0.124087395220497,5.47325566088379,57.2334885434978));
#56050=CARTESIAN_POINT('Ctrl Pts',(-2.51360048916101,4.86351085039795,57.3726620009195));
#56051=CARTESIAN_POINT('Ctrl Pts',(-4.53662496237246,3.06446719052892,57.5118354583416));
#56052=CARTESIAN_POINT('Ctrl Pts',(-5.45028564185634,0.516053905346834,
57.6510089157635));
#56053=CARTESIAN_POINT('Ctrl Pts',(-5.03116047135304,-2.15855264530281,
57.7901823731854));
#56054=CARTESIAN_POINT('Ctrl Pts',(-3.38174024369924,-4.30531742560222,
57.9293558306074));
#56055=CARTESIAN_POINT('Ctrl Pts',(-0.905366010090001,-5.39928121131163,
58.0685292880294));
#56056=CARTESIAN_POINT('Ctrl Pts',(1.7924019424173,-5.17293151780186,58.2077027454513));
#56057=CARTESIAN_POINT('Ctrl Pts',(4.05186480353684,-3.68161877778084,58.3468762028732));
#56058=CARTESIAN_POINT('Ctrl Pts',(5.32050471865464,-1.29002122068698,58.4860496602953));
#56059=CARTESIAN_POINT('Ctrl Pts',(5.28809476780659,1.41703173491132,58.6252231177171));
#56060=CARTESIAN_POINT('Ctrl Pts',(3.96256031981318,3.77757077007051,58.7643965751392));
#56061=CARTESIAN_POINT('Ctrl Pts',(1.66804100185088,5.21436136331128,58.903570032561));
#56062=CARTESIAN_POINT('Ctrl Pts',(-1.03437279918081,5.3760578608646,59.0427434899831));
#56063=CARTESIAN_POINT('Ctrl Pts',(-3.48384620021349,4.22311980226786,59.181916947405));
#56064=CARTESIAN_POINT('Ctrl Pts',(-5.08139711052062,2.037480948682,59.3210904048269));
#56065=CARTESIAN_POINT('Ctrl Pts',(-5.43636834480891,-0.646393402355297,
59.4602638622489));
#56066=CARTESIAN_POINT('Ctrl Pts',(-4.46195699598345,-3.17220191303188,
59.5994373196709));
#56067=CARTESIAN_POINT('Ctrl Pts',(-2.39644078802365,-4.92229588307611,
59.7386107770928));
#56068=CARTESIAN_POINT('Ctrl Pts',(0.255089178202091,-5.46871600306753,
59.8777842345147));
#56069=CARTESIAN_POINT('Ctrl Pts',(2.84424090051047,-4.67784340384815,60.0169576919367));
#56070=CARTESIAN_POINT('Ctrl Pts',(4.73787604345754,-2.74307415281825,60.1561311493586));
#56071=CARTESIAN_POINT('Ctrl Pts',(5.47293445031603,-0.137527137735913,
60.2953046067806));
#56072=CARTESIAN_POINT('Ctrl Pts',(4.86966857976191,2.50165008231294,60.4344780642026));
#56073=CARTESIAN_POINT('Ctrl Pts',(3.07559807920623,4.52908618444462,60.5736515216245));
#56074=CARTESIAN_POINT('Ctrl Pts',(0.529436060934367,5.44900198832429,60.7128249790465));
#56075=CARTESIAN_POINT('Ctrl Pts',(-2.1461916287808,5.03644584035882,60.8519984364684));
#56076=CARTESIAN_POINT('Ctrl Pts',(-4.29700024999853,3.39230217755033,60.9911718938904));
#56077=CARTESIAN_POINT('Ctrl Pts',(-5.39704171733157,0.918621745298845,
61.1303453513123));
#56078=CARTESIAN_POINT('Ctrl Pts',(-5.17731734062487,-1.77969389667896,
61.2695188087343));
#56079=CARTESIAN_POINT('Ctrl Pts',(-3.69155742920964,-4.04281201174977,
61.4086922661562));
#56080=CARTESIAN_POINT('Ctrl Pts',(-1.30308235372075,-5.31732090190619,
61.5478657235782));
#56081=CARTESIAN_POINT('Ctrl Pts',(1.40404202812768,-5.2915584882225,61.687039181));
#56082=CARTESIAN_POINT('Ctrl Pts',(3.76782892205851,-3.97182456202382,61.8262126384221));
#56083=CARTESIAN_POINT('Ctrl Pts',(5.21024960907278,-1.68084036193013,61.965386095844));
#56084=CARTESIAN_POINT('Ctrl Pts',(5.37858164549095,1.02116826789435,62.104559553266));
#56085=CARTESIAN_POINT('Ctrl Pts',(4.23166201667799,3.47346536196786,62.243733010688));
#56086=CARTESIAN_POINT('Ctrl Pts',(2.04995263487357,5.07637865165108,62.3829064681099));
#56087=CARTESIAN_POINT('Ctrl Pts',(-0.633041838628581,5.4379390494839,62.5220799255319));
#56088=CARTESIAN_POINT('Ctrl Pts',(-3.16123572883666,4.46973356166634,62.6612533829538));
#56089=CARTESIAN_POINT('Ctrl Pts',(-4.91639604752523,2.40852003127419,62.8004268403757));
#56090=CARTESIAN_POINT('Ctrl Pts',(-5.4693264952344,-0.241658050599369,
62.9396002977978));
#56091=CARTESIAN_POINT('Ctrl Pts',(-4.68481247433395,-2.83274813170046,
63.0787737552196));
#56092=CARTESIAN_POINT('Ctrl Pts',(-2.75470242334704,-4.73112058423557,
63.2179472126416));
#56093=CARTESIAN_POINT('Ctrl Pts',(-0.150961718488229,-5.47259055056005,
63.3571206700635));
#56094=CARTESIAN_POINT('Ctrl Pts',(2.48967613925437,-4.87577682760848,63.4962941274855));
#56095=CARTESIAN_POINT('Ctrl Pts',(4.52153658546732,-3.08674968495679,63.6354675849075));
#56096=CARTESIAN_POINT('Ctrl Pts',(5.44765327151243,-0.542738212792294,
63.7746410423294));
#56097=CARTESIAN_POINT('Ctrl Pts',(5.04176410147828,2.13366548356399,63.9138144997514));
#56098=CARTESIAN_POINT('Ctrl Pts',(3.40271563592693,4.2889787428324,64.0529879571733));
#56099=CARTESIAN_POINT('Ctrl Pts',(1.75568482074802,5.02557757704978,64.1457702621213));
#56100=CARTESIAN_POINT('Ctrl Pts',(0.893815385175997,5.17445361664725,64.1921614145953));
#56101=CARTESIAN_POINT('Ctrl Pts',(-2.43856727558399,5.02329722221656,-0.192161414595295));
#56102=CARTESIAN_POINT('Ctrl Pts',(-3.27525973866718,4.6171235936328,-0.145770262121311));
#56103=CARTESIAN_POINT('Ctrl Pts',(-4.7409061902274,3.37901548549523,-0.0529879571733427));
#56104=CARTESIAN_POINT('Ctrl Pts',(-5.78018190643871,0.693748699029605,
0.0861855002486099));
#56105=CARTESIAN_POINT('Ctrl Pts',(-5.40591960021603,-2.16040399080713,
0.225358957670562));
#56106=CARTESIAN_POINT('Ctrl Pts',(-3.7097635565088,-4.48663573945948,0.364532415092514));
#56107=CARTESIAN_POINT('Ctrl Pts',(-1.10641808766565,-5.71553783957422,
0.503705872514466));
#56108=CARTESIAN_POINT('Ctrl Pts',(1.76747397197042,-5.54688787644949,0.642879329936418));
#56109=CARTESIAN_POINT('Ctrl Pts',(4.20916255196555,-4.02177959155299,0.782052787358371));
#56110=CARTESIAN_POINT('Ctrl Pts',(5.62156037495095,-1.51323079903301,0.921226244780322));
#56111=CARTESIAN_POINT('Ctrl Pts',(5.65929121063359,1.36536905471062,1.06039970220228));
#56112=CARTESIAN_POINT('Ctrl Pts',(4.31312622178469,3.91008160895074,1.19957315962423));
#56113=CARTESIAN_POINT('Ctrl Pts',(1.91225111807969,5.4986456196878,1.33874661704618));
#56114=CARTESIAN_POINT('Ctrl Pts',(-0.95623660784315,5.74259630620146,1.47792007446813));
#56115=CARTESIAN_POINT('Ctrl Pts',(-3.59089086470998,4.58228184574727,1.61709353189008));
#56116=CARTESIAN_POINT('Ctrl Pts',(-5.34744651334115,2.3014384196533,1.75626698931204));
#56117=CARTESIAN_POINT('Ctrl Pts',(-5.79636405509312,-0.542187118398736,
1.89544044673399));
#56118=CARTESIAN_POINT('Ctrl Pts',(-4.82786746047639,-3.25322902643482,
2.03461390415594));
#56119=CARTESIAN_POINT('Ctrl Pts',(-2.67878806713384,-5.16874236244017,
2.17378736157789));
#56120=CARTESIAN_POINT('Ctrl Pts',(0.12534888559152,-5.82031707927296,2.31296081899985));
#56121=CARTESIAN_POINT('Ctrl Pts',(2.89883364474431,-5.04862027513358,2.4521342764218));
#56122=CARTESIAN_POINT('Ctrl Pts',(4.96345198432844,-3.04235888834433,2.59130773384375));
#56123=CARTESIAN_POINT('Ctrl Pts',(5.814332365256,-0.292134126616094,2.7304811912657));
#56124=CARTESIAN_POINT('Ctrl Pts',(5.24340471369441,2.52952766498078,2.86965464868766));
#56125=CARTESIAN_POINT('Ctrl Pts',(3.39028084955746,4.73263129387092,3.00882810610961));
#56126=CARTESIAN_POINT('Ctrl Pts',(0.708114501950619,5.7784407111682,3.14800156353156));
#56127=CARTESIAN_POINT('Ctrl Pts',(-2.14721065790853,5.41121886381668,3.28717502095351));
#56128=CARTESIAN_POINT('Ctrl Pts',(-4.47746756084426,3.72076436268896,3.42634847837546));
#56129=CARTESIAN_POINT('Ctrl Pts',(-5.71282672794544,1.1204525771617,3.56552193579742));
#56130=CARTESIAN_POINT('Ctrl Pts',(-5.55119954850806,-1.75384913087046,
3.70469539321937));
#56131=CARTESIAN_POINT('Ctrl Pts',(-4.03210953227885,-4.19927326103818,
3.84386885064132));
#56132=CARTESIAN_POINT('Ctrl Pts',(-1.52702742621441,-5.6178279112831,3.98304230806327));
#56133=CARTESIAN_POINT('Ctrl Pts',(1.35146640171921,-5.66262675497904,4.12221576548523));
#56134=CARTESIAN_POINT('Ctrl Pts',(3.89947933097964,-4.32271490483154,4.26138922290718));
#56135=CARTESIAN_POINT('Ctrl Pts',(5.49393290277561,-1.92574776670952,4.40056268032913));
#56136=CARTESIAN_POINT('Ctrl Pts',(5.74492733962891,0.942132190072912,4.53973613775108));
#56137=CARTESIAN_POINT('Ctrl Pts',(4.59108570538524,3.57962780844535,4.67890959517303));
#56138=CARTESIAN_POINT('Ctrl Pts',(2.31456271711773,5.34177897611984,4.81808305259498));
#56139=CARTESIAN_POINT('Ctrl Pts',(-0.527951971583234,5.7976779763013,4.95725651001694));
#56140=CARTESIAN_POINT('Ctrl Pts',(-3.24136390064256,4.835841526022,5.09642996743889));
#56141=CARTESIAN_POINT('Ctrl Pts',(-5.16214875924906,2.69147234586779,5.23560342486085));
#56142=CARTESIAN_POINT('Ctrl Pts',(-5.82060733370272,-0.111056148113278,
5.37477688228279));
#56143=CARTESIAN_POINT('Ctrl Pts',(-5.05572342622942,-2.88642752181006,
5.51395033970475));
#56144=CARTESIAN_POINT('Ctrl Pts',(-3.05453795830575,-4.95596620876867,
5.65312379712669));
#56145=CARTESIAN_POINT('Ctrl Pts',(-0.306410910327196,-5.81359747103461,
5.79229725454865));
#56146=CARTESIAN_POINT('Ctrl Pts',(2.51664434369428,-5.24960040846341,5.93147071197061));
#56147=CARTESIAN_POINT('Ctrl Pts',(4.72429185743747,-3.40189206867849,6.07064416939256));
#56148=CARTESIAN_POINT('Ctrl Pts',(5.77668444464111,-0.722301895490428,
6.20981762681451));
#56149=CARTESIAN_POINT('Ctrl Pts',(5.41647523561366,2.13391640491643,6.34899108423645));
#56150=CARTESIAN_POINT('Ctrl Pts',(3.7317480058439,4.46831735914848,6.48816454165842));
#56151=CARTESIAN_POINT('Ctrl Pts',(1.13447760591239,5.71005812254752,6.62733799908035));
#56152=CARTESIAN_POINT('Ctrl Pts',(-1.74021232753414,5.55548956045152,6.76651145650233));
#56153=CARTESIAN_POINT('Ctrl Pts',(-4.18935935946756,4.04240910329832,6.90568491392425));
#56154=CARTESIAN_POINT('Ctrl Pts',(-5.61406120784397,1.5408179502359,7.04485837134623));
#56155=CARTESIAN_POINT('Ctrl Pts',(-5.66592834067543,-1.33755719112062,
7.18403182876816));
#56156=CARTESIAN_POINT('Ctrl Pts',(-4.33227742625066,-3.88885272325741,
7.32320528619014));
#56157=CARTESIAN_POINT('Ctrl Pts',(-1.93923285223794,-5.48918747593746,
7.46237874361206));
#56158=CARTESIAN_POINT('Ctrl Pts',(0.928022116445518,-5.74722351684494,
7.60155220103404));
#56159=CARTESIAN_POINT('Ctrl Pts',(3.56834315422174,-4.59986199085434,7.74072565845597));
#56160=CARTESIAN_POINT('Ctrl Pts',(5.33607923473955,-2.32767300146927,7.87989911587794));
#56161=CARTESIAN_POINT('Ctrl Pts',(5.79895693428468,0.513713612335872,8.01907257329988));
#56162=CARTESIAN_POINT('Ctrl Pts',(4.84378643331985,3.22947924433246,8.15824603072184));
#56163=CARTESIAN_POINT('Ctrl Pts',(2.70414039420875,5.15552402085338,8.29741948814379));
#56164=CARTESIAN_POINT('Ctrl Pts',(-0.096762740512612,5.82086249392957,
8.43659294556575));
#56165=CARTESIAN_POINT('Ctrl Pts',(-2.8740039940344,5.06279608946103,8.57576640298769));
#56166=CARTESIAN_POINT('Ctrl Pts',(-4.94845054875377,3.06669861051362,8.71493986040966));
#56167=CARTESIAN_POINT('Ctrl Pts',(-5.81282752104771,0.320685845864631,
8.85411331783159));
#56168=CARTESIAN_POINT('Ctrl Pts',(-5.25576444825995,-2.50374584684515,
8.99328677525356));
#56169=CARTESIAN_POINT('Ctrl Pts',(-3.41348277450347,-4.71592393379662,
9.13246023267551));
#56170=CARTESIAN_POINT('Ctrl Pts',(-0.736484933562084,-5.77489334480071,
9.27163369009745));
#56171=CARTESIAN_POINT('Ctrl Pts',(2.12060928446497,-5.42169894625556,9.4108071475194));
#56172=CARTESIAN_POINT('Ctrl Pts',(4.45914021362855,-3.7427091466461,9.54998060494137));
#56173=CARTESIAN_POINT('Ctrl Pts',(5.7072550856607,-1.14849579380492,9.6891540623633));
#56174=CARTESIAN_POINT('Ctrl Pts',(5.5597460729518,1.72656503077199,9.82832751978527));
#56175=CARTESIAN_POINT('Ctrl Pts',(4.05268429870575,4.1794201961769,9.96750097720722));
#56176=CARTESIAN_POINT('Ctrl Pts',(1.5545991831692,5.610260651777,10.1066744346292));
#56177=CARTESIAN_POINT('Ctrl Pts',(-1.32363991509035,5.66919576098472,10.2458478920511));
#56178=CARTESIAN_POINT('Ctrl Pts',(-3.87820266586403,4.34181382416067,10.3850213494731));
#56179=CARTESIAN_POINT('Ctrl Pts',(-5.48440894945526,1.95270624424735,10.524194806895));
#56180=CARTESIAN_POINT('Ctrl Pts',(-5.74948503846692,-0.913906446871129,
10.663368264317));
#56181=CARTESIAN_POINT('Ctrl Pts',(-4.60861053928669,-3.55703698299067,
10.8025417217389));
#56182=CARTESIAN_POINT('Ctrl Pts',(-2.34076925001888,-5.33034731695352,
10.9417151791609));
#56183=CARTESIAN_POINT('Ctrl Pts',(0.499472155410101,-5.80020092472301,
11.0808886365829));
#56184=CARTESIAN_POINT('Ctrl Pts',(3.21757511435457,-4.8517021327235,11.2200620940048));
#56185=CARTESIAN_POINT('Ctrl Pts',(5.14886819479476,-2.71679213666018,11.3592355514268));
#56186=CARTESIAN_POINT('Ctrl Pts',(5.82108255452146,0.0824687494353655,
11.4984090088487));
#56187=CARTESIAN_POINT('Ctrl Pts',(5.06983822417648,2.86156313609655,11.6375824662707));
#56188=CARTESIAN_POINT('Ctrl Pts',(3.07884077061625,4.94090504972305,11.7767559236926));
#56189=CARTESIAN_POINT('Ctrl Pts',(0.334958847675559,5.81202251987648,11.9159293811145));
#56190=CARTESIAN_POINT('Ctrl Pts',(-2.49083225247991,5.26189679594663,12.0551028385365));
#56191=CARTESIAN_POINT('Ctrl Pts',(-4.70752757326881,3.42505289712457,12.1942762959584));
#56192=CARTESIAN_POINT('Ctrl Pts',(-5.77306742251802,0.75066353065058,12.3334497533804));
#56193=CARTESIAN_POINT('Ctrl Pts',(-5.42688996420728,-2.10728937679993,
12.4726232108023));
#56194=CARTESIAN_POINT('Ctrl Pts',(-3.75364771901881,-4.44993617962017,
12.6117966682243));
#56195=CARTESIAN_POINT('Ctrl Pts',(-1.16250705630058,-5.70441763418834,
12.7509701256463));
#56196=CARTESIAN_POINT('Ctrl Pts',(1.71290732287186,-5.56396906034169,12.8901435830682));
#56197=CARTESIAN_POINT('Ctrl Pts',(4.16945583110153,-4.06293505654238,13.0293170404902));
#56198=CARTESIAN_POINT('Ctrl Pts',(5.60642626599816,-1.56837104191373,13.1684904979121));
#56199=CARTESIAN_POINT('Ctrl Pts',(5.67242899620512,1.3097146575491,13.3076639553341));
#56200=CARTESIAN_POINT('Ctrl Pts',(4.35132404105704,3.86752922301908,13.446837412756));
#56201=CARTESIAN_POINT('Ctrl Pts',(1.96616786149375,5.47959735214338,13.586010870178));
#56202=CARTESIAN_POINT('Ctrl Pts',(-0.899785266466895,5.75171189085794,
13.7251843275999));
#56203=CARTESIAN_POINT('Ctrl Pts',(-3.54570936292791,4.61733129792882,13.8643577850219));
#56204=CARTESIAN_POINT('Ctrl Pts',(-5.32458325732504,2.35385138379666,14.0035312424438));
#56205=CARTESIAN_POINT('Ctrl Pts',(-5.80140994011502,-0.485227686681423,
14.1427046998658));
#56206=CARTESIAN_POINT('Ctrl Pts',(-4.85958857650155,-3.2056515824904,14.2818781572877));
#56207=CARTESIAN_POINT('Ctrl Pts',(-2.72942749693245,-5.14218132120763,
14.4210516147097));
#56208=CARTESIAN_POINT('Ctrl Pts',(0.068174261073915,-5.82126751415142,
14.5602250721316));
#56209=CARTESIAN_POINT('Ctrl Pts',(2.84910502301452,-5.07684978791188,14.6993985295536));
#56210=CARTESIAN_POINT('Ctrl Pts',(4.93332975717568,-3.09096436539676,14.8385719869756));
#56211=CARTESIAN_POINT('Ctrl Pts',(5.81118247237508,-0.349229829694178,
14.9777454443975));
#56212=CARTESIAN_POINT('Ctrl Pts',(5.26799741454557,2.47790363846716,15.1169189018194));
#56213=CARTESIAN_POINT('Ctrl Pts',(3.43660236677431,4.69910282648388,15.2560923592414));
#56214=CARTESIAN_POINT('Ctrl Pts',(0.764837601259375,5.77120668880326,15.3952658166634));
#56215=CARTESIAN_POINT('Ctrl Pts',(-2.09395676223998,5.43204825816717,15.5344392740853));
#56216=CARTESIAN_POINT('Ctrl Pts',(-4.4407053126234,3.76456365700274,15.6736127315073));
#56217=CARTESIAN_POINT('Ctrl Pts',(-5.70154578524018,1.17651130891186,15.8127861889292));
#56218=CARTESIAN_POINT('Ctrl Pts',(-5.56815849715669,-1.69923928618934,
15.9519596463512));
#56219=CARTESIAN_POINT('Ctrl Pts',(-4.07316131499641,-4.15946632432628,
16.0911331037731));
#56220=CARTESIAN_POINT('Ctrl Pts',(-1.5821334434256,-5.60255807362867,16.2303065611951));
#56221=CARTESIAN_POINT('Ctrl Pts',(1.29578150246575,-5.6756280268403,16.369480018617));
#56222=CARTESIAN_POINT('Ctrl Pts',(3.8568324590831,-4.36080801959346,16.508653476039));
#56223=CARTESIAN_POINT('Ctrl Pts',(5.47475271301557,-1.97961762280401,16.6478269334609));
#56224=CARTESIAN_POINT('Ctrl Pts',(5.75390406059017,0.885658660383087,16.7870003908829));
#56225=CARTESIAN_POINT('Ctrl Pts',(4.62602421419481,3.5343603623387,16.9261738483048));
#56226=CARTESIAN_POINT('Ctrl Pts',(2.36691932391769,5.31878709061123,17.0653473057268));
#56227=CARTESIAN_POINT('Ctrl Pts',(-0.470980292043627,5.80258397317041,
17.2045207631488));
#56228=CARTESIAN_POINT('Ctrl Pts',(-3.19370872063852,4.86744571709895,17.3436942205707));
#56229=CARTESIAN_POINT('Ctrl Pts',(-5.13546344041366,2.7420463988347,17.4828676779926));
#56230=CARTESIAN_POINT('Ctrl Pts',(-5.82141737170413,-0.0538793616236169,
17.6220411354146));
#56231=CARTESIAN_POINT('Ctrl Pts',(-5.08383073838774,-2.83662972991039,
17.7612145928365));
#56232=CARTESIAN_POINT('Ctrl Pts',(-3.10306932175022,-4.92572471679043,
17.9003880502585));
#56233=CARTESIAN_POINT('Ctrl Pts',(-0.363498705866874,-5.81030738360895,
18.0395615076804));
#56234=CARTESIAN_POINT('Ctrl Pts',(2.46496008276608,-5.2740662672702,18.1787349651024));
#56235=CARTESIAN_POINT('Ctrl Pts',(4.6906497442428,-3.4481311138097,18.3179084225244));
#56236=CARTESIAN_POINT('Ctrl Pts',(5.7693111548766,-0.779007059919226,18.4570818799463));
#56237=CARTESIAN_POINT('Ctrl Pts',(5.43717379703085,2.08061152118044,18.5962553373683));
#56238=CARTESIAN_POINT('Ctrl Pts',(3.77545689477508,4.43144766830016,18.7354287947902));
#56239=CARTESIAN_POINT('Ctrl Pts',(1.19050846719343,5.6986395561334,18.8746022522122));
#56240=CARTESIAN_POINT('Ctrl Pts',(-1.68556100314242,5.57231435813462,19.0137757096341));
#56241=CARTESIAN_POINT('Ctrl Pts',(-4.14945173608767,4.0833630124037,19.1529491670561));
#56242=CARTESIAN_POINT('Ctrl Pts',(-5.59865609799368,1.59588630471778,19.292122624478));
#56243=CARTESIAN_POINT('Ctrl Pts',(-5.67879283360018,-1.28184053385698,
19.4312960819));
#56244=CARTESIAN_POINT('Ctrl Pts',(-4.3702657025817,-3.84611243855737,19.5704695393219));
#56245=CARTESIAN_POINT('Ctrl Pts',(-1.99305544707629,-5.46987506128495,
19.7096429967438));
#56246=CARTESIAN_POINT('Ctrl Pts',(0.871526713802932,-5.75606153444484,
19.8488164541659));
#56247=CARTESIAN_POINT('Ctrl Pts',(3.52299004965729,-4.63468923566654,19.9879899115878));
#56248=CARTESIAN_POINT('Ctrl Pts',(5.31295885176283,-2.37997299158259,20.1271633690097));
#56249=CARTESIAN_POINT('Ctrl Pts',(5.80372301680978,0.456730057408082,20.2663368264317));
#56250=CARTESIAN_POINT('Ctrl Pts',(4.87527350713739,3.18174660081407,20.4055102838537));
#56251=CARTESIAN_POINT('Ctrl Pts',(2.75464876627528,5.12871459292147,20.5446837412756));
#56252=CARTESIAN_POINT('Ctrl Pts',(-0.0395841372822963,5.82153212627597,
20.6838571986975));
#56253=CARTESIAN_POINT('Ctrl Pts',(-2.82413733200982,5.09078103350911,20.8230306561195));
#56254=CARTESIAN_POINT('Ctrl Pts',(-4.91808997442551,3.11515556668409,20.9622041135414));
#56255=CARTESIAN_POINT('Ctrl Pts',(-5.80939725885485,0.377765390152733,
21.1013775709634));
#56256=CARTESIAN_POINT('Ctrl Pts',(-5.28010331752553,-2.45200166342593,
21.2405510283853));
#56257=CARTESIAN_POINT('Ctrl Pts',(-3.45963906871272,-4.68216837751742,
21.3797244858073));
#56258=CARTESIAN_POINT('Ctrl Pts',(-0.793171821188707,-5.76738083216808,
21.5188979432292));
#56259=CARTESIAN_POINT('Ctrl Pts',(2.06725373409271,-5.44226654989145,21.6580714006512));
#56260=CARTESIAN_POINT('Ctrl Pts',(4.42216330247374,-3.78632736664991,21.7972448580731));
#56261=CARTESIAN_POINT('Ctrl Pts',(5.6956989643925,-1.20449844674284,21.9364183154952));
#56262=CARTESIAN_POINT('Ctrl Pts',(5.57643661821572,1.67187255621067,22.075591772917));
#56263=CARTESIAN_POINT('Ctrl Pts',(4.0935400872484,4.13941212677331,22.214765230339));
#56264=CARTESIAN_POINT('Ctrl Pts',(1.60962954286109,5.59472036262192,22.353938687761));
#56265=CARTESIAN_POINT('Ctrl Pts',(-1.26789183578624,5.68192339740111,22.4931121451829));
#56266=CARTESIAN_POINT('Ctrl Pts',(-3.83536922608317,4.37969703299233,22.6322856026049));
#56267=CARTESIAN_POINT('Ctrl Pts',(-5.46496442636354,2.00648125328111,22.7714590600268));
#56268=CARTESIAN_POINT('Ctrl Pts',(-5.75818429941249,-0.857389511941446,
22.9106325174488));
#56269=CARTESIAN_POINT('Ctrl Pts',(-4.64332631009428,-3.51159849344621,
23.0498059748707));
#56270=CARTESIAN_POINT('Ctrl Pts',(-2.39301230807819,-5.30709857592394,
23.1889794322927));
#56271=CARTESIAN_POINT('Ctrl Pts',(0.442477068703314,-5.80482706416472,
23.3281528897146));
#56272=CARTESIAN_POINT('Ctrl Pts',(3.16976529514827,-4.88307189941549,23.4673263471366));
#56273=CARTESIAN_POINT('Ctrl Pts',(5.12193481942643,-2.76723452326229,23.6064998045585));
#56274=CARTESIAN_POINT('Ctrl Pts',(5.82161177717496,0.0252886742497559,
23.7456732619805));
#56275=CARTESIAN_POINT('Ctrl Pts',(5.0977006313659,2.81162790464161,23.8848467194024));
#56276=CARTESIAN_POINT('Ctrl Pts',(3.12722302731866,4.91042557611817,24.0240201768244));
#56277=CARTESIAN_POINT('Ctrl Pts',(0.39202979652405,5.80845210360083,24.1631936342463));
#56278=CARTESIAN_POINT('Ctrl Pts',(-2.43902845858562,5.28610852890829,24.3023670916683));
#56279=CARTESIAN_POINT('Ctrl Pts',(-4.67365877745015,3.47112616209074,24.4415405490902));
#56280=CARTESIAN_POINT('Ctrl Pts',(-5.76541573231747,0.807331799654702,
24.5807140065122));
#56281=CARTESIAN_POINT('Ctrl Pts',(-5.44732648603983,-2.05388348152386,
24.7198874639342));
#56282=CARTESIAN_POINT('Ctrl Pts',(-3.79717500707861,-4.41285227112865,
24.8590609213561));
#56283=CARTESIAN_POINT('Ctrl Pts',(-1.21848116320093,-5.69272402774911,
24.9982343787781));
#56284=CARTESIAN_POINT('Ctrl Pts',(1.65817402793505,-5.58052525254293,25.1374078362));
#56285=CARTESIAN_POINT('Ctrl Pts',(4.12934755692176,-4.10369247816303,25.276581293622));
#56286=CARTESIAN_POINT('Ctrl Pts',(5.5907508912458,-1.62336307498414,25.4157547510439));
#56287=CARTESIAN_POINT('Ctrl Pts',(5.68501969936585,1.25393549236386,25.5549282084659));
#56288=CARTESIAN_POINT('Ctrl Pts',(4.38910195395465,3.82460288644182,25.6941016658878));
#56289=CARTESIAN_POINT('Ctrl Pts',(2.01989496046113,5.46002083786238,25.8332751233098));
#56290=CARTESIAN_POINT('Ctrl Pts',(-0.843247140045628,5.76027234269287,
25.9724485807317));
#56291=CARTESIAN_POINT('Ctrl Pts',(-3.5001857623963,4.6519353853967,26.1116220381537));
#56292=CARTESIAN_POINT('Ctrl Pts',(-5.30120629843185,2.40603719477776,26.2507954955756));
#56293=CARTESIAN_POINT('Ctrl Pts',(-5.80589610857789,-0.428221411874423,
26.3899689529976));
#56294=CARTESIAN_POINT('Ctrl Pts',(-4.89084084690916,-3.15776487588807,
26.5291424104195));
#56295=CARTESIAN_POINT('Ctrl Pts',(-2.77980359390399,-5.11512416081038,
26.6683158678415));
#56296=CARTESIAN_POINT('Ctrl Pts',(0.0109930587272379,-5.82165632392082,
26.8074893252635));
#56297=CARTESIAN_POINT('Ctrl Pts',(2.79910152323723,-5.10458949023314,26.9466627826854));
#56298=CARTESIAN_POINT('Ctrl Pts',(4.90273156808454,-3.13927163088748,27.0858362401074));
#56299=CARTESIAN_POINT('Ctrl Pts',(5.80747192354612,-0.406291838966868,
27.2250096975293));
#56300=CARTESIAN_POINT('Ctrl Pts',(5.29208186520726,2.42604054647321,27.3641831549512));
#56301=CARTESIAN_POINT('Ctrl Pts',(3.48259232467691,4.66512099535361,27.5033566123732));
#56302=CARTESIAN_POINT('Ctrl Pts',(0.821486909932954,5.76341586717429,27.6425300697952));
#56303=CARTESIAN_POINT('Ctrl Pts',(-2.04050084409615,5.45235357496472,27.7817035272171));
#56304=CARTESIAN_POINT('Ctrl Pts',(-4.40351463041004,3.80799975065023,27.920876984639));
#56305=CARTESIAN_POINT('Ctrl Pts',(-5.68971476414206,1.23245653225239,28.0600504420611));
#56306=CARTESIAN_POINT('Ctrl Pts',(-5.58458023646188,-1.64446550091725,
28.1992238994829));
#56307=CARTESIAN_POINT('Ctrl Pts',(-4.11382012392897,-4.11925808722209,
28.338397356905));
#56308=CARTESIAN_POINT('Ctrl Pts',(-1.63708681827409,-5.58674770780111,
28.4775708143268));
#56309=CARTESIAN_POINT('Ctrl Pts',(1.23997158774619,-5.68808172082379,28.6167442717488));
#56310=CARTESIAN_POINT('Ctrl Pts',(3.81381348455404,-4.39848040875725,28.7559177291707));
#56311=CARTESIAN_POINT('Ctrl Pts',(5.45504432559113,-2.03329648773209,28.8950911865927));
#56312=CARTESIAN_POINT('Ctrl Pts',(5.76232565169517,0.829099683393584,29.0342646440147));
#56313=CARTESIAN_POINT('Ctrl Pts',(4.66051640966128,3.48875192532595,29.1734381014366));
#56314=CARTESIAN_POINT('Ctrl Pts',(2.4190475731416,5.29528205481685,29.3126115588586));
#56315=CARTESIAN_POINT('Ctrl Pts',(-0.413963172882623,5.80693014360295,
29.4517850162805));
#56316=CARTESIAN_POINT('Ctrl Pts',(-3.14574541539564,4.89858030277191,29.5909584737025));
#56317=CARTESIAN_POINT('Ctrl Pts',(-5.10828265814138,2.79235590240922,29.7301319311244));
#56318=CARTESIAN_POINT('Ctrl Pts',(-5.82166576624494,0.00330262308311963,
29.8693053885464));
#56319=CARTESIAN_POINT('Ctrl Pts',(-5.1114475685712,-2.78655826333045,30.0084788459683));
#56320=CARTESIAN_POINT('Ctrl Pts',(-3.15130130473782,-4.89500799671923,
30.1476523033903));
#56321=CARTESIAN_POINT('Ctrl Pts',(-0.420551431481474,-5.8064567246012,
30.2868257608123));
#56322=CARTESIAN_POINT('Ctrl Pts',(2.41303800540543,-5.29802329040337,30.4259992182342));
#56323=CARTESIAN_POINT('Ctrl Pts',(4.6565550827104,-3.4940374873306,30.5651726756561));
#56324=CARTESIAN_POINT('Ctrl Pts',(5.76138124879765,-0.835637066668541,
30.7043461330781));
#56325=CARTESIAN_POINT('Ctrl Pts',(5.4573477863529,2.02710590250649,30.8435195905));
#56326=CARTESIAN_POINT('Ctrl Pts',(3.81880153209184,4.39415043662375,30.9826930479221));
#56327=CARTESIAN_POINT('Ctrl Pts',(1.24642446962601,5.6866711917171,31.1218665053439));
#56328=CARTESIAN_POINT('Ctrl Pts',(-1.63074705781936,5.58860154552112,31.261039962766));
#56329=CARTESIAN_POINT('Ctrl Pts',(-4.10914377851356,4.12392296347676,31.4002134201878));
#56330=CARTESIAN_POINT('Ctrl Pts',(-5.58271083642691,1.65080068997717,31.5393868776098));
#56331=CARTESIAN_POINT('Ctrl Pts',(-5.69110944331103,-1.22600020613517,
31.6785603350318));
#56332=CARTESIAN_POINT('Ctrl Pts',(-4.40783234084832,-3.80300108547963,
31.8177337924537));
#56333=CARTESIAN_POINT('Ctrl Pts',(-2.04668575428317,-5.45003491955803,
31.9569072498757));
#56334=CARTESIAN_POINT('Ctrl Pts',(0.814947227294078,-5.76434421403799,
32.0960807072976));
#56335=CARTESIAN_POINT('Ctrl Pts',(3.47729705118092,-4.66906933114471,32.2352541647196));
#56336=CARTESIAN_POINT('Ctrl Pts',(5.28932588080193,-2.43204336471751,32.3744276221415));
#56337=CARTESIAN_POINT('Ctrl Pts',(5.8079291630047,0.399702437704683,32.5136010795635));
#56338=CARTESIAN_POINT('Ctrl Pts',(4.906290220335,3.13370698614799,32.6527745369854));
#56339=CARTESIAN_POINT('Ctrl Pts',(2.80489137308793,5.10141035267351,32.7919479944074));
#56340=CARTESIAN_POINT('Ctrl Pts',(0.0175982849787489,5.82164010409038,
32.9311214518293));
#56341=CARTESIAN_POINT('Ctrl Pts',(-2.77399820055673,5.11827482502606,33.0702949092513));
#56342=CARTESIAN_POINT('Ctrl Pts',(-4.88725490859519,3.16331197633109,33.2094683666733));
#56343=CARTESIAN_POINT('Ctrl Pts',(-5.80540651288768,0.434808488082928,
33.3486418240952));
#56344=CARTESIAN_POINT('Ctrl Pts',(-5.30393276867,-2.40002091378723,33.4878152815172));
#56345=CARTESIAN_POINT('Ctrl Pts',(-3.5054615810378,-4.64796109117274,33.6269887389391));
#56346=CARTESIAN_POINT('Ctrl Pts',(-0.849782184536431,-5.75931188945624,
33.766162196361));
#56347=CARTESIAN_POINT('Ctrl Pts',(2.013698737526,-5.46230909008945,33.905335653783));
#56348=CARTESIAN_POINT('Ctrl Pts',(4.38475974623548,-3.82958028626905,34.044509111205));
#56349=CARTESIAN_POINT('Ctrl Pts',(5.68359332882687,-1.26038489109569,34.1836825686269));
#56350=CARTESIAN_POINT('Ctrl Pts',(5.59258915547232,1.61701878136309,34.3228560260489));
#56351=CARTESIAN_POINT('Ctrl Pts',(4.13400093588665,4.09900469178505,34.4620294834708));
#56352=CARTESIAN_POINT('Ctrl Pts',(1.66450460739921,5.57864030146543,34.6012029408928));
#56353=CARTESIAN_POINT('Ctrl Pts',(-1.21202143177777,5.69410284857053,34.7403763983147));
#56354=CARTESIAN_POINT('Ctrl Pts',(-3.79216575441697,4.41715769383601,34.8795498557367));
#56355=CARTESIAN_POINT('Ctrl Pts',(-5.44499264996964,2.06006267937756,35.0187233131586));
#56356=CARTESIAN_POINT('Ctrl Pts',(-5.76632801754946,-0.80078985708593,
35.1578967705806));
#56357=CARTESIAN_POINT('Ctrl Pts',(-4.67759409827316,-3.46582120903368,
35.2970702280025));
#56358=CARTESIAN_POINT('Ctrl Pts',(-2.4450244911413,-5.28333781230264,35.4362436854245));
#56359=CARTESIAN_POINT('Ctrl Pts',(0.385439292332358,-5.80889316075911,
35.5754171428464));
#56360=CARTESIAN_POINT('Ctrl Pts',(3.12164966073643,-4.91397055310791,35.7145906002684));
#56361=CARTESIAN_POINT('Ctrl Pts',(5.09450728584655,-2.81740993035165,35.8537640576903));
#56362=CARTESIAN_POINT('Ctrl Pts',(5.82157933761185,-0.0318938407573063,
35.9929375151123));
#56363=CARTESIAN_POINT('Ctrl Pts',(5.12507121842963,2.76142141065283,36.1321109725343));
#56364=CARTESIAN_POINT('Ctrl Pts',(3.17530357324334,4.87947235046327,36.2712844299562));
#56365=CARTESIAN_POINT('Ctrl Pts',(0.449062922801674,5.8043212947383,36.4104578873782));
#56366=CARTESIAN_POINT('Ctrl Pts',(-2.38698935011123,5.3098102643732,36.5496313448001));
#56367=CARTESIAN_POINT('Ctrl Pts',(-4.63933907256208,3.51686453691161,36.6888048022221));
#56368=CARTESIAN_POINT('Ctrl Pts',(-5.75720780162824,0.863922178242041,
36.827978259644));
#56369=CARTESIAN_POINT('Ctrl Pts',(-5.46723745625785,-2.00027942999941,
36.967151717066));
#56370=CARTESIAN_POINT('Ctrl Pts',(-3.84033594818631,-4.37534261587085,
37.1063251744879));
#56371=CARTESIAN_POINT('Ctrl Pts',(-1.27433771248041,-5.68048119403081,
37.2454986319099));
#56372=CARTESIAN_POINT('Ctrl Pts',(1.60328075432964,-5.59654304227027,37.3846720893318));
#56373=CARTESIAN_POINT('Ctrl Pts',(4.08884088817506,-4.1440539803887,37.5238455467538));
#56374=CARTESIAN_POINT('Ctrl Pts',(5.5745361274619,-1.6781984879059,37.6630190041757));
#56375=CARTESIAN_POINT('Ctrl Pts',(5.69706191855208,1.19803534896567,37.8021924615977));
#56376=CARTESIAN_POINT('Ctrl Pts',(4.42645641148869,3.78130755670287,37.9413659190196));
#56377=CARTESIAN_POINT('Ctrl Pts',(2.07342718235268,5.43991754723071,38.0805393764416));
#56378=CARTESIAN_POINT('Ctrl Pts',(-0.786627658137758,5.76827705026729,
38.2197128338635));
#56379=CARTESIAN_POINT('Ctrl Pts',(-3.45432446808336,4.68609065964246,38.3588862912855));
#56380=CARTESIAN_POINT('Ctrl Pts',(-5.27731788542694,2.45799087413699,38.4980597487074));
#56381=CARTESIAN_POINT('Ctrl Pts',(-5.80982213105326,-0.371173822772242,
38.6372332061294));
#56382=CARTESIAN_POINT('Ctrl Pts',(-4.92162125477832,-3.10957351186651,
38.7764066635514));
#56383=CARTESIAN_POINT('Ctrl Pts',(-2.82991149871363,-5.08757349928589,
38.9155801209733));
#56384=CARTESIAN_POINT('Ctrl Pts',(-0.0461892042167428,-5.82148346717581,
39.0547535783952));
#56385=CARTESIAN_POINT('Ctrl Pts',(2.74882796945665,-5.1318367077997,39.1939270358172));
#56386=CARTESIAN_POINT('Ctrl Pts',(4.87166036925221,-3.18727602316538,39.3331004932391));
#56387=CARTESIAN_POINT('Ctrl Pts',(5.80320107669691,-0.463314649683628,
39.4722739506611));
#56388=CARTESIAN_POINT('Ctrl Pts',(5.31565574207175,2.37394339295762,39.611447408083));
#56389=CARTESIAN_POINT('Ctrl Pts',(3.52824628619234,4.63068907886911,39.750620865505));
#56390=CARTESIAN_POINT('Ctrl Pts',(0.878056962521374,5.75506899800126,39.8897943229269));
#56391=CARTESIAN_POINT('Ctrl Pts',(-1.98684806084503,5.47213285514013,40.0289677803489));
#56392=CARTESIAN_POINT('Ctrl Pts',(-4.36589910231502,3.85106845298709,40.1681412377708));
#56393=CARTESIAN_POINT('Ctrl Pts',(-5.67733480609507,1.28828284964488,40.3073146951929));
#56394=CARTESIAN_POINT('Ctrl Pts',(-5.6004631820731,-1.58953305955909,40.4464881526147));
#56395=CARTESIAN_POINT('Ctrl Pts',(-4.15408203636321,-4.07865242897112,
40.5856616100368));
#56396=CARTESIAN_POINT('Ctrl Pts',(-1.69188224892336,-5.57039833916441,
40.7248350674586));
#56397=CARTESIAN_POINT('Ctrl Pts',(1.18404204203471,-5.69998663541256,40.8640085248806));
#56398=CARTESIAN_POINT('Ctrl Pts',(3.77042655781207,-4.43572843773523,41.0031819823026));
#56399=CARTESIAN_POINT('Ctrl Pts',(5.43480964194405,-2.08677918262082,41.1423554397245));
#56400=CARTESIAN_POINT('Ctrl Pts',(5.77019130043884,0.772460715847387,41.2815288971464));
#56401=CARTESIAN_POINT('Ctrl Pts',(4.69455896401856,3.44280689765496,41.4207023545685));
#56402=CARTESIAN_POINT('Ctrl Pts',(2.47094243551778,5.27126613647471,41.5598758119903));
#56403=CARTESIAN_POINT('Ctrl Pts',(-0.356906115044386,5.81071606828552,
41.6990492694124));
#56404=CARTESIAN_POINT('Ctrl Pts',(-3.09747861235679,4.92924227921288,41.8382227268342));
#56405=CARTESIAN_POINT('Ctrl Pts',(-5.08060903480191,2.84239600279005,41.9773961842563));
#56406=CARTESIAN_POINT('Ctrl Pts',(-5.82135249336035,0.0604842891567615,
42.1165696416782));
#56407=CARTESIAN_POINT('Ctrl Pts',(-5.13857125234072,-2.736217952906,42.2557430991002));
#56408=CARTESIAN_POINT('Ctrl Pts',(-3.19922925390397,-4.86381901206784,
42.3949165565221));
#56409=CARTESIAN_POINT('Ctrl Pts',(-0.477563582791606,-5.80204586551837,
42.534090013944));
#56410=CARTESIAN_POINT('Ctrl Pts',(2.36088312099284,-5.32146916651771,42.673263471366));
#56411=CARTESIAN_POINT('Ctrl Pts',(4.62201116225283,-3.53960676024863,42.812436928788));
#56412=CARTESIAN_POINT('Ctrl Pts',(5.75289549147219,-0.892186452142408,
42.9516103862099));
#56413=CARTESIAN_POINT('Ctrl Pts',(5.47699525721726,1.97340471105329,43.0907838436319));
#56414=CARTESIAN_POINT('Ctrl Pts',(3.86177773595497,4.35642926251191,43.2299573010538));
#56415=CARTESIAN_POINT('Ctrl Pts',(1.30222021850063,5.67415418399216,43.3691307584758));
#56416=CARTESIAN_POINT('Ctrl Pts',(-1.57577577994933,5.60434955124256,43.5083042158977));
#56417=CARTESIAN_POINT('Ctrl Pts',(-4.06843937560915,4.16408504334153,43.6474776733197));
#56418=CARTESIAN_POINT('Ctrl Pts',(-5.56622696152361,1.70555580793924,43.7866511307416));
#56419=CARTESIAN_POINT('Ctrl Pts',(-5.70287698151609,-1.17004159536382,
43.9258245881636));
#56420=CARTESIAN_POINT('Ctrl Pts',(-4.44497371666576,-3.75952282335648,
44.0649980455855));
#56421=CARTESIAN_POINT('Ctrl Pts',(-2.10011859967,-5.4296689649101,44.2041715030075));
#56422=CARTESIAN_POINT('Ctrl Pts',(0.75828911564091,-5.77207075652127,44.3433449604294));
#56423=CARTESIAN_POINT('Ctrl Pts',(3.43126856719911,-4.70299896033786,44.4825184178514));
#56424=CARTESIAN_POINT('Ctrl Pts',(5.26518260193794,-2.483879097186,44.6216918752733));
#56425=CARTESIAN_POINT('Ctrl Pts',(5.81157496706545,0.342636255182992,44.7608653326952));
#56426=CARTESIAN_POINT('Ctrl Pts',(4.93683358045688,3.08536503513943,44.9000387901173));
#56427=CARTESIAN_POINT('Ctrl Pts',(2.85486336729942,5.0736139343903,45.0392122475392));
#56428=CARTESIAN_POINT('Ctrl Pts',(0.0747790093780736,5.82118641695523,
45.1783857049612));
#56429=CARTESIAN_POINT('Ctrl Pts',(-2.7235914370392,5.14527481144343,45.317559162383));
#56430=CARTESIAN_POINT('Ctrl Pts',(-4.85594832619352,3.21116319338118,45.4567326198051));
#56431=CARTESIAN_POINT('Ctrl Pts',(-5.8008556681686,0.491809636204625,45.595906077227));
#56432=CARTESIAN_POINT('Ctrl Pts',(-5.32725050265616,-2.34780861297027,
45.7350795346489));
#56433=CARTESIAN_POINT('Ctrl Pts',(-3.55094589057689,-4.61330537504105,
45.8742529920709));
#56434=CARTESIAN_POINT('Ctrl Pts',(-0.906310561904393,-5.75068729514726,
46.0134264494928));
#56435=CARTESIAN_POINT('Ctrl Pts',(1.95994946168753,-5.48182463316899,46.1525999069148));
#56436=CARTESIAN_POINT('Ctrl Pts',(4.34693315356459,-3.87246373251302,46.2917733643367));
#56437=CARTESIAN_POINT('Ctrl Pts',(5.67093934690125,-1.3161497350054,46.4309468217587));
#56438=CARTESIAN_POINT('Ctrl Pts',(5.60820212634388,1.56200899845666,46.5701202791807));
#56439=CARTESIAN_POINT('Ctrl Pts',(4.17406294100556,4.05820178967379,46.7092937366026));
#56440=CARTESIAN_POINT('Ctrl Pts',(1.71921908250202,5.56202201969288,46.8484671940246));
#56441=CARTESIAN_POINT('Ctrl Pts',(-1.15603409337561,5.70573293943389,46.9876406514465));
#56442=CARTESIAN_POINT('Ctrl Pts',(-3.74859641908543,4.45419219253138,47.1268141088685));
#56443=CARTESIAN_POINT('Ctrl Pts',(-5.42449554712695,2.11344535306392,47.2659875662903));
#56444=CARTESIAN_POINT('Ctrl Pts',(-5.77391540718154,-0.744112942972513,
47.4051610237125));
#56445=CARTESIAN_POINT('Ctrl Pts',(-4.71141059770752,-3.41970954629144,
47.5443344811342));
#56446=CARTESIAN_POINT('Ctrl Pts',(-2.49680078113419,-5.25906731850005,
47.6835079385564));
#56447=CARTESIAN_POINT('Ctrl Pts',(0.328364329234575,-5.81239882221393,
47.8226813959781));
#56448=CARTESIAN_POINT('Ctrl Pts',(3.07323285325868,-4.94439511273513,47.9618548534003));
#56449=CARTESIAN_POINT('Ctrl Pts',(5.06658824023115,-2.86731351706418,48.101028310822));
#56450=CARTESIAN_POINT('Ctrl Pts',(5.82098523896187,-0.0890732786842594,
48.2402017682442));
#56451=CARTESIAN_POINT('Ctrl Pts',(5.15194734468573,2.71094849799351,48.379375225666));
#56452=CARTESIAN_POINT('Ctrl Pts',(3.22307776963596,4.84804835908905,48.518548683088));
#56453=CARTESIAN_POINT('Ctrl Pts',(0.50605272401972,5.79963049182444,48.65772214051));
#56454=CARTESIAN_POINT('Ctrl Pts',(-2.33471994772851,5.33299971562592,48.7968955979319));
#56455=CARTESIAN_POINT('Ctrl Pts',(-4.60457176972921,3.56226360880274,48.9360690553539));
#56456=CARTESIAN_POINT('Ctrl Pts',(-5.74844442234177,0.920429206639673,
49.0752425127758));
#56457=CARTESIAN_POINT('Ctrl Pts',(-5.48662095387445,-1.94648239388221,
49.2144159701978));
#56458=CARTESIAN_POINT('Ctrl Pts',(-3.88312637822522,-4.33741083273409,
49.3535894276197));
#56459=CARTESIAN_POINT('Ctrl Pts',(-1.33007131516494,-5.66769031420763,
49.4927628850416));
#56460=CARTESIAN_POINT('Ctrl Pts',(1.54823279809409,-5.61202088414622,49.6319363424636));
#56461=CARTESIAN_POINT('Ctrl Pts',(4.04793973289715,-4.18401566918912,49.7711097998856));
#56462=CARTESIAN_POINT('Ctrl Pts',(5.55778353902781,-1.7328719902229,49.9102832573075));
#56463=CARTESIAN_POINT('Ctrl Pts',(5.70855449194466,1.14201962053459,50.0494567147295));
#56464=CARTESIAN_POINT('Ctrl Pts',(4.46338380974508,3.7376474108847,50.1886301721514));
#56465=CARTESIAN_POINT('Ctrl Pts',(2.12675936244259,5.41928941979025,50.3278036295734));
#56466=CARTESIAN_POINT('Ctrl Pts',(-0.729932283324382,5.77572524129643,
50.4669770869953));
#56467=CARTESIAN_POINT('Ctrl Pts',(-3.40812990463278,4.71979382540543,50.6061505444173));
#56468=CARTESIAN_POINT('Ctrl Pts',(-5.25292032303615,2.50970740944466,50.7453240018392));
#56469=CARTESIAN_POINT('Ctrl Pts',(-5.81318762876312,-0.31409042325878,
50.8844974592612));
#56470=CARTESIAN_POINT('Ctrl Pts',(-4.95192683045167,-3.06108213987153,
51.0236709166831));
#56471=CARTESIAN_POINT('Ctrl Pts',(-2.87974637700998,-5.05953199468938,
51.1628443741051));
#56472=CARTESIAN_POINT('Ctrl Pts',(-0.103367010880947,-5.8207489605934,
51.302017831527));
#56473=CARTESIAN_POINT('Ctrl Pts',(2.69828921200576,-5.15858881183226,51.4411912889491));
#56474=CARTESIAN_POINT('Ctrl Pts',(4.84011915839122,-3.2349729108235,51.5803647463709));
#56475=CARTESIAN_POINT('Ctrl Pts',(5.79837034387368,-0.520292760351136,
51.719538203793));
#56476=CARTESIAN_POINT('Ctrl Pts',(5.3387167707593,2.32161720419214,51.8587116612148));
#56477=CARTESIAN_POINT('Ctrl Pts',(3.57355984668041,4.59581039898092,51.9978851186368));
#56478=CARTESIAN_POINT('Ctrl Pts',(0.9345423012129,5.74616688658024,52.1370585760588));
#56479=CARTESIAN_POINT('Ctrl Pts',(-1.93300358884367,5.49138419041184,52.2762320334806));
#56480=CARTESIAN_POINT('Ctrl Pts',(-4.32786235743999,3.89376560879588,52.4154054909027));
#56481=CARTESIAN_POINT('Ctrl Pts',(-5.66440710550295,1.34398487503219,52.5545789483246));
#56482=CARTESIAN_POINT('Ctrl Pts',(-5.6158058016225,-1.53444726193202,52.6937524057466));
#56483=CARTESIAN_POINT('Ctrl Pts',(-4.1939431678773,-4.03765326715939,52.8329258631685));
#56484=CARTESIAN_POINT('Ctrl Pts',(-1.74651444877488,-5.55351154508642,
52.9720993205905));
#56485=CARTESIAN_POINT('Ctrl Pts',(1.12799826134796,-5.71134162203449,53.1112727780124));
#56486=CARTESIAN_POINT('Ctrl Pts',(3.72667586477672,-4.47254851288147,53.2504462354344));
#56487=CARTESIAN_POINT('Ctrl Pts',(5.41405061429276,-2.14006054752284,53.3896196928563));
#56488=CARTESIAN_POINT('Ctrl Pts',(5.77750024795265,0.715747222205316,53.5287931502783));
#56489=CARTESIAN_POINT('Ctrl Pts',(4.72814859288117,3.39652971204778,53.6679666077002));
#56490=CARTESIAN_POINT('Ctrl Pts',(2.52259890429111,5.24674165261229,53.8071400651222));
#56491=CARTESIAN_POINT('Ctrl Pts',(-0.29981462332651,5.81394138195658,53.9463135225441));
#56492=CARTESIAN_POINT('Ctrl Pts',(-3.04891296824617,4.95942868819059,54.0854869799661));
#56493=CARTESIAN_POINT('Ctrl Pts',(-5.05244524031375,2.89216187216734,54.2246604373881));
#56494=CARTESIAN_POINT('Ctrl Pts',(-5.82047758327454,0.117660119777667,
54.3638338948099));
#56495=CARTESIAN_POINT('Ctrl Pts',(-5.16519917283532,-2.68561365541081,
54.503007352232));
#56496=CARTESIAN_POINT('Ctrl Pts',(-3.2468485452167,-4.83216077191268,54.6421808096539));
#56497=CARTESIAN_POINT('Ctrl Pts',(-0.534529659332205,-5.79707523191495,
54.7813542670758));
#56498=CARTESIAN_POINT('Ctrl Pts',(2.30850046137003,-5.34440163358274,54.9205277244978));
#56499=CARTESIAN_POINT('Ctrl Pts',(4.58702131562675,-3.58483453609416,55.0597011819197));
#56500=CARTESIAN_POINT('Ctrl Pts',(5.74385470159609,-0.948649760522845,
55.1988746393417));
#56501=CARTESIAN_POINT('Ctrl Pts',(5.49611431405908,1.91951312784842,55.3380480967636));
#56502=CARTESIAN_POINT('Ctrl Pts',(3.904381360071,4.31828778525907,55.4772215541856));
#56503=CARTESIAN_POINT('Ctrl Pts',(1.3578903307091,5.66108974058479,55.6163950116076));
#56504=CARTESIAN_POINT('Ctrl Pts',(-1.52065247309652,5.61955685594985,55.7555684690295));
#56505=CARTESIAN_POINT('Ctrl Pts',(-4.02734245448736,4.2038453772078,55.8947419264515));
#56506=CARTESIAN_POINT('Ctrl Pts',(-5.54920606362863,1.76014637589462,56.0339153838734));
#56507=CARTESIAN_POINT('Ctrl Pts',(-5.7140943128971,-1.11397010036391,56.1730888412954));
#56508=CARTESIAN_POINT('Ctrl Pts',(-4.48168624667778,-3.71568184691945,
56.3122622987173));
#56509=CARTESIAN_POINT('Ctrl Pts',(-2.15334882809892,-5.40877916222438,
56.4514357561393));
#56510=CARTESIAN_POINT('Ctrl Pts',(0.701557845151013,-5.779240416447,56.5906092135613));
#56511=CARTESIAN_POINT('Ctrl Pts',(3.38490903848553,-4.73647484975552,56.7297826709831));
#56512=CARTESIAN_POINT('Ctrl Pts',(5.24053134448586,-2.53547518793791,56.8689561284052));
#56513=CARTESIAN_POINT('Ctrl Pts',(5.81466007724915,0.285537015520778,57.0081295858271));
#56514=CARTESIAN_POINT('Ctrl Pts',(4.96690064071577,3.03672541176262,57.1473030432491));
#56515=CARTESIAN_POINT('Ctrl Pts',(2.90455992767087,5.04532801983738,57.286476500671));
#56516=CARTESIAN_POINT('Ctrl Pts',(0.131952519187058,5.82017110864172,57.4256499580929));
#56517=CARTESIAN_POINT('Ctrl Pts',(-2.67292190464218,5.17177838783446,57.5648234155149));
#56518=CARTESIAN_POINT('Ctrl Pts',(-4.82417324764246,3.25870460120556,57.7039968729369));
#56519=CARTESIAN_POINT('Ctrl Pts',(-5.79574516375778,0.548763335114487,
57.8431703303588));
#56520=CARTESIAN_POINT('Ctrl Pts',(-5.35005426981655,-2.29536979835607,
57.9823437877808));
#56521=CARTESIAN_POINT('Ctrl Pts',(-3.59608760905766,-4.57820457266488,
58.1215172452027));
#56522=CARTESIAN_POINT('Ctrl Pts',(-0.962751499501605,-5.74150788133178,
58.2606907026247));
#56523=CARTESIAN_POINT('Ctrl Pts',(1.90601109224386,-5.50081129629358,58.3998641600466));
#56524=CARTESIAN_POINT('Ctrl Pts',(4.30868717392597,-3.91497356803764,58.5390376174686));
#56525=CARTESIAN_POINT('Ctrl Pts',(5.65773823945683,-1.37178759834585,58.6782110748905));
#56526=CARTESIAN_POINT('Ctrl Pts',(5.62327402450946,1.5068485147701,58.8173845323124));
#56527=CARTESIAN_POINT('Ctrl Pts',(4.21372223747032,4.01700735705519,58.9565579897345));
#56528=CARTESIAN_POINT('Ctrl Pts',(1.77376768938181,5.54486712061639,59.0957314471563));
#56529=CARTESIAN_POINT('Ctrl Pts',(-1.09993522217184,5.71681254793381,59.2349049045784));
#56530=CARTESIAN_POINT('Ctrl Pts',(-3.7046654236064,4.49079695603381,59.3740783620002));
#56531=CARTESIAN_POINT('Ctrl Pts',(-5.40347509537171,2.16662412404312,59.5132518194223));
#56532=CARTESIAN_POINT('Ctrl Pts',(-5.78094573628633,-0.687364237722812,
59.6524252768441));
#56533=CARTESIAN_POINT('Ctrl Pts',(-4.74477254582164,-3.37326795401793,
59.7915987342661));
#56534=CARTESIAN_POINT('Ctrl Pts',(-2.54833618274159,-5.23428943610499,
59.9307721916881));
#56535=CARTESIAN_POINT('Ctrl Pts',(0.271257685934548,-5.81534371030653,
60.06994564911));
#56536=CARTESIAN_POINT('Ctrl Pts',(3.02451954391174,-4.97434264297288,60.209119106532));
#56537=CARTESIAN_POINT('Ctrl Pts',(5.03818037617574,-2.91694046875862,60.3482925639539));
#56538=CARTESIAN_POINT('Ctrl Pts',(5.81982953854485,-0.146244122931207,
60.487466021376));
#56539=CARTESIAN_POINT('Ctrl Pts',(5.17832641715366,2.66021403623932,60.6266394787978));
#56540=CARTESIAN_POINT('Ctrl Pts',(3.2705410073059,4.81615663372771,60.7658129362198));
#56541=CARTESIAN_POINT('Ctrl Pts',(0.562993701855536,5.79438014745602,60.9049863936418));
#56542=CARTESIAN_POINT('Ctrl Pts',(-2.28222529429992,5.35567464531002,61.0441598510637));
#56543=CARTESIAN_POINT('Ctrl Pts',(-4.56936022331354,3.60731899784347,61.1833333084857));
#56544=CARTESIAN_POINT('Ctrl Pts',(-5.73912643983364,0.976847432866766,
61.3225067659076));
#56545=CARTESIAN_POINT('Ctrl Pts',(-5.50547510899733,-1.89249756295959,
61.4616802233296));
#56546=CARTESIAN_POINT('Ctrl Pts',(-3.92554216842628,-4.29906058228176,
61.6008536807515));
#56547=CARTESIAN_POINT('Ctrl Pts',(-1.38567659492106,-5.65435262047561,
61.7400271381735));
#56548=CARTESIAN_POINT('Ctrl Pts',(1.49303547170834,-5.62695728850115,61.8792005955955));
#56549=CARTESIAN_POINT('Ctrl Pts',(4.00664803422118,-4.22357368205809,62.0183740530173));
#56550=CARTESIAN_POINT('Ctrl Pts',(5.54049474799077,-1.78737832085199,62.1575475104394));
#56551=CARTESIAN_POINT('Ctrl Pts',(5.71949629948441,1.08589373822549,62.2967209678611));
#56552=CARTESIAN_POINT('Ctrl Pts',(4.49988060799419,3.69362660894395,62.4358944252834));
#56553=CARTESIAN_POINT('Ctrl Pts',(2.17988631242708,5.39813854777881,62.5750678827051));
#56554=CARTESIAN_POINT('Ctrl Pts',(-0.673166401869321,5.78261599810781,
62.7142413401272));
#56555=CARTESIAN_POINT('Ctrl Pts',(-3.36160669198678,4.75304201937018,62.853414797549));
#56556=CARTESIAN_POINT('Ctrl Pts',(-5.22801564687486,2.56118105368074,62.9925882549711));
#56557=CARTESIAN_POINT('Ctrl Pts',(-5.81599289775397,-0.256975243148529,
63.1317617123929));
#56558=CARTESIAN_POINT('Ctrl Pts',(-4.98175343925368,-3.0122983203602,63.270935169815));
#56559=CARTESIAN_POINT('Ctrl Pts',(-2.92930578263549,-5.03099673064092,
63.4101086272369));
#56560=CARTESIAN_POINT('Ctrl Pts',(-0.160530237740378,-5.81946384113401,
63.5492820846588));
#56561=CARTESIAN_POINT('Ctrl Pts',(2.64748113981279,-5.18482182863154,63.6884555420808));
#56562=CARTESIAN_POINT('Ctrl Pts',(4.80812851288484,-3.2823994436052,63.8276289995028));
#56563=CARTESIAN_POINT('Ctrl Pts',(5.79294594392005,-0.577138993930893,
63.9668024569247));
#56564=CARTESIAN_POINT('Ctrl Pts',(5.36132999774257,2.26890519507368,64.1059759143467));
#56565=CARTESIAN_POINT('Ctrl Pts',(3.61839250022299,4.56083028297295,64.2451493717686));
#56566=CARTESIAN_POINT('Ctrl Pts',(1.8669667018529,5.34411751075773,64.3379316767166));
#56567=CARTESIAN_POINT('Ctrl Pts',(0.950468752709476,5.50242987146594,64.3843228291906));
#56568=CARTESIAN_POINT('Ctrl Pts',(-2.58391981634373,5.3227144339337,-1.4432899320127E-14));
#56569=CARTESIAN_POINT('Ctrl Pts',(-3.47048393011347,4.89233053668302,0.0463911524739698));
#56570=CARTESIAN_POINT('Ctrl Pts',(-5.02349128318444,3.58042411219188,0.139173457421938));
#56571=CARTESIAN_POINT('Ctrl Pts',(-6.12471376929358,0.735100084764204,
0.278346914843891));
#56572=CARTESIAN_POINT('Ctrl Pts',(-5.72814329152084,-2.28917641069296,
0.417520372265842));
#56573=CARTESIAN_POINT('Ctrl Pts',(-3.93088665774734,-4.75406486094537,
0.556693829687795));
#56574=CARTESIAN_POINT('Ctrl Pts',(-1.17236692647549,-6.05621654674303,
0.695867287109747));
#56575=CARTESIAN_POINT('Ctrl Pts',(1.87282551798883,-5.87751408234647,0.835040744531699));
#56576=CARTESIAN_POINT('Ctrl Pts',(4.460052686318,-4.2615006309766,0.974214201953651));
#56577=CARTESIAN_POINT('Ctrl Pts',(5.95663748835038,-1.60342799949463,1.1133876593756));
#56578=CARTESIAN_POINT('Ctrl Pts',(5.99661729738974,1.44675285050091,1.25256111679755));
#56579=CARTESIAN_POINT('Ctrl Pts',(4.57021318478563,4.14314481049915,1.39173457421951));
#56580=CARTESIAN_POINT('Ctrl Pts',(2.02623220909413,5.82639631148172,1.53090803164146));
#56581=CARTESIAN_POINT('Ctrl Pts',(-1.01323377249359,6.0848878525618,1.67008148906341));
#56582=CARTESIAN_POINT('Ctrl Pts',(-3.80492847441726,4.85541202157831,1.80925494648536));
#56583=CARTESIAN_POINT('Ctrl Pts',(-5.66618487462113,2.43861729720475,1.94842840390732));
#56584=CARTESIAN_POINT('Ctrl Pts',(-6.14186046645374,-0.574504568081465,
2.08760186132927));
#56585=CARTESIAN_POINT('Ctrl Pts',(-5.11563594193564,-3.44714006157422,
2.22677531875122));
#56586=CARTESIAN_POINT('Ctrl Pts',(-2.83845913941177,-5.47682893541894,
2.36594877617318));
#56587=CARTESIAN_POINT('Ctrl Pts',(0.132820395270488,-6.16724122771442,
2.50512223359512));
#56588=CARTESIAN_POINT('Ctrl Pts',(3.07162069053227,-5.34954688547102,2.64429569101708));
#56589=CARTESIAN_POINT('Ctrl Pts',(5.25930207798151,-3.22370085858687,2.78346914843903));
#56590=CARTESIAN_POINT('Ctrl Pts',(6.16089979055235,-0.309546989476669,
2.92264260586099));
#56591=CARTESIAN_POINT('Ctrl Pts',(5.55594158934163,2.68030196459035,3.06181606328293));
#56592=CARTESIAN_POINT('Ctrl Pts',(3.5923609563094,5.01472315573198,3.20098952070489));
#56593=CARTESIAN_POINT('Ctrl Pts',(0.750322171608787,6.1228687888378,3.34016297812684));
#56594=CARTESIAN_POINT('Ctrl Pts',(-2.27519667978226,5.7337584215059,3.47933643554879));
#56595=CARTESIAN_POINT('Ctrl Pts',(-4.74435020650838,3.94254317482165,3.61850989297074));
#56596=CARTESIAN_POINT('Ctrl Pts',(-6.05334383737304,1.18723795172224,3.7576833503927));
#56597=CARTESIAN_POINT('Ctrl Pts',(-5.88208275469158,-1.85838855852283,
3.89685680781465));
#56598=CARTESIAN_POINT('Ctrl Pts',(-4.27244629518299,-4.44957393715546,
4.0360302652366));
#56599=CARTESIAN_POINT('Ctrl Pts',(-1.61804698447391,-5.95268254852498,
4.17520372265855));
#56600=CARTESIAN_POINT('Ctrl Pts',(1.43202151996764,-6.0001516592336,4.3143771800805));
#56601=CARTESIAN_POINT('Ctrl Pts',(4.13191057619189,-4.58037340812065,4.45355063750246));
#56602=CARTESIAN_POINT('Ctrl Pts',(5.82140268971859,-2.04053333508643,4.59272409492441));
#56603=CARTESIAN_POINT('Ctrl Pts',(6.08735782889834,0.998288650848016,4.73189755234636));
#56604=CARTESIAN_POINT('Ctrl Pts',(4.86474064154572,3.79299407565527,4.87107100976832));
#56605=CARTESIAN_POINT('Ctrl Pts',(2.45252387777502,5.66017951980371,5.01024446719026));
#56606=CARTESIAN_POINT('Ctrl Pts',(-0.559420925192705,6.14325270487215,
5.14941792461222));
#56607=CARTESIAN_POINT('Ctrl Pts',(-3.43456770650121,5.12408530734228,5.28859138203417));
#56608=CARTESIAN_POINT('Ctrl Pts',(-5.46984231580947,2.85189947362147,5.42776483945613));
#56609=CARTESIAN_POINT('Ctrl Pts',(-6.16754878296635,-0.117675728986478,
5.56693829687808));
#56610=CARTESIAN_POINT('Ctrl Pts',(-5.35707342495131,-3.05847509179701,
5.70611175430003));
#56611=CARTESIAN_POINT('Ctrl Pts',(-3.23660587069502,-5.25137010743336,
5.84528521172199));
#56612=CARTESIAN_POINT('Ctrl Pts',(-0.324674751057878,-6.16012109243705,
5.98445866914392));
#56613=CARTESIAN_POINT('Ctrl Pts',(2.66665072375488,-5.56250658291383,6.12363212656589));
#56614=CARTESIAN_POINT('Ctrl Pts',(5.00588664124526,-3.60466427042304,6.26280558398783));
#56615=CARTESIAN_POINT('Ctrl Pts',(6.12100783879243,-0.765355214853815,
6.4019790414098));
#56616=CARTESIAN_POINT('Ctrl Pts',(5.73932810309077,2.26111001336394,6.54115249883174));
#56617=CARTESIAN_POINT('Ctrl Pts',(3.95418150585638,4.73465460051793,6.6803259562537));
#56618=CARTESIAN_POINT('Ctrl Pts',(1.20209895230915,6.05041020727682,6.81949941367564));
#56619=CARTESIAN_POINT('Ctrl Pts',(-1.84393892380284,5.886628475855,6.9586728710976));
#56620=CARTESIAN_POINT('Ctrl Pts',(-4.43906911041475,4.28335977947497,7.09784632851955));
#56621=CARTESIAN_POINT('Ctrl Pts',(-5.94869132804232,1.63265950251008,7.2370197859415));
#56622=CARTESIAN_POINT('Ctrl Pts',(-6.00365003829891,-1.41728324095633,
7.37619324336345));
#56623=CARTESIAN_POINT('Ctrl Pts',(-4.59050591044546,-4.12065056194135,
7.51536670078541));
#56624=CARTESIAN_POINT('Ctrl Pts',(-2.05482220875044,-5.81637440833104,
7.65454015820736));
#56625=CARTESIAN_POINT('Ctrl Pts',(0.983337536223896,-6.08979087139413,
7.79371361562931));
#56626=CARTESIAN_POINT('Ctrl Pts',(3.78103679157256,-4.87404004376625,7.93288707305127));
#56627=CARTESIAN_POINT('Ctrl Pts',(5.65414004127548,-2.4664156099708,8.07206053047321));
#56628=CARTESIAN_POINT('Ctrl Pts',(6.14460789605782,0.544333878392784,8.21123398789517));
#56629=CARTESIAN_POINT('Ctrl Pts',(5.13250377650304,3.42197465677996,8.35040744531711));
#56630=CARTESIAN_POINT('Ctrl Pts',(2.86532261001403,5.46282270515937,8.48958090273908));
#56631=CARTESIAN_POINT('Ctrl Pts',(-0.102530352636915,6.16781915220042,
8.62875436016102));
#56632=CARTESIAN_POINT('Ctrl Pts',(-3.04531105079234,5.36456765931648,8.76792781758298));
#56633=CARTESIAN_POINT('Ctrl Pts',(-5.24340647114583,3.24949136724629,8.90710127500493));
#56634=CARTESIAN_POINT('Ctrl Pts',(-6.15930524903233,0.339800554303714,
9.04627473242688));
#56635=CARTESIAN_POINT('Ctrl Pts',(-5.56903803469641,-2.65298340280655,
9.18544818984883));
#56636=CARTESIAN_POINT('Ctrl Pts',(-3.61694584853098,-4.99701994155083,
9.32462164727079));
#56637=CARTESIAN_POINT('Ctrl Pts',(-0.780383643019917,-6.11910997916929,
9.46379510469274));
#56638=CARTESIAN_POINT('Ctrl Pts',(2.24700971251217,-5.74486317672912,9.60296856211469));
#56639=CARTESIAN_POINT('Ctrl Pts',(4.72493044469749,-3.96579599326958,9.74214201953664));
#56640=CARTESIAN_POINT('Ctrl Pts',(6.04744009337826,-1.21695270428369,9.8813154769586));
#56641=CARTESIAN_POINT('Ctrl Pts',(5.89113870081706,1.8294781701889,10.0204889343805));
#56642=CARTESIAN_POINT('Ctrl Pts',(4.2942474352292,4.42853751621115,10.1596623918025));
#56643=CARTESIAN_POINT('Ctrl Pts',(1.64726217565612,5.94466423712179,10.2988358492245));
#56644=CARTESIAN_POINT('Ctrl Pts',(-1.40253641576754,6.00711221552488,10.4380093066464));
#56645=CARTESIAN_POINT('Ctrl Pts',(-4.1093657002853,4.60061073215078,10.5771827640684));
#56646=CARTESIAN_POINT('Ctrl Pts',(-5.81131105437156,2.06909869189489,10.7163562214903));
#56647=CARTESIAN_POINT('Ctrl Pts',(-6.09218719262449,-0.968380492102368,
10.8555296789123));
#56648=CARTESIAN_POINT('Ctrl Pts',(-4.88331005566418,-3.76905670794581,
10.9947031363342));
#56649=CARTESIAN_POINT('Ctrl Pts',(-2.4802924697507,-5.64806646844389,11.1338765937562));
#56650=CARTESIAN_POINT('Ctrl Pts',(0.529243549275131,-6.14592603543298,
11.2730500511781));
#56651=CARTESIAN_POINT('Ctrl Pts',(3.40936097264904,-5.14089129681224,11.4122235086001));
#56652=CARTESIAN_POINT('Ctrl Pts',(5.455770153844,-2.87872846859289,11.551396966022));
#56653=CARTESIAN_POINT('Ctrl Pts',(6.16805232966076,0.0873843580322454,
11.690570423444));
#56654=CARTESIAN_POINT('Ctrl Pts',(5.37202954549153,3.03212864664881,11.8297438808659));
#56655=CARTESIAN_POINT('Ctrl Pts',(3.2623572694572,5.23541121726669,11.9689173382879));
#56656=CARTESIAN_POINT('Ctrl Pts',(0.354924308561887,6.15845226519246,12.1080907957098));
#56657=CARTESIAN_POINT('Ctrl Pts',(-2.63930008444389,5.57553590533831,12.2472642531318));
#56658=CARTESIAN_POINT('Ctrl Pts',(-4.98812310996854,3.62920561655853,12.3864377105538));
#56659=CARTESIAN_POINT('Ctrl Pts',(-6.11717522148735,0.795407365494881,
12.5256111679757));
#56660=CARTESIAN_POINT('Ctrl Pts',(-5.75036360900621,-2.23289586225585,
12.6647846253977));
#56661=CARTESIAN_POINT('Ctrl Pts',(-3.97738656704597,-4.71517779768107,
12.8039580828196));
#56662=CARTESIAN_POINT('Ctrl Pts',(-1.23179911806814,-6.04443351358825,
12.9431315402416));
#56663=CARTESIAN_POINT('Ctrl Pts',(1.81500638487368,-5.89561340238062,13.0823049976635));
#56664=CARTESIAN_POINT('Ctrl Pts',(4.4179792180525,-4.30510919679378,13.2214784550855));
#56665=CARTESIAN_POINT('Ctrl Pts',(5.94060130004532,-1.6618549158582,13.3606519125074));
#56666=CARTESIAN_POINT('Ctrl Pts',(6.01053817003534,1.38778113332413,13.4998253699294));
#56667=CARTESIAN_POINT('Ctrl Pts',(4.61068781230449,4.09805605927116,13.6389988273513));
#56668=CARTESIAN_POINT('Ctrl Pts',(2.08336269843318,5.80621265837202,13.7781722847733));
#56669=CARTESIAN_POINT('Ctrl Pts',(-0.953417608674055,6.09454677813966,
13.9173457421952));
#56670=CARTESIAN_POINT('Ctrl Pts',(-3.75705389701448,4.89255062134165,14.0565191996172));
#56671=CARTESIAN_POINT('Ctrl Pts',(-5.64195883793242,2.49415437343771,14.1956926570391));
#56672=CARTESIAN_POINT('Ctrl Pts',(-6.14720711504926,-0.514150028833914,
14.3348661144611));
#56673=CARTESIAN_POINT('Ctrl Pts',(-5.14924781769343,-3.39672673016858,
14.474039571883));
#56674=CARTESIAN_POINT('Ctrl Pts',(-2.89211696852113,-5.44868470439008,
14.613213029305));
#56675=CARTESIAN_POINT('Ctrl Pts',(0.0722378365023835,-6.16824831394129,
14.7523864867269));
#56676=CARTESIAN_POINT('Ctrl Pts',(3.01892795885593,-5.37945903848149,14.8915599441489));
#56677=CARTESIAN_POINT('Ctrl Pts',(5.2273843940071,-3.27520349974674,15.0307334015708));
#56678=CARTESIAN_POINT('Ctrl Pts',(6.15756214606091,-0.370045922636593,
15.1699068589928));
#56679=CARTESIAN_POINT('Ctrl Pts',(5.58200015565758,2.62560085117693,15.3090803164147));
#56680=CARTESIAN_POINT('Ctrl Pts',(3.64144350057961,4.97919620014604,15.4482537738367));
#56681=CARTESIAN_POINT('Ctrl Pts',(0.810426291686102,6.11520357741311,15.5874272312586));
#56682=CARTESIAN_POINT('Ctrl Pts',(-2.21876854770109,5.7558293667546,15.7266006886806));
#56683=CARTESIAN_POINT('Ctrl Pts',(-4.70539671827687,3.98895315729471,15.8657741461025));
#56684=CARTESIAN_POINT('Ctrl Pts',(-6.04139048603638,1.24663810413905,16.0049476035245));
#56685=CARTESIAN_POINT('Ctrl Pts',(-5.90005255356337,-1.80052365512164,
16.1441210609464));
#56686=CARTESIAN_POINT('Ctrl Pts',(-4.31594499867261,-4.40739427960503,
16.2832945183684));
#56687=CARTESIAN_POINT('Ctrl Pts',(-1.67643763512254,-5.93650254131226,
16.4224679757903));
#56688=CARTESIAN_POINT('Ctrl Pts',(1.37301748259998,-6.01392788117193,16.5616414332123));
#56689=CARTESIAN_POINT('Ctrl Pts',(4.08672170709572,-4.62073709014209,16.7008148906342));
#56690=CARTESIAN_POINT('Ctrl Pts',(5.80107925107558,-2.09761414235381,16.8399883480562));
#56691=CARTESIAN_POINT('Ctrl Pts',(6.09686961371142,0.938448976164669,16.9791618054781));
#56692=CARTESIAN_POINT('Ctrl Pts',(4.90176168507831,3.74502843115517,17.1183352629001));
#56693=CARTESIAN_POINT('Ctrl Pts',(2.50800123744496,5.63581718656992,17.257508720322));
#56694=CARTESIAN_POINT('Ctrl Pts',(-0.499053408082674,6.14845112718181,
17.396682177744));
#56695=CARTESIAN_POINT('Ctrl Pts',(-3.38407200552272,5.15757328875699,17.5358556351659));
#56696=CARTESIAN_POINT('Ctrl Pts',(-5.44156639952264,2.90548802906646,17.6750290925879));
#56697=CARTESIAN_POINT('Ctrl Pts',(-6.16840710386026,-0.057090879380428,
17.8142025500099));
#56698=CARTESIAN_POINT('Ctrl Pts',(-5.38685609348673,-3.00570906701349,
17.9533760074318));
#56699=CARTESIAN_POINT('Ctrl Pts',(-3.2880299806525,-5.21932604976855,18.0925494648538));
#56700=CARTESIAN_POINT('Ctrl Pts',(-0.385165305344935,-6.15663489700508,
18.2317229222757));
#56701=CARTESIAN_POINT('Ctrl Pts',(2.61188578561166,-5.58843074667496,18.3708963796977));
#56702=CARTESIAN_POINT('Ctrl Pts',(4.97023926591231,-3.65365942680015,18.5100698371196));
#56703=CARTESIAN_POINT('Ctrl Pts',(6.11319505883557,-0.825440331029876,
18.6492432945416));
#56704=CARTESIAN_POINT('Ctrl Pts',(5.7612604170159,2.20462785403522,18.7884167519635));
#56705=CARTESIAN_POINT('Ctrl Pts',(4.00049569426957,4.69558726546455,18.9275902093855));
#56706=CARTESIAN_POINT('Ctrl Pts',(1.26146957301766,6.03831102907202,19.0667636668074));
#56707=CARTESIAN_POINT('Ctrl Pts',(-1.78603006826333,5.90445612759732,19.2059371242294));
#56708=CARTESIAN_POINT('Ctrl Pts',(-4.39678276469571,4.32675477552601,19.3451105816513));
#56709=CARTESIAN_POINT('Ctrl Pts',(-5.93236798563808,1.69101024551557,19.4842840390733));
#56710=CARTESIAN_POINT('Ctrl Pts',(-6.01728132849471,-1.35824555261966,
19.6234574964952));
#56711=CARTESIAN_POINT('Ctrl Pts',(-4.63075850506662,-4.07536271210495,
19.7626309539172));
#56712=CARTESIAN_POINT('Ctrl Pts',(-2.11185293772081,-5.79591086343658,
19.9018044113391));
#56713=CARTESIAN_POINT('Ctrl Pts',(0.92347468483484,-6.09915568533313,20.0409778687611));
#56714=CARTESIAN_POINT('Ctrl Pts',(3.73298038288122,-4.9109431913316,20.1801513261831));
#56715=CARTESIAN_POINT('Ctrl Pts',(5.62964155139038,-2.52183297827614,20.319324783605));
#56716=CARTESIAN_POINT('Ctrl Pts',(6.14965806432926,0.483953778053599,20.458498241027));
#56717=CARTESIAN_POINT('Ctrl Pts',(5.16586765980059,3.3713968750191,20.5976716984489));
#56718=CARTESIAN_POINT('Ctrl Pts',(2.91884156960177,5.43441528216485,20.7368451558709));
#56719=CARTESIAN_POINT('Ctrl Pts',(-0.0419435780020967,6.16852869846015,
20.8760186132928));
#56720=CARTESIAN_POINT('Ctrl Pts',(-2.99247205083102,5.39422066590322,21.0151920707148));
#56721=CARTESIAN_POINT('Ctrl Pts',(-5.21123623314264,3.30083663483117,21.1543655281367));
#56722=CARTESIAN_POINT('Ctrl Pts',(-6.15567052361625,0.400282365517453,
21.2935389855587));
#56723=CARTESIAN_POINT('Ctrl Pts',(-5.59482763961418,-2.5981549704495,21.4327124429806));
#56724=CARTESIAN_POINT('Ctrl Pts',(-3.66585332155845,-4.96125236127746,
21.5718859004026));
#56725=CARTESIAN_POINT('Ctrl Pts',(-0.840449392991975,-6.11114967786599,
21.7110593578245));
#56726=CARTESIAN_POINT('Ctrl Pts',(2.19047386652622,-5.76665672704107,21.8502328152465));
#56727=CARTESIAN_POINT('Ctrl Pts',(4.68574949839482,-4.01201410836936,21.9894062726684));
#56728=CARTESIAN_POINT('Ctrl Pts',(6.03519516126426,-1.27629343527068,22.1285797300904));
#56729=CARTESIAN_POINT('Ctrl Pts',(5.90882409792905,1.7715257116946,22.2677531875123));
#56730=CARTESIAN_POINT('Ctrl Pts',(4.33753846217141,4.38614473731157,22.4069266449343));
#56731=CARTESIAN_POINT('Ctrl Pts',(1.70557265916508,5.92819765795395,22.5461001023563));
#56732=CARTESIAN_POINT('Ctrl Pts',(-1.34346543245728,6.02059849178258,22.6852735597782));
#56733=CARTESIAN_POINT('Ctrl Pts',(-4.06397914279307,4.64075199664936,22.8244470172002));
#56734=CARTESIAN_POINT('Ctrl Pts',(-5.79070752662021,2.12607899867485,22.9636204746221));
#56735=CARTESIAN_POINT('Ctrl Pts',(-6.10140497921985,-0.908494824978891,
23.102793932044));
#56736=CARTESIAN_POINT('Ctrl Pts',(-4.92009508473742,-3.72090982484188,
23.241967389466));
#56737=CARTESIAN_POINT('Ctrl Pts',(-2.53564951252636,-5.62343196963269,
23.3811408468879));
#56738=CARTESIAN_POINT('Ctrl Pts',(0.468851229797039,-6.15082791921381,
23.5203143043099));
#56739=CARTESIAN_POINT('Ctrl Pts',(3.35870141508839,-5.1741308808094,23.6594877617318));
#56740=CARTESIAN_POINT('Ctrl Pts',(5.42723139543778,-2.93217750960558,23.7986612191538));
#56741=CARTESIAN_POINT('Ctrl Pts',(6.16861309700777,0.0267960237051835,
23.9378346765757));
#56742=CARTESIAN_POINT('Ctrl Pts',(5.4015527113228,2.97921699012736,24.0770081339977));
#56743=CARTESIAN_POINT('Ctrl Pts',(3.31362338505898,5.20311499291073,24.2161815914197));
#56744=CARTESIAN_POINT('Ctrl Pts',(0.415397011998718,6.15466903170957,24.3553550488416));
#56745=CARTESIAN_POINT('Ctrl Pts',(-2.58440848848693,5.60119079590215,24.4945285062636));
#56746=CARTESIAN_POINT('Ctrl Pts',(-4.95223554043221,3.67802511132568,24.6337019636856));
#56747=CARTESIAN_POINT('Ctrl Pts',(-6.10906744683801,0.855453387068176,
24.7728754211075));
#56748=CARTESIAN_POINT('Ctrl Pts',(-5.77201826429046,-2.1763066705222,24.9120488785295));
#56749=CARTESIAN_POINT('Ctrl Pts',(-4.0235083301384,-4.67588347638917,25.0512223359514));
#56750=CARTESIAN_POINT('Ctrl Pts',(-1.29110960151063,-6.03204290140159,
25.1903957933733));
#56751=CARTESIAN_POINT('Ctrl Pts',(1.7570106728763,-5.91315643821987,25.3295692507953));
#56752=CARTESIAN_POINT('Ctrl Pts',(4.37548026159963,-4.34829599358349,25.4687427082172));
#56753=CARTESIAN_POINT('Ctrl Pts',(5.92399158340687,-1.72012478826007,25.6079161656392));
#56754=CARTESIAN_POINT('Ctrl Pts',(6.02387935103308,1.32867721123663,25.7470896230612));
#56755=CARTESIAN_POINT('Ctrl Pts',(4.65071750462981,4.05257106780277,25.8862630804831));
#56756=CARTESIAN_POINT('Ctrl Pts',(2.14029223943311,5.78546927200246,26.0254365379051));
#56757=CARTESIAN_POINT('Ctrl Pts',(-0.893509486925035,6.1036174818084,26.164609995327));
#56758=CARTESIAN_POINT('Ctrl Pts',(-3.70881682982232,4.92921731011009,26.303783452749));
#56759=CARTESIAN_POINT('Ctrl Pts',(-5.61718847874047,2.54945075688227,26.4429569101709));
#56760=CARTESIAN_POINT('Ctrl Pts',(-6.15196068478126,-0.453745854380916,
26.5821303675929));
#56761=CARTESIAN_POINT('Ctrl Pts',(-5.18236290195643,-3.34598570228385,
26.7213038250148));
#56762=CARTESIAN_POINT('Ctrl Pts',(-2.94549576866256,-5.42001478266002,
26.8604772824367));
#56763=CARTESIAN_POINT('Ctrl Pts',(0.0116483078290116,-6.16866029899418,
26.9996507398587));
#56764=CARTESIAN_POINT('Ctrl Pts',(2.96594396483013,-5.40885218553345,27.1388241972807));
#56765=CARTESIAN_POINT('Ctrl Pts',(5.19496237804368,-3.3263901542322,27.2779976547026));
#56766=CARTESIAN_POINT('Ctrl Pts',(6.15363042732399,-0.430509153647837,
27.4171711121246));
#56767=CARTESIAN_POINT('Ctrl Pts',(5.60752017716922,2.5706464226148,27.5563445695465));
#56768=CARTESIAN_POINT('Ctrl Pts',(3.69017472270629,4.94318885774778,27.6955180269685));
#56769=CARTESIAN_POINT('Ctrl Pts',(0.870452222784836,6.10694837830739,27.8346914843904));
#56770=CARTESIAN_POINT('Ctrl Pts',(-2.16212635145099,5.77734499643421,27.9738649418124));
#56771=CARTESIAN_POINT('Ctrl Pts',(-4.66598925893933,4.03497829026688,28.1130383992343));
#56772=CARTESIAN_POINT('Ctrl Pts',(-6.02885426849212,1.30591798239655,28.2522118566564));
#56773=CARTESIAN_POINT('Ctrl Pts',(-5.91745312234585,-1.74248503933367,
28.3913853140782));
#56774=CARTESIAN_POINT('Ctrl Pts',(-4.35902730489465,-4.36478940186638,
28.5305587715003));
#56775=CARTESIAN_POINT('Ctrl Pts',(-1.7346665450516,-5.91974978735934,28.6697322289221));
#56776=CARTESIAN_POINT('Ctrl Pts',(1.31388097813024,-6.02712388646274,28.8089056863441));
#56777=CARTESIAN_POINT('Ctrl Pts',(4.0411385559244,-4.66065496891622,28.948079143766));
#56778=CARTESIAN_POINT('Ctrl Pts',(5.78019613116984,-2.15449257429016,29.087252601188));
#56779=CARTESIAN_POINT('Ctrl Pts',(6.10579317975746,0.878518761034432,29.2264260586099));
#56780=CARTESIAN_POINT('Ctrl Pts',(4.93830981244283,3.69670147074295,29.3655995160319));
#56781=CARTESIAN_POINT('Ctrl Pts',(2.56323662812275,5.61091111636177,29.5047729734539));
#56782=CARTESIAN_POINT('Ctrl Pts',(-0.438637742890223,6.15305635420109,
29.6439464308758));
#56783=CARTESIAN_POINT('Ctrl Pts',(-3.33324981328087,5.19056367360283,29.7831198882978));
#56784=CARTESIAN_POINT('Ctrl Pts',(-5.41276548734757,2.95879626646398,29.9222933457198));
#56785=CARTESIAN_POINT('Ctrl Pts',(-6.16867030413476,0.00349947828611944,
30.0614668031416));
#56786=CARTESIAN_POINT('Ctrl Pts',(-5.41611904451953,-2.9526530549753,30.2006402605636));
#56787=CARTESIAN_POINT('Ctrl Pts',(-3.33913686536758,-5.18677843770153,
30.3398137179856));
#56788=CARTESIAN_POINT('Ctrl Pts',(-0.445618699339021,-6.15255471672228,
30.4789871754075));
#56789=CARTESIAN_POINT('Ctrl Pts',(2.55686885581799,-5.61381574524941,30.6181606328295));
#56790=CARTESIAN_POINT('Ctrl Pts',(4.93411236777539,-3.70230208243847,30.7573340902514));
#56791=CARTESIAN_POINT('Ctrl Pts',(6.10479248505205,-0.885445809699391,
30.8965075476734));
#56792=CARTESIAN_POINT('Ctrl Pts',(5.78263689135225,2.14793299481948,31.0356810050953));
#56793=CARTESIAN_POINT('Ctrl Pts',(4.04642391959121,4.65606690570727,31.1748544625173));
#56794=CARTESIAN_POINT('Ctrl Pts',(1.32071848863418,6.02562928176321,31.3140279199392));
#56795=CARTESIAN_POINT('Ctrl Pts',(-1.72794889865594,5.9217141243981,31.4532013773612));
#56796=CARTESIAN_POINT('Ctrl Pts',(-4.35407222257742,4.36973233139537,31.5923748347831));
#56797=CARTESIAN_POINT('Ctrl Pts',(-5.91547229538928,1.74919784185328,31.7315482922051));
#56798=CARTESIAN_POINT('Ctrl Pts',(-6.03033207850711,-1.299076822359,31.870721749627));
#56799=CARTESIAN_POINT('Ctrl Pts',(-4.67056432958597,-4.0296816760957,32.009895207049));
#56800=CARTESIAN_POINT('Ctrl Pts',(-2.16867991761837,-5.77488813591925,
32.1490686644709));
#56801=CARTESIAN_POINT('Ctrl Pts',(0.863522737700732,-6.10793205994764,
32.2882421218929));
#56802=CARTESIAN_POINT('Ctrl Pts',(3.68456382065906,-4.9473725369081,32.4274155793149));
#56803=CARTESIAN_POINT('Ctrl Pts',(5.60459992034892,-2.57700704311941,32.5665890367368));
#56804=CARTESIAN_POINT('Ctrl Pts',(6.15411492086643,0.423526986426445,32.7057624941588));
#56805=CARTESIAN_POINT('Ctrl Pts',(5.19873314629818,3.32049382487648,32.8449359515807));
#56806=CARTESIAN_POINT('Ctrl Pts',(2.97207892280822,5.40548355321348,32.9841094090027));
#56807=CARTESIAN_POINT('Ctrl Pts',(0.0186472432995035,6.16864311236916,
33.1232828664246));
#56808=CARTESIAN_POINT('Ctrl Pts',(-2.9393443407067,5.42335324446212,33.2624563238466));
#56809=CARTESIAN_POINT('Ctrl Pts',(-5.17856322123317,3.35186344160279,33.4016297812685));
#56810=CARTESIAN_POINT('Ctrl Pts',(-6.15144190639095,0.460725557962153,
33.5408032386905));
#56811=CARTESIAN_POINT('Ctrl Pts',(-5.62007746218061,-2.54307587117484,
33.6799766961124));
#56812=CARTESIAN_POINT('Ctrl Pts',(-3.71440711739459,-4.925006125246,33.8191501535344));
#56813=CARTESIAN_POINT('Ctrl Pts',(-0.900434057400942,-6.10259978007199,
33.9583236109563));
#56814=CARTESIAN_POINT('Ctrl Pts',(2.13372668621321,-5.78789391713461,34.0974970683783));
#56815=CARTESIAN_POINT('Ctrl Pts',(4.64611647652438,-4.05784514909464,34.2366705258002));
#56816=CARTESIAN_POINT('Ctrl Pts',(6.02236796066139,-1.33551103097705,34.3758439832222));
#56817=CARTESIAN_POINT('Ctrl Pts',(5.92593941868295,1.71340233849548,34.5150174406441));
#56818=CARTESIAN_POINT('Ctrl Pts',(4.38041100853469,4.34332878835697,34.6541908980661));
#56819=CARTESIAN_POINT('Ctrl Pts',(1.76371859104191,5.91115913328978,34.793364355488));
#56820=CARTESIAN_POINT('Ctrl Pts',(-1.28426483319145,6.0335039078209,34.93253781291));
#56821=CARTESIAN_POINT('Ctrl Pts',(-4.01820049740123,4.68044552688595,35.0717112703319));
#56822=CARTESIAN_POINT('Ctrl Pts',(-5.76954531825774,2.18285418386855,35.2108847277539));
#56823=CARTESIAN_POINT('Ctrl Pts',(-6.11003410948152,-0.848521507349445,
35.3500581851759));
#56824=CARTESIAN_POINT('Ctrl Pts',(-4.95640542885802,-3.67240395276024,
35.4892316425978));
#56825=CARTESIAN_POINT('Ctrl Pts',(-2.5907619188371,-5.59825492875822,35.6284051000198));
#56826=CARTESIAN_POINT('Ctrl Pts',(0.408413676106909,-6.15513637839415,
35.7675785574417));
#56827=CARTESIAN_POINT('Ctrl Pts',(3.30771781398888,-5.20687127078083,35.9067520148636));
#56828=CARTESIAN_POINT('Ctrl Pts',(5.39816902416752,-2.98534365760133,36.0459254722856));
#56829=CARTESIAN_POINT('Ctrl Pts',(6.16857872386138,-0.0337948958706249,
36.1850989297076));
#56830=CARTESIAN_POINT('Ctrl Pts',(5.43055474173921,2.92601790227538,36.3242723871295));
#56831=CARTESIAN_POINT('Ctrl Pts',(3.36456980619704,5.17031677817611,36.4634458445514));
#56832=CARTESIAN_POINT('Ctrl Pts',(0.475829638423382,6.15029200304019,36.6026193019734));
#56833=CARTESIAN_POINT('Ctrl Pts',(-2.52926755185657,5.6263052902049,36.7417927593954));
#56834=CARTESIAN_POINT('Ctrl Pts',(-4.91587018506997,3.7264897545817,36.8809662168174));
#56835=CARTESIAN_POINT('Ctrl Pts',(-6.10037027658913,0.915416875510875,
37.0201396742393));
#56836=CARTESIAN_POINT('Ctrl Pts',(-5.7931160420816,-2.11950751129575,37.1593131316613));
#56837=CARTESIAN_POINT('Ctrl Pts',(-4.06924190990749,-4.6361380313915,37.2984865890831));
#56838=CARTESIAN_POINT('Ctrl Pts',(-1.35029552022647,-6.01907032485238,
37.4376600465052));
#56839=CARTESIAN_POINT('Ctrl Pts',(1.69884544656774,-5.93012897972197,37.5768335039271));
#56840=CARTESIAN_POINT('Ctrl Pts',(4.33255916398767,-4.39106327192045,37.7160069613491));
#56841=CARTESIAN_POINT('Ctrl Pts',(5.90681032706917,-1.77822870505769,37.855180418771));
#56842=CARTESIAN_POINT('Ctrl Pts',(6.03663935527803,1.26944509994355,37.994353876193));
#56843=CARTESIAN_POINT('Ctrl Pts',(4.69029850123278,4.00669508907226,38.1335273336149));
#56844=CARTESIAN_POINT('Ctrl Pts',(2.19701528757021,5.76416771040234,38.2727007910369));
#56845=CARTESIAN_POINT('Ctrl Pts',(-0.833515160437645,6.11209931568384,
38.4118742484588));
#56846=CARTESIAN_POINT('Ctrl Pts',(-3.66022194037028,4.96540843382439,38.5510477058808));
#56847=CARTESIAN_POINT('Ctrl Pts',(-5.59187617984988,2.60450117233415,38.6902211633027));
#56848=CARTESIAN_POINT('Ctrl Pts',(-6.15612072062488,-0.393297903064726,
38.8293946207246));
#56849=CARTESIAN_POINT('Ctrl Pts',(-5.21497799797801,-3.29492185765726,
38.9685680781466));
#56850=CARTESIAN_POINT('Ctrl Pts',(-2.99859039085709,-5.39082194431627,
39.1077415355686));
#56851=CARTESIAN_POINT('Ctrl Pts',(-0.0489423446593162,-6.16847713899966,
39.2469149929905));
#56852=CARTESIAN_POINT('Ctrl Pts',(2.91267382003966,-5.43772349292586,39.3860884504125));
#56853=CARTESIAN_POINT('Ctrl Pts',(5.1620391582563,-3.37725588253109,39.5252619078344));
#56854=CARTESIAN_POINT('Ctrl Pts',(6.14910501360392,-0.490930849645275,
39.6644353652564));
#56855=CARTESIAN_POINT('Ctrl Pts',(5.63249919176854,2.51544398112719,39.8036088226783));
#56856=CARTESIAN_POINT('Ctrl Pts',(3.73854992114163,4.9067046023369,39.9427822801003));
#56857=CARTESIAN_POINT('Ctrl Pts',(0.930394173682962,6.09810398804735,40.0819557375222));
#56858=CARTESIAN_POINT('Ctrl Pts',(-2.10527555580855,5.79830323470386,40.2211291949442));
#56859=CARTESIAN_POINT('Ctrl Pts',(-4.6261316304785,4.08061413330745,40.3603026523661));
#56860=CARTESIAN_POINT('Ctrl Pts',(-6.01573639422086,1.36507186723222,40.4994761097882));
#56861=CARTESIAN_POINT('Ctrl Pts',(-5.93428278225215,-1.68427831065054,
40.63864956721));
#56862=CARTESIAN_POINT('Ctrl Pts',(-4.40168905731968,-4.32176341441019,
40.7778230246321));
#56863=CARTESIAN_POINT('Ctrl Pts',(-1.79272809640488,-5.90242590295064,
40.9169964820539));
#56864=CARTESIAN_POINT('Ctrl Pts',(1.25461771197804,-6.03973840197183,41.056169939476));
#56865=CARTESIAN_POINT('Ctrl Pts',(3.99516552048621,-4.70012319321317,41.1953433968978));
#56866=CARTESIAN_POINT('Ctrl Pts',(5.75875534477997,-2.21116314333212,41.3345168543199));
#56867=CARTESIAN_POINT('Ctrl Pts',(6.11412766610142,0.818503787453346,41.4736903117417));
#56868=CARTESIAN_POINT('Ctrl Pts',(4.97438149751934,3.64801785694636,41.6128637691638));
#56869=CARTESIAN_POINT('Ctrl Pts',(2.61822472076339,5.58546371208744,41.7520372265856));
#56870=CARTESIAN_POINT('Ctrl Pts',(-0.378179758447216,6.15706794162312,
41.8912106840077));
#56871=CARTESIAN_POINT('Ctrl Pts',(-3.28210603304057,5.22305327900653,42.0303841414296));
#56872=CARTESIAN_POINT('Ctrl Pts',(-5.3834423579622,3.01181904269839,42.1695575988515));
#56873=CARTESIAN_POINT('Ctrl Pts',(-6.16833835839655,0.0640894983272365,
42.3087310562735));
#56874=CARTESIAN_POINT('Ctrl Pts',(-5.44485945479489,-2.89931217446363,
42.4479045136954));
#56875=CARTESIAN_POINT('Ctrl Pts',(-3.38992159410854,-5.15373041138735,
42.5870779711174));
#56876=CARTESIAN_POINT('Ctrl Pts',(-0.506029100568308,-6.14788094523961,
42.7262514285393));
#56877=CARTESIAN_POINT('Ctrl Pts',(2.50160524234212,-5.6386591295226,42.8654248859613));
#56878=CARTESIAN_POINT('Ctrl Pts',(4.89750943231479,-3.75058754435221,43.0045983433832));
#56879=CARTESIAN_POINT('Ctrl Pts',(6.09580092811226,-0.945365861604859,
43.1437718008052));
#56880=CARTESIAN_POINT('Ctrl Pts',(5.8034554637229,2.09103090556957,43.2829452582271));
#56881=CARTESIAN_POINT('Ctrl Pts',(4.09196175072059,4.61609733412348,43.4221187156491));
#56882=CARTESIAN_POINT('Ctrl Pts',(1.37983998289368,6.01236618887025,43.561292173071));
#56883=CARTESIAN_POINT('Ctrl Pts',(-1.66970101858295,5.93840080122631,43.700465630493));
#56884=CARTESIAN_POINT('Ctrl Pts',(-4.31094160472234,4.41228830065944,43.839639087915));
#56885=CARTESIAN_POINT('Ctrl Pts',(-5.89800588737206,1.8072166776529,43.9788125453369));
#56886=CARTESIAN_POINT('Ctrl Pts',(-6.04280102921519,-1.23978275870331,
44.1179860027589));
#56887=CARTESIAN_POINT('Ctrl Pts',(-4.70991954358473,-3.98361186116582,
44.2571594601808));
#56888=CARTESIAN_POINT('Ctrl Pts',(-2.22529766584334,-5.75330825402695,
44.3963329176028));
#56889=CARTESIAN_POINT('Ctrl Pts',(0.80348747891454,-6.11611914850338,44.5355063750247));
#56890=CARTESIAN_POINT('Ctrl Pts',(3.63579177607875,-4.98332456583558,44.6746798324467));
#56891=CARTESIAN_POINT('Ctrl Pts',(5.57901756413806,-2.63193248137206,44.8138532898686));
#56892=CARTESIAN_POINT('Ctrl Pts',(6.15797803567706,0.363059333416714,44.9530267472906));
#56893=CARTESIAN_POINT('Ctrl Pts',(5.23109706517253,3.26927041741817,45.0922002047125));
#56894=CARTESIAN_POINT('Ctrl Pts',(3.02502953335652,5.3760303096042,45.2313736621344));
#56895=CARTESIAN_POINT('Ctrl Pts',(0.0792362655371347,6.16816238288892,
45.3705471195565));
#56896=CARTESIAN_POINT('Ctrl Pts',(-2.88593304611797,5.45196258431645,45.5097205769783));
#56897=CARTESIAN_POINT('Ctrl Pts',(-5.14539058767098,3.40256686455523,45.6488940344004));
#56898=CARTESIAN_POINT('Ctrl Pts',(-6.14661980532839,0.521124300150113,
45.7880674918222));
#56899=CARTESIAN_POINT('Ctrl Pts',(-5.64478506632273,-2.48775141894889,
45.9272409492443));
#56900=CARTESIAN_POINT('Ctrl Pts',(-3.76260255162662,-4.88828473045045,
46.0664144066661));
#56901=CARTESIAN_POINT('Ctrl Pts',(-0.96033184899738,-6.0934611106713,46.2055878640882));
#56902=CARTESIAN_POINT('Ctrl Pts',(2.07677364647398,-5.80857269807079,46.34476132151));
#56903=CARTESIAN_POINT('Ctrl Pts',(4.60603520283319,-4.10328469372083,46.4839347789321));
#56904=CARTESIAN_POINT('Ctrl Pts',(6.00895972912288,-1.39459977815919,46.6231082363539));
#56905=CARTESIAN_POINT('Ctrl Pts',(5.9424830118128,1.65511365826597,46.762281693776));
#56906=CARTESIAN_POINT('Ctrl Pts',(4.42286093802635,4.30009380017957,46.9014551511978));
#56907=CARTESIAN_POINT('Ctrl Pts',(1.82169436143568,5.89355030698609,47.0406286086199));
#56908=CARTESIAN_POINT('Ctrl Pts',(-1.22494032957404,6.0458272185405,47.1798020660416));
#56909=CARTESIAN_POINT('Ctrl Pts',(-3.97203418077946,4.71968749327557,47.3189755234639));
#56910=CARTESIAN_POINT('Ctrl Pts',(-5.74782647098904,2.23941876987309,47.4581489808855));
#56911=CARTESIAN_POINT('Ctrl Pts',(-6.11807375088118,-0.788466325368954,
47.5973224383078));
#56912=CARTESIAN_POINT('Ctrl Pts',(-4.99223758484679,-3.62354377149019,
47.7364958957295));
#56913=CARTESIAN_POINT('Ctrl Pts',(-2.64562437150301,-5.57253777487165,
47.8756693531516));
#56914=CARTESIAN_POINT('Ctrl Pts',(0.347936719148598,-6.15885099729895,
48.0148428105735));
#56915=CARTESIAN_POINT('Ctrl Pts',(3.25641508818817,-5.23910930797237,48.1540162679955));
#56916=CARTESIAN_POINT('Ctrl Pts',(5.36858584393653,-3.03822178317292,48.2931897254174));
#56917=CARTESIAN_POINT('Ctrl Pts',(6.16794921353787,-0.0943825549547815,
48.4323631828394));
#56918=CARTESIAN_POINT('Ctrl Pts',(5.45903283865907,2.87253651567811,48.5715366402613));
#56919=CARTESIAN_POINT('Ctrl Pts',(3.41519161762082,5.13701973739587,48.7107100976833));
#56920=CARTESIAN_POINT('Ctrl Pts',(0.536216357367407,6.14532160147488,48.8498835551052));
#56921=CARTESIAN_POINT('Ctrl Pts',(-2.47388259448532,5.65087696522981,48.9890570125272));
#56922=CARTESIAN_POINT('Ctrl Pts',(-4.87903055236837,3.774594870515,49.1282304699491));
#56923=CARTESIAN_POINT('Ctrl Pts',(-6.09108454983344,0.975292045616384,
49.2674039273711));
#56924=CARTESIAN_POINT('Ctrl Pts',(-5.81365490689088,-2.06250386449231,
49.4065773847931));
#56925=CARTESIAN_POINT('Ctrl Pts',(-4.11458289403143,-4.59594529728175,
49.545750842215));
#56926=CARTESIAN_POINT('Ctrl Pts',(-1.40935116402794,-6.00551703551953,
49.684924299637));
#56927=CARTESIAN_POINT('Ctrl Pts',(1.64051631766061,-5.9465293893961,49.8240977570588));
#56928=CARTESIAN_POINT('Ctrl Pts',(4.28922006619361,-4.43340690566795,49.9632712144809));
#56929=CARTESIAN_POINT('Ctrl Pts',(5.88905918865963,-1.83616106045353,50.1024446719028));
#56930=CARTESIAN_POINT('Ctrl Pts',(6.04881695169999,1.21009051408931,50.2416181293247));
#56931=CARTESIAN_POINT('Ctrl Pts',(4.72942698338542,3.96043254914008,50.3807915867467));
#56932=CARTESIAN_POINT('Ctrl Pts',(2.25352637027147,5.74231002872132,50.5199650441686));
#56933=CARTESIAN_POINT('Ctrl Pts',(-0.773440417394008,6.1199914614486,50.6591385015906));
#56934=CARTESIAN_POINT('Ctrl Pts',(-3.61127391703609,5.0011205008075,50.7983119590126));
#56935=CARTESIAN_POINT('Ctrl Pts',(-5.56602438336132,2.65930030859425,50.9374854164345));
#56936=CARTESIAN_POINT('Ctrl Pts',(-6.15968682122481,-0.332812006832159,
51.0766588738565));
#56937=CARTESIAN_POINT('Ctrl Pts',(-5.24708995909226,-3.24354012286813,
51.2158323312784));
#56938=CARTESIAN_POINT('Ctrl Pts',(-3.0513957125984,-5.36110900584928,51.3550057887004));
#56939=CARTESIAN_POINT('Ctrl Pts',(-0.109528275248135,-6.16769885162882,
51.4941792461224));
#56940=CARTESIAN_POINT('Ctrl Pts',(2.85912266392506,-5.46607017518914,51.6333527035443));
#56941=CARTESIAN_POINT('Ctrl Pts',(5.12861791103823,-3.42779577717813,51.7725261609662));
#56942=CARTESIAN_POINT('Ctrl Pts',(6.14398634150724,-0.551305181215167,
51.9116996183881));
#56943=CARTESIAN_POINT('Ctrl Pts',(5.65693478950973,2.45999885258035,52.0508730758102));
#56944=CARTESIAN_POINT('Ctrl Pts',(3.78656442870373,4.86974695387121,52.190046533232));
#56945=CARTESIAN_POINT('Ctrl Pts',(0.990246361251975,6.08867125992932,52.3292199906541));
#56946=CARTESIAN_POINT('Ctrl Pts',(-2.04822164567128,5.8187020595375,52.4683934480759));
#56947=CARTESIAN_POINT('Ctrl Pts',(-4.58582767831123,4.12585628352428,52.607566905498));
#56948=CARTESIAN_POINT('Ctrl Pts',(-6.00203812881962,1.42409405154916,52.7467403629199));
#56949=CARTESIAN_POINT('Ctrl Pts',(-5.95053990957657,-1.62590908478877,
52.8859138203418));
#56950=CARTESIAN_POINT('Ctrl Pts',(-4.44392613999212,-4.27832046833299,
53.0250872777638));
#56951=CARTESIAN_POINT('Ctrl Pts',(-1.85061668747234,-5.88453255947412,
53.1642607351857));
#56952=CARTESIAN_POINT('Ctrl Pts',(1.19523340179344,-6.0517702106656,53.3034341926077));
#56953=CARTESIAN_POINT('Ctrl Pts',(3.94880703620541,-4.73913795518518,53.4426076500296));
#56954=CARTESIAN_POINT('Ctrl Pts',(5.73675896048776,-2.26762038196999,53.5817811074516));
#56955=CARTESIAN_POINT('Ctrl Pts',(6.12187226864186,0.758409845595327,53.7209545648735));
#56956=CARTESIAN_POINT('Ctrl Pts',(5.0099732601542,3.59898228670302,53.8601280222956));
#56957=CARTESIAN_POINT('Ctrl Pts',(2.67296021018055,5.55947742888248,53.9993014797174));
#56958=CARTESIAN_POINT('Ctrl Pts',(-0.31768528766863,6.16048550241465,54.1384749371395));
#56959=CARTESIAN_POINT('Ctrl Pts',(-3.2306455990934,5.25503897040932,54.2776483945613));
#56960=CARTESIAN_POINT('Ctrl Pts',(-5.35359984042742,3.06455124219481,54.4168218519833));
#56961=CARTESIAN_POINT('Ctrl Pts',(-6.16741129867142,0.12467333508929,54.5559953094053));
#56962=CARTESIAN_POINT('Ctrl Pts',(-5.47307455147189,-2.84569157174367,
54.6951687668272));
#56963=CARTESIAN_POINT('Ctrl Pts',(-3.44037926722471,-5.12018515926061,
54.8343422242492));
#56964=CARTESIAN_POINT('Ctrl Pts',(-0.566390680708578,-6.14261403347702,
54.9735156816711));
#56965=CARTESIAN_POINT('Ctrl Pts',(2.44610027695225,-5.66295850263414,55.1126891390931));
#56966=CARTESIAN_POINT('Ctrl Pts',(4.86043399093854,-3.79851115401699,55.251862596515));
#56967=CARTESIAN_POINT('Ctrl Pts',(6.086221255511,-1.00519470573039,55.391036053937));
#56968=CARTESIAN_POINT('Ctrl Pts',(5.82371412557653,2.03392707613192,55.530209511359));
#56969=CARTESIAN_POINT('Ctrl Pts',(4.13710479422145,4.57568240693037,55.6693829687809));
#56970=CARTESIAN_POINT('Ctrl Pts',(1.438828351824,5.99852303000078,55.8085564262028));
#56971=CARTESIAN_POINT('Ctrl Pts',(-1.61129204773131,5.954514548171,55.9477298836248));
#56972=CARTESIAN_POINT('Ctrl Pts',(-4.26739507232172,4.45441857756841,56.0869033410467));
#56973=CARTESIAN_POINT('Ctrl Pts',(-5.87997044672494,1.86506115532538,56.2260767984687));
#56974=CARTESIAN_POINT('Ctrl Pts',(-6.05468697762929,-1.18036908227415,
56.3652502558907));
#56975=CARTESIAN_POINT('Ctrl Pts',(-4.74882035011812,-3.93715771207684,
56.5044237133125));
#56976=CARTESIAN_POINT('Ctrl Pts',(-2.28170071998218,-5.73117329976114,
56.6435971707346));
#56977=CARTESIAN_POINT('Ctrl Pts',(0.743374700607,-6.1237161611198,56.7827706281565));
#56978=CARTESIAN_POINT('Ctrl Pts',(3.58666895460946,-5.01879580950479,56.9219440855785));
#56979=CARTESIAN_POINT('Ctrl Pts',(5.55289695091324,-2.68660399389279,57.0611175430004));
#56980=CARTESIAN_POINT('Ctrl Pts',(6.16124703605245,0.302556652872041,57.2002910004224));
#56981=CARTESIAN_POINT('Ctrl Pts',(5.26295629399103,3.21773159461793,57.3394644578443));
#56982=CARTESIAN_POINT('Ctrl Pts',(3.07768829263442,5.34605839295113,57.4786379152663));
#56983=CARTESIAN_POINT('Ctrl Pts',(0.139817643153607,6.16708655639964,57.6178113726882));
#56984=CARTESIAN_POINT('Ctrl Pts',(-2.83224332012334,5.48004592527096,57.7569848301102));
#56985=CARTESIAN_POINT('Ctrl Pts',(-5.11172153291249,3.4529420118822,57.8961582875321));
#56986=CARTESIAN_POINT('Ctrl Pts',(-6.1412046856592,0.581472764882143,58.0353317449541));
#56987=CARTESIAN_POINT('Ctrl Pts',(-5.66894806828008,-2.43218695140933,
58.174505202376));
#56988=CARTESIAN_POINT('Ctrl Pts',(-3.81043497441608,-4.85109171972752,
58.313678659798));
#56989=CARTESIAN_POINT('Ctrl Pts',(-1.02013698891321,-6.08373455135193,
58.4528521172199));
#56990=CARTESIAN_POINT('Ctrl Pts',(2.01962024207041,-5.82869107478529,58.5920255746419));
#56991=CARTESIAN_POINT('Ctrl Pts',(4.5655095443151,-4.14832835829445,58.7311990320639));
#56992=CARTESIAN_POINT('Ctrl Pts',(5.99497176025902,-1.45355397600471,58.8703724894857));
#56993=CARTESIAN_POINT('Ctrl Pts',(5.95845328121232,1.59666529462889,59.0095459469078));
#56994=CARTESIAN_POINT('Ctrl Pts',(4.46488415512748,4.25644394403988,59.1487194043297));
#56995=CARTESIAN_POINT('Ctrl Pts',(1.87949437691273,5.87537287792151,59.2878928617516));
#56996=CARTESIAN_POINT('Ctrl Pts',(-1.16549764516288,6.05756723500302,59.4270663191736));
#56997=CARTESIAN_POINT('Ctrl Pts',(-3.92548464699931,4.75847410979977,59.5662397765955));
#56998=CARTESIAN_POINT('Ctrl Pts',(-5.7255530802228,2.29576729940424,59.7054132340175));
#56999=CARTESIAN_POINT('Ctrl Pts',(-6.12552312776374,-0.728335073090324,
59.8445866914395));
#57000=CARTESIAN_POINT('Ctrl Pts',(-5.02758809565984,-3.57433399500399,
59.9837601488614));
#57001=CARTESIAN_POINT('Ctrl Pts',(-2.70023157745952,-5.54628298913386,
60.1229336062834));
#57002=CARTESIAN_POINT('Ctrl Pts',(0.287426193667008,-6.16197141754554,
60.2621070637053));
#57003=CARTESIAN_POINT('Ctrl Pts',(3.20479818731301,-5.2708418820976,60.4012805211273));
#57004=CARTESIAN_POINT('Ctrl Pts',(5.33848470889396,-3.090806784699,60.5404539785492));
#57005=CARTESIAN_POINT('Ctrl Pts',(6.16672462677367,-0.154961108126498,
60.6796274359711));
#57006=CARTESIAN_POINT('Ctrl Pts',(5.4869842545454,2.8187779901657,60.8188008933931));
#57007=CARTESIAN_POINT('Ctrl Pts',(3.46548393540557,5.1032270830108,60.9579743508151));
#57008=CARTESIAN_POINT('Ctrl Pts',(0.596551342776706,6.13975830658775,61.097147808237));
#57009=CARTESIAN_POINT('Ctrl Pts',(-2.41825895981904,5.67490345026123,61.236321265659));
#57010=CARTESIAN_POINT('Ctrl Pts',(-4.84172019662853,3.82233581813661,61.3754947230809));
#57011=CARTESIAN_POINT('Ctrl Pts',(-6.08121116233572,1.03507312043469,61.5146681805029));
#57012=CARTESIAN_POINT('Ctrl Pts',(-5.83363287736978,-2.00530122924022,
61.6538416379248));
#57013=CARTESIAN_POINT('Ctrl Pts',(-4.15952690764293,-4.55530915281376,
61.7930150953468));
#57014=CARTESIAN_POINT('Ctrl Pts',(-1.46827083612136,-5.99138433904502,
61.9321885527687));
#57015=CARTESIAN_POINT('Ctrl Pts',(1.58202891528899,-5.96235608877982,62.0713620101907));
#57016=CARTESIAN_POINT('Ctrl Pts',(4.24546714638385,-4.47532280209235,62.2105354676127));
#57017=CARTESIAN_POINT('Ctrl Pts',(5.87073988690873,-1.89391627977385,62.3497089250346));
#57018=CARTESIAN_POINT('Ctrl Pts',(6.06041095347787,1.15061920855663,62.4888823824565));
#57019=CARTESIAN_POINT('Ctrl Pts',(4.76809919931039,3.91378785592005,62.6280558398785));
#57020=CARTESIAN_POINT('Ctrl Pts',(2.3098199899806,5.71989844390654,62.7672292973004));
#57021=CARTESIAN_POINT('Ctrl Pts',(-0.713290965110059,6.12729294673171,
62.9064027547224));
#57022=CARTESIAN_POINT('Ctrl Pts',(-3.5619776551369,5.03635047707401,63.0455762121444));
#57023=CARTESIAN_POINT('Ctrl Pts',(-5.53963524622449,2.71384207608729,63.1847496695663));
#57024=CARTESIAN_POINT('Ctrl Pts',(-6.16265930027355,-0.272292435697687,
63.3239231269883));
#57025=CARTESIAN_POINT('Ctrl Pts',(-5.2786944041734,-3.19184850901995,63.4630965844102));
#57026=CARTESIAN_POINT('Ctrl Pts',(-3.10390914192393,-5.33087287704626,
63.6022700418322));
#57027=CARTESIAN_POINT('Ctrl Pts',(-0.170098756992531,-6.16633713170798,
63.7414434992541));
#57028=CARTESIAN_POINT('Ctrl Pts',(2.8052861403712,-5.49386682965458,63.8806169566761));
#57029=CARTESIAN_POINT('Ctrl Pts',(5.09472044030236,-3.47804920225361,64.019790414098));
#57030=CARTESIAN_POINT('Ctrl Pts',(6.13823861632767,-0.611539775069484,
64.15896387152));
#57031=CARTESIAN_POINT('Ctrl Pts',(5.68089589400686,2.40414490658337,64.2981373289419));
#57032=CARTESIAN_POINT('Ctrl Pts',(3.83406936451904,4.8326818231135,64.4373107863639));
#57033=CARTESIAN_POINT('Ctrl Pts',(1.97824858295778,5.66265744446568,64.5300930913119));
#57034=CARTESIAN_POINT('Ctrl Pts',(1.00712212024295,5.83040612628463,64.5764842437858));
#57035=CARTESIAN_POINT('Ctrl Pts',(-5.91644646386006,0.000128480793576948,
61.5616248077951));
#57036=CARTESIAN_POINT('Ctrl Pts',(-5.91593193090335,-0.652955704091308,
61.5923637511717));
#57037=CARTESIAN_POINT('Ctrl Pts',(-5.80809740540869,-1.30620561360789,
61.6231026945482));
#57038=CARTESIAN_POINT('Ctrl Pts',(-5.59587826324296,-1.92357349155666,
61.6538416379248));
#57039=CARTESIAN_POINT('Ctrl Pts',(-5.27559755412752,-2.85530387043135,
61.7002327903988));
#57040=CARTESIAN_POINT('Ctrl Pts',(-4.71756223088528,-3.70530651162249,
61.7466239428728));
#57041=CARTESIAN_POINT('Ctrl Pts',(-3.99000189067727,-4.36965369658994,
61.7930150953468));
#57042=CARTESIAN_POINT('Ctrl Pts',(-3.26244155046918,-5.03400088155746,
61.8394062478208));
#57043=CARTESIAN_POINT('Ctrl Pts',(-2.36535619329527,-5.51269261030126,
61.8857974002948));
#57044=CARTESIAN_POINT('Ctrl Pts',(-1.40843022280656,-5.74720043296228,
61.9321885527687));
#57045=CARTESIAN_POINT('Ctrl Pts',(-0.451504252317853,-5.9817082556233,
61.9785797052427));
#57046=CARTESIAN_POINT('Ctrl Pts',(0.565262331485657,-5.97203217220155,
62.0249708577167));
#57047=CARTESIAN_POINT('Ctrl Pts',(1.51755199523657,-5.71935524937607,62.0713620101907));
#57048=CARTESIAN_POINT('Ctrl Pts',(2.46984165898738,-5.46667832655061,62.1177531626647));
#57049=CARTESIAN_POINT('Ctrl Pts',(3.3576544026856,-4.97100056432147,62.1641443151387));
#57050=CARTESIAN_POINT('Ctrl Pts',(4.07243956462219,-4.29292726282051,62.2105354676127));
#57051=CARTESIAN_POINT('Ctrl Pts',(4.78722472655881,-3.61485396131952,62.2569266200867));
#57052=CARTESIAN_POINT('Ctrl Pts',(5.32898230673377,-2.75438512054668,62.3033177725606));
#57053=CARTESIAN_POINT('Ctrl Pts',(5.63147294124944,-1.81672811877186,62.3497089250346));
#57054=CARTESIAN_POINT('Ctrl Pts',(5.93396357576511,-0.879071116997042,
62.3961000775086));
#57055=CARTESIAN_POINT('Ctrl Pts',(5.99718726462149,0.135774045779763,62.4424912299826));
#57056=CARTESIAN_POINT('Ctrl Pts',(5.81341381668844,1.10372473506206,62.4888823824565));
#57057=CARTESIAN_POINT('Ctrl Pts',(5.62964036875539,2.07167542434442,62.5352735349305));
#57058=CARTESIAN_POINT('Ctrl Pts',(5.19886978403288,2.99273164013226,62.5816646874045));
#57059=CARTESIAN_POINT('Ctrl Pts',(4.57377129011664,3.75427817935727,62.6280558398785));
#57060=CARTESIAN_POINT('Ctrl Pts',(3.94867279620046,4.51582471858219,62.6744469923525));
#57061=CARTESIAN_POINT('Ctrl Pts',(3.1292463930906,5.11786158124432,62.7208381448265));
#57062=CARTESIAN_POINT('Ctrl Pts',(2.21568136568727,5.4867790963796,62.7672292973004));
#57063=CARTESIAN_POINT('Ctrl Pts',(1.30211633828383,5.85569661151491,62.8136204497744));
#57064=CARTESIAN_POINT('Ctrl Pts',(0.294412686586882,5.99149477912333,62.8600116022484));
#57065=CARTESIAN_POINT('Ctrl Pts',(-0.68422025426609,5.87757011798457,62.9064027547224));
#57066=CARTESIAN_POINT('Ctrl Pts',(-1.66285319511901,5.76364545684581,62.9527939071964));
#57067=CARTESIAN_POINT('Ctrl Pts',(-2.61241542512795,5.39999796695991,62.9991850596704));
#57068=CARTESIAN_POINT('Ctrl Pts',(-3.41680613864703,4.83108948851917,63.0455762121444));
#57069=CARTESIAN_POINT('Ctrl Pts',(-4.22119685216606,4.26218101007847,63.0919673646183));
#57070=CARTESIAN_POINT('Ctrl Pts',(-4.88041604919522,3.48801154308295,63.1383585170923));
#57071=CARTESIAN_POINT('Ctrl Pts',(-5.31386299005133,2.60323772428773,63.1847496695663));
#57072=CARTESIAN_POINT('Ctrl Pts',(-5.70900759272686,1.79664857546361,63.2270413823092));
#57073=CARTESIAN_POINT('Ctrl Pts',(-5.91651851507,0.898138913726484,63.2693330950522));
#57074=CARTESIAN_POINT('Ctrl Pts',(-5.9171574445836,-8.64418186984388E-5,
63.3116248077951));
#57075=CARTESIAN_POINT('',(-2.85728222003707,-4.00342940649516,-1.53523027623947E-15));
#57076=CARTESIAN_POINT('Ctrl Pts',(-2.85728222003706,-4.00342940649517,
-5.3776427755281E-16));
#57077=CARTESIAN_POINT('Ctrl Pts',(-2.95928271123691,-3.94487512701868,
-5.18176765844195E-16));
#57078=CARTESIAN_POINT('Ctrl Pts',(-3.05898490657923,-3.88272744726811,
-7.71266662334843E-16));
#57079=CARTESIAN_POINT('Ctrl Pts',(-3.15618864747685,-3.81711101865418,
-7.21644966006352E-16));
#57080=CARTESIAN_POINT('Ctrl Pts',(-3.27550031648898,-3.73657085075272,
-6.98637490506031E-16));
#57081=CARTESIAN_POINT('Ctrl Pts',(-3.39104882900031,-3.65080626318817,
-5.84937091110779E-16));
#57082=CARTESIAN_POINT('Ctrl Pts',(-3.50262914174305,-3.56021018039735,
-6.52256026967279E-16));
#57083=CARTESIAN_POINT('Ctrl Pts',(-3.61584744679976,-3.46828415253254,
-7.20563200773708E-16));
#57084=CARTESIAN_POINT('Ctrl Pts',(-3.72498077963315,-3.3713833795464,-7.19044273329439E-16));
#57085=CARTESIAN_POINT('Ctrl Pts',(-3.82979628327283,-3.26986793650992,
-6.80011602582908E-16));
#57086=CARTESIAN_POINT('Ctrl Pts',(-3.9300117525662,-3.17280769817535,-6.42691957293752E-16));
#57087=CARTESIAN_POINT('Ctrl Pts',(-4.02628037930183,-3.07152824151411,
-1.00568777733274E-15));
#57088=CARTESIAN_POINT('Ctrl Pts',(-4.11837549701657,-2.96630706901007,
-1.1518563880486E-15));
#57089=CARTESIAN_POINT('Ctrl Pts',(-4.15643398619576,-2.92282421178012,
-1.21226085494441E-15));
#57090=CARTESIAN_POINT('Ctrl Pts',(-4.19377942809832,-2.87866780488849,
-5.54864022283868E-16));
#57091=CARTESIAN_POINT('Ctrl Pts',(-4.23039440888198,-2.83385586799541,
-4.9960036108132E-16));
#57092=CARTESIAN_POINT('Ctrl Pts',(-4.25014618584021,-2.8096822821124,-4.69788642309225E-16));
#57093=CARTESIAN_POINT('Ctrl Pts',(-4.26968538238833,-2.78531792146795,
-3.55933796205804E-16));
#57094=CARTESIAN_POINT('Ctrl Pts',(-4.28900915147612,-2.76076551556,-3.19189119579733E-16));
#57095=CARTESIAN_POINT('Ctrl Pts',(-4.30443367755228,-2.74116741213417,
-2.8985896042683E-16));
#57096=CARTESIAN_POINT('Ctrl Pts',(-4.31972315914379,-2.72144646705537,
-2.13147410180917E-16));
#57097=CARTESIAN_POINT('Ctrl Pts',(-4.33485992958826,-2.70162560333916,
-2.08166817117217E-16));
#57098=CARTESIAN_POINT('Ctrl Pts',(-4.4278307771548,-2.57988480625452,-1.77575750137973E-16));
#57099=CARTESIAN_POINT('Ctrl Pts',(-4.51516326633763,-2.45422884936395,
-1.03603524343314E-15));
#57100=CARTESIAN_POINT('Ctrl Pts',(-4.59662203129057,-2.32508248185065,
-8.88178419700125E-16));
#57101=CARTESIAN_POINT('Ctrl Pts',(-4.67808079624352,-2.19593611433734,
-7.40321595967114E-16));
#57102=CARTESIAN_POINT('Ctrl Pts',(-4.75366645541919,-2.06329874970035,
-1.11603729512037E-16));
#57103=CARTESIAN_POINT('Ctrl Pts',(-4.82311411010153,-1.92754875329055,
2.77555756156289E-17));
#57104=CARTESIAN_POINT('Ctrl Pts',(-4.89136206219792,-1.79414382702721,
1.68047749947343E-16));
#57105=CARTESIAN_POINT('Ctrl Pts',(-4.95368291217718,-1.65773229238894,
-1.11642256479697E-15));
#57106=CARTESIAN_POINT('Ctrl Pts',(-5.01004456451512,-1.51873876158455,
-1.27675647831893E-15));
#57107=CARTESIAN_POINT('Ctrl Pts',(-5.06678008578305,-1.37882323221405,
-1.43815394952959E-15));
#57108=CARTESIAN_POINT('Ctrl Pts',(-5.11747740025848,-1.23629066654526,
-2.18559075597774E-17));
#57109=CARTESIAN_POINT('Ctrl Pts',(-5.1620585192726,-1.09154709310106,0.));
#57110=CARTESIAN_POINT('Ctrl Pts',(-5.17533073261087,-1.04845558645932,
6.50670674602739E-18));
#57111=CARTESIAN_POINT('Ctrl Pts',(-5.18806054212299,-1.00516797275366,
-3.13319586228567E-16));
#57112=CARTESIAN_POINT('Ctrl Pts',(-5.20024505801854,-0.96169464478646,
-3.05311331771918E-16));
#57113=CARTESIAN_POINT('Ctrl Pts',(-5.2055486682428,-0.94277180955312,-3.01825542054964E-16));
#57114=CARTESIAN_POINT('Ctrl Pts',(-5.21074888095922,-0.923813872462111,
1.00782795168963E-16));
#57115=CARTESIAN_POINT('Ctrl Pts',(-5.21584187742371,-0.904835564223655,
1.11022302462516E-16));
#57116=CARTESIAN_POINT('Ctrl Pts',(-5.25575457855815,-0.756106706852481,
1.91267085120645E-16));
#57117=CARTESIAN_POINT('Ctrl Pts',(-5.28914618801543,-0.605917493293632,
1.21266317269936E-16));
#57118=CARTESIAN_POINT('Ctrl Pts',(-5.31602599346966,-0.454734459029675,
1.11022302462516E-16));
#57119=CARTESIAN_POINT('Ctrl Pts',(-5.34317079103733,-0.302061000594503,
1.00677297968299E-16));
#57120=CARTESIAN_POINT('Ctrl Pts',(-5.36367506573315,-0.148373349291817,
1.13229940710053E-15));
#57121=CARTESIAN_POINT('Ctrl Pts',(-5.37750436397203,0.00587829643313097,
1.0547118733939E-15));
#57122=CARTESIAN_POINT('Ctrl Pts',(-5.39135928407949,0.160415727837723,
9.76980591424825E-16));
#57123=CARTESIAN_POINT('Ctrl Pts',(-5.39851473413966,0.315519992364312,
1.72186685042656E-16));
#57124=CARTESIAN_POINT('Ctrl Pts',(-5.39888790157043,0.47075779833462,2.77555756156289E-16));
#57125=CARTESIAN_POINT('Ctrl Pts',(-5.39902973997675,0.529762634193127,
3.17605824544993E-16));
#57126=CARTESIAN_POINT('Ctrl Pts',(-5.39819122013145,0.588786903914602,
7.39732282841607E-16));
#57127=CARTESIAN_POINT('Ctrl Pts',(-5.39636585059798,0.647807199370088,
7.7715611723761E-16));
#57128=CARTESIAN_POINT('Ctrl Pts',(-5.39278164456781,0.7636965549195,7.9126101240072E-16));
#57129=CARTESIAN_POINT('Ctrl Pts',(-5.38539362454781,0.879570616150454,
2.25912163058052E-16));
#57130=CARTESIAN_POINT('Ctrl Pts',(-5.37425683908509,0.995265406518742,
2.22044604925031E-16));
#57131=CARTESIAN_POINT('Ctrl Pts',(-5.37119198986139,1.02710467375017,2.20980250890262E-16));
#57132=CARTESIAN_POINT('Ctrl Pts',(-5.3678431309615,1.05893036198002,-4.98345963791524E-17));
#57133=CARTESIAN_POINT('Ctrl Pts',(-5.36421119278863,1.09073904150971,-5.55111512312578E-17));
#57134=CARTESIAN_POINT('Ctrl Pts',(-5.36130959000465,1.11615141052175,-6.00462249517562E-17));
#57135=CARTESIAN_POINT('Ctrl Pts',(-5.35822677414316,1.14155649394533,-1.11305744570047E-16));
#57136=CARTESIAN_POINT('Ctrl Pts',(-5.35496675861173,1.16692638663651,-1.11022302462516E-16));
#57137=CARTESIAN_POINT('Ctrl Pts',(-5.33509845623767,1.32154426938163,-1.09294852564294E-16));
#57138=CARTESIAN_POINT('Ctrl Pts',(-5.30863314216658,1.4750401212272,2.16862255230366E-16));
#57139=CARTESIAN_POINT('Ctrl Pts',(-5.27581080798388,1.62701588796501,2.22044604925031E-16));
#57140=CARTESIAN_POINT('Ctrl Pts',(-5.24225444461877,1.78239039676614,2.27342851188421E-16));
#57141=CARTESIAN_POINT('Ctrl Pts',(-5.20205360448928,1.93617674988367,3.58795532194926E-16));
#57142=CARTESIAN_POINT('Ctrl Pts',(-5.15541121814811,2.08796002984681,2.77555756156289E-16));
#57143=CARTESIAN_POINT('Ctrl Pts',(-5.10857408351102,2.24037705815435,1.95976775604635E-16));
#57144=CARTESIAN_POINT('Ctrl Pts',(-5.05524139421354,2.39077501296198,7.1419842572492E-16));
#57145=CARTESIAN_POINT('Ctrl Pts',(-4.99556586525404,2.53873318984042,7.7715611723761E-16));
#57146=CARTESIAN_POINT('Ctrl Pts',(-4.94308833481477,2.66884480956559,8.32519919290971E-16));
#57147=CARTESIAN_POINT('Ctrl Pts',(-4.88570498504201,2.79707005286713,-9.60359478345213E-16));
#57148=CARTESIAN_POINT('Ctrl Pts',(-4.82348716797381,2.9231153225656,-1.0547118733939E-15));
#57149=CARTESIAN_POINT('Ctrl Pts',(-4.79237825943971,2.98613795741484,-1.10188807091824E-15));
#57150=CARTESIAN_POINT('Ctrl Pts',(-4.76006026636089,3.04861544670858,-2.34131068753582E-16));
#57151=CARTESIAN_POINT('Ctrl Pts',(-4.72653934608425,3.11050991069538,-2.22044604925031E-16));
#57152=CARTESIAN_POINT('Ctrl Pts',(-4.71542868620718,3.13102510932223,-2.18038492097365E-16));
#57153=CARTESIAN_POINT('Ctrl Pts',(-4.70418510044029,3.15147759934516,-9.30594094610435E-17));
#57154=CARTESIAN_POINT('Ctrl Pts',(-4.69281112422588,3.17186176124398,-1.11022302462516E-16));
#57155=CARTESIAN_POINT('Ctrl Pts',(-4.66986975336546,3.21297672482261,-1.47253553724545E-16));
#57156=CARTESIAN_POINT('Ctrl Pts',(-4.64641569423652,3.25378205022521,4.87358186177378E-16));
#57157=CARTESIAN_POINT('Ctrl Pts',(-4.6224537842997,3.29426742849354,4.44089209850063E-16));
#57158=CARTESIAN_POINT('Ctrl Pts',(-4.5407901963357,3.43224396117347,1.8116204744435E-16));
#57159=CARTESIAN_POINT('Ctrl Pts',(-4.45323198209242,3.56650537742696,-3.2643330626556E-16));
#57160=CARTESIAN_POINT('Ctrl Pts',(-4.36016765818568,3.69680903327971,-1.66533453693773E-16));
#57161=CARTESIAN_POINT('Ctrl Pts',(-4.26589053581423,3.828810784247,-4.54981339791011E-18));
#57162=CARTESIAN_POINT('Ctrl Pts',(-4.16596252106395,3.95675153466492,-4.38639487339398E-16));
#57163=CARTESIAN_POINT('Ctrl Pts',(-4.06073706621468,4.08036089658611,-2.77555756156289E-16));
#57164=CARTESIAN_POINT('Ctrl Pts',(-4.00840964546727,4.14183042502705,-1.97450650511893E-16));
#57165=CARTESIAN_POINT('Ctrl Pts',(-3.95477144372171,4.2022284838368,4.11439993416818E-16));
#57166=CARTESIAN_POINT('Ctrl Pts',(-3.89986178457086,4.26151948427011,4.9960036108132E-16));
#57167=CARTESIAN_POINT('Ctrl Pts',(-3.87477357591952,4.28860952658727,5.3988080960258E-16));
#57168=CARTESIAN_POINT('Ctrl Pts',(-3.8494199054371,4.31546843826014,-4.89272403562093E-16));
#57169=CARTESIAN_POINT('Ctrl Pts',(-3.82380434918523,4.34209269619914,-5.55111512312578E-16));
#57170=CARTESIAN_POINT('Ctrl Pts',(-3.8018891935949,4.36487083732063,-6.11439561487415E-16));
#57171=CARTESIAN_POINT('Ctrl Pts',(-3.77977994088804,4.38747952479312,1.3621248594443E-16));
#57172=CARTESIAN_POINT('Ctrl Pts',(-3.75749701858742,4.40989850208082,1.11022302462516E-16));
#57173=CARTESIAN_POINT('Ctrl Pts',(-3.64082422534835,4.52728367564249,-2.08728336147496E-17));
#57174=CARTESIAN_POINT('Ctrl Pts',(-3.5192998591356,4.63956980826707,-2.21183261000239E-15));
#57175=CARTESIAN_POINT('Ctrl Pts',(-3.39330838152807,4.74648957497586,-4.10782519111308E-15));
#57176=CARTESIAN_POINT('Ctrl Pts',(-3.26677453657137,4.85386960924834,-6.0119796295953E-15));
#57177=CARTESIAN_POINT('Ctrl Pts',(-3.13573457516067,4.95583757780676,-8.63900142651335E-15));
#57178=CARTESIAN_POINT('Ctrl Pts',(-3.00053335242381,5.05209514857636,-1.06581410364015E-14));
#57179=CARTESIAN_POINT('Ctrl Pts',(-2.86569963082772,5.14809107402686,-1.26717922631599E-14));
#57180=CARTESIAN_POINT('Ctrl Pts',(-2.72672672727089,5.23840818298683,-1.44182212246245E-14));
#57181=CARTESIAN_POINT('Ctrl Pts',(-2.58391981634373,5.3227144339337,-1.4432899320127E-14));
#57182=CARTESIAN_POINT('Ctrl Pts',(-2.85728222003707,-4.00342940649516,
-1.52221985016965E-15));
#57183=CARTESIAN_POINT('Ctrl Pts',(-2.28500641414625,-4.41104155800517,
0.0397943477746339));
#57184=CARTESIAN_POINT('Ctrl Pts',(-0.854537515415942,-5.02713941244452,
0.125979848023253));
#57185=CARTESIAN_POINT('Ctrl Pts',(1.5567708799336,-4.88563546465558,0.258556500745857));
#57186=CARTESIAN_POINT('Ctrl Pts',(3.70738228326065,-3.54233751270576,0.39772995816781));
#57187=CARTESIAN_POINT('Ctrl Pts',(4.95140614815209,-1.33283639810976,0.536903415589762));
#57188=CARTESIAN_POINT('Ctrl Pts',(4.98463903712129,1.20260146313003,0.676076873011714));
#57189=CARTESIAN_POINT('Ctrl Pts',(3.79895229578282,3.44395520585394,0.815250330433666));
#57190=CARTESIAN_POINT('Ctrl Pts',(1.68428893605082,4.84314423609996,0.954423787855619));
#57191=CARTESIAN_POINT('Ctrl Pts',(-0.842242278542283,5.05801321348077,
1.09359724527757));
#57192=CARTESIAN_POINT('Ctrl Pts',(-3.16281564529539,4.03602149408518,1.23277070269952));
#57193=CARTESIAN_POINT('Ctrl Pts',(-4.61370980268822,2.15207184328641,1.36328514227675));
#57194=CARTESIAN_POINT('Ctrl Pts',(-4.91768134020962,0.666110914719361,
1.44740842938));
#57195=CARTESIAN_POINT('Ctrl Pts',(-4.91836475234218,-0.000121599733084975,
1.48514056400926));
#57196=CARTESIAN_POINT('Origin',(0.,0.,-3.23514056400933));
#57197=CARTESIAN_POINT('',(2.85706463458462,-4.00329423553976,0.));
#57198=CARTESIAN_POINT('Origin',(0.,0.,0.));
#57199=CARTESIAN_POINT('Ctrl Pts',(2.85706463458441,-4.0032942355399,0.));
#57200=CARTESIAN_POINT('Ctrl Pts',(3.52386294776537,-3.52741468062806,0.046391152473984));
#57201=CARTESIAN_POINT('Ctrl Pts',(4.61438908619534,-2.23650256226449,0.139173457421952));
#57202=CARTESIAN_POINT('Ctrl Pts',(5.12163790500659,0.248365779535813,0.278346914843904));
#57203=CARTESIAN_POINT('Ctrl Pts',(4.37650875504895,2.67182739135543,0.417520372265856));
#57204=CARTESIAN_POINT('Ctrl Pts',(2.56115201646861,4.44226470421493,0.556693829687809));
#57205=CARTESIAN_POINT('Ctrl Pts',(0.119512633872891,5.12624413067081,0.695867287109761));
#57206=CARTESIAN_POINT('Ctrl Pts',(-2.35135624542669,4.55676348086115,0.835040744531713));
#57207=CARTESIAN_POINT('Ctrl Pts',(-4.24723382866677,2.87295023988583,0.974214201953666));
#57208=CARTESIAN_POINT('Ctrl Pts',(-4.8731083061567,1.13076638505056,1.07582043244));
#57209=CARTESIAN_POINT('Ctrl Pts',(-4.91851593873139,0.155927429260441,
1.13103551045236));
#57210=CARTESIAN_POINT('Ctrl Pts',(-4.91835559909507,0.00012341875379537,
1.13985943599073));
#57211=CARTESIAN_POINT('Ctrl Pts',(3.43710408716079,-4.81604049573118,-0.576484243785842));
#57212=CARTESIAN_POINT('Ctrl Pts',(4.23927537156343,-4.24354817498196,-0.530093091311858));
#57213=CARTESIAN_POINT('Ctrl Pts',(5.55119943592679,-2.69055589595426,-0.43731078636389));
#57214=CARTESIAN_POINT('Ctrl Pts',(6.16142958866421,0.298788842793687,-0.298137328941937));
#57215=CARTESIAN_POINT('Ctrl Pts',(5.26502479061354,3.21426009613248,-0.158963871519986));
#57216=CARTESIAN_POINT('Ctrl Pts',(3.08111547673245,5.34413047093264,-0.0197904140980329));
#57217=CARTESIAN_POINT('Ctrl Pts',(0.143776013107478,6.16697096734542,0.119383043323919));
#57218=CARTESIAN_POINT('Ctrl Pts',(-2.82872710112941,5.48187471669485,0.258556500745872));
#57219=CARTESIAN_POINT('Ctrl Pts',(-5.10950455055458,3.45621477798876,0.397729958167823));
#57220=CARTESIAN_POINT('Ctrl Pts',(-6.14083048116305,0.58541647896675,0.536903415589776));
#57221=CARTESIAN_POINT('Ctrl Pts',(-5.67050742409554,-2.42855065362853,
0.676076873011728));
#57222=CARTESIAN_POINT('Ctrl Pts',(-3.81354694446943,-4.84864486784236,
0.815250330433681));
#57223=CARTESIAN_POINT('Ctrl Pts',(-1.02404039718864,-6.08307916434686,
0.954423787855633));
#57224=CARTESIAN_POINT('Ctrl Pts',(2.01587981812662,-5.82998553179797,1.09359724527759));
#57225=CARTESIAN_POINT('Ctrl Pts',(4.56284681947448,-4.15125708628714,1.23277070269954));
#57226=CARTESIAN_POINT('Ctrl Pts',(5.99403783840857,-1.45740030245642,1.37194416012149));
#57227=CARTESIAN_POINT('Ctrl Pts',(5.95947655212953,1.59284167705623,1.51111761754344));
#57228=CARTESIAN_POINT('Ctrl Pts',(4.46761438646609,4.25357817423206,1.65029107496539));
#57229=CARTESIAN_POINT('Ctrl Pts',(1.88326393488574,5.87416567017125,1.78946453238735));
#57230=CARTESIAN_POINT('Ctrl Pts',(-1.16161055136132,6.05831382819653,1.9286379898093));
#57231=CARTESIAN_POINT('Ctrl Pts',(-3.9224305471212,4.76099191815651,2.06781144723125));
#57232=CARTESIAN_POINT('Ctrl Pts',(-5.72407880918856,2.29944063955624,2.2069849046532));
#57233=CARTESIAN_POINT('Ctrl Pts',(-6.12598919626941,-0.724404466168149,
2.34615836207515));
#57234=CARTESIAN_POINT('Ctrl Pts',(-5.02988053374446,-3.57110729008621,
2.48533181949711));
#57235=CARTESIAN_POINT('Ctrl Pts',(-2.70378980360807,-5.54454922987053,
2.62450527691906));
#57236=CARTESIAN_POINT('Ctrl Pts',(0.283472290417655,-6.16215456821602,
2.76367873434101));
#57237=CARTESIAN_POINT('Ctrl Pts',(3.20141547489109,-5.2728971562611,2.90285219176296));
#57238=CARTESIAN_POINT('Ctrl Pts',(5.33650037903085,-3.09423159563492,3.04202564918492));
#57239=CARTESIAN_POINT('Ctrl Pts',(6.16662391766363,-0.158917969608813,
3.18119910660686));
#57240=CARTESIAN_POINT('Ctrl Pts',(5.48879179310159,2.8152566694643,3.32037256402882));
#57241=CARTESIAN_POINT('Ctrl Pts',(3.46875771508856,5.10100238942732,3.45954602145077));
#57242=CARTESIAN_POINT('Ctrl Pts',(0.600490809753028,6.13937425560414,3.59871947887272));
#57243=CARTESIAN_POINT('Ctrl Pts',(-2.41461714335042,5.67645395594698,3.73789293629468));
#57244=CARTESIAN_POINT('Ctrl Pts',(-4.83926658230211,3.82544172722223,3.87706639371663));
#57245=CARTESIAN_POINT('Ctrl Pts',(-6.08054574508388,1.03897492986976,4.01623985113858));
#57246=CARTESIAN_POINT('Ctrl Pts',(-5.83491837456198,-2.0015576497205,4.15541330856054));
#57247=CARTESIAN_POINT('Ctrl Pts',(-4.16244897107871,-4.55263923742286,
4.29458676598249));
#57248=CARTESIAN_POINT('Ctrl Pts',(-1.47211491710019,-5.99044097991182,
4.43376022340444));
#57249=CARTESIAN_POINT('Ctrl Pts',(1.57820282580624,-5.96336996199074,4.57293368082639));
#57250=CARTESIAN_POINT('Ctrl Pts',(4.24259466815234,-4.47804599627128,4.71210713824835));
#57251=CARTESIAN_POINT('Ctrl Pts',(5.86952342828491,-1.89768284699277,4.85128059567029));
#57252=CARTESIAN_POINT('Ctrl Pts',(6.06114800705314,1.14673026451377,4.99045405309225));
#57253=CARTESIAN_POINT('Ctrl Pts',(4.77060947927874,3.91072763807093,5.1296275105142));
#57254=CARTESIAN_POINT('Ctrl Pts',(2.31348974317856,5.71841504887182,5.26880096793615));
#57255=CARTESIAN_POINT('Ctrl Pts',(-0.709359313623553,6.12774957281476,
5.40797442535811));
#57256=CARTESIAN_POINT('Ctrl Pts',(-3.55874515805866,5.03863457326983,5.54714788278005));
#57257=CARTESIAN_POINT('Ctrl Pts',(-5.53789309166834,2.71739683671858,5.68632134020202));
#57258=CARTESIAN_POINT('Ctrl Pts',(-6.16283208352363,-0.268339660221467,
5.82549479762395));
#57259=CARTESIAN_POINT('Ctrl Pts',(-5.28074264852207,-3.18845770601339,
5.96466825504592));
#57260=CARTESIAN_POINT('Ctrl Pts',(-3.10732656720241,-5.32888610008828,
6.10384171246786));
#57261=CARTESIAN_POINT('Ctrl Pts',(-0.174060240924557,-6.16621508670314,
6.24301516988982));
#57262=CARTESIAN_POINT('Ctrl Pts',(2.80176991436952,-5.49568838362309,6.38218862731176));
#57263=CARTESIAN_POINT('Ctrl Pts',(5.0924691348527,-3.48127326901073,6.52136208473373));
#57264=CARTESIAN_POINT('Ctrl Pts',(6.13788118133806,-0.615564835522726,
6.66053554215567));
#57265=CARTESIAN_POINT('Ctrl Pts',(5.68236617097953,2.40067077331804,6.79970899957763));
#57266=CARTESIAN_POINT('Ctrl Pts',(3.83731348777568,4.82985824424392,6.93888245699957));
#57267=CARTESIAN_POINT('Ctrl Pts',(1.05390317443291,6.07797610737952,7.07805591442153));
#57268=CARTESIAN_POINT('Ctrl Pts',(-1.98722340011894,5.83981580368557,7.21722937184348));
#57269=CARTESIAN_POINT('Ctrl Pts',(-4.54240420916778,4.17361587397437,7.35640282926544));
#57270=CARTESIAN_POINT('Ctrl Pts',(-5.98680799610826,1.48682059465498,7.49557628668739));
#57271=CARTESIAN_POINT('Ctrl Pts',(-5.96722741450003,-1.5635544271292,7.63474974410934));
#57272=CARTESIAN_POINT('Ctrl Pts',(-4.48845060276677,-4.23158559519698,
7.77392320153129));
#57273=CARTESIAN_POINT('Ctrl Pts',(-1.91209031654676,-5.86484578521245,
7.91309665895325));
#57274=CARTESIAN_POINT('Ctrl Pts',(1.13184306313101,-6.06394564152732,8.0522701163752));
#57275=CARTESIAN_POINT('Ctrl Pts',(3.89900114733389,-4.78019827162483,8.19144357379714));
#57276=CARTESIAN_POINT('Ctrl Pts',(5.71271680673197,-2.32752489761939,8.33061703121911));
#57277=CARTESIAN_POINT('Ctrl Pts',(6.12947299917573,0.694309884224369,8.46979048864104));
#57278=CARTESIAN_POINT('Ctrl Pts',(5.04735822998721,3.54636156661111,8.60896394606302));
#57279=CARTESIAN_POINT('Ctrl Pts',(2.73098748399595,5.53120356027632,8.74813740348494));
#57280=CARTESIAN_POINT('Ctrl Pts',(-0.25320541194086,6.16347243705364,8.88731086090693));
#57281=CARTESIAN_POINT('Ctrl Pts',(-3.17548071082857,5.28855629809418,9.02648431832885));
#57282=CARTESIAN_POINT('Ctrl Pts',(-5.32123968811336,3.12040280165932,9.16565777575082));
#57283=CARTESIAN_POINT('Ctrl Pts',(-6.16576907364188,0.189201462672217,
9.30483123317277));
#57284=CARTESIAN_POINT('Ctrl Pts',(-5.50255183529998,-2.78826626468724,
9.44400469059472));
#57285=CARTESIAN_POINT('Ctrl Pts',(-3.4937678309544,-5.08390517283163,9.58317814801667));
#57286=CARTESIAN_POINT('Ctrl Pts',(-0.630635149453913,-6.13635109582472,
9.72235160543862));
#57287=CARTESIAN_POINT('Ctrl Pts',(2.38670992730932,-5.68824412150526,9.86152506286057));
#57288=CARTESIAN_POINT('Ctrl Pts',(4.82042078227819,-3.84916210943844,10.0006985202825));
#57289=CARTESIAN_POINT('Ctrl Pts',(6.07536981965241,-1.0688250639897,10.1398719777045));
#57290=CARTESIAN_POINT('Ctrl Pts',(5.84467801888626,1.97287716761684,10.2790454351264));
#57291=CARTESIAN_POINT('Ctrl Pts',(4.18475761008524,4.53214179034479,10.4182188925484));
#57292=CARTESIAN_POINT('Ctrl Pts',(1.50151730672395,5.98313891202306,10.5573923499703));
#57293=CARTESIAN_POINT('Ctrl Pts',(-1.54889660026354,5.97104888479805,10.6965658073923));
#57294=CARTESIAN_POINT('Ctrl Pts',(-4.22055100590104,4.49882814403304,10.8357392648142));
#57295=CARTESIAN_POINT('Ctrl Pts',(-5.86013277728699,1.92648625625064,10.9749127222362));
#57296=CARTESIAN_POINT('Ctrl Pts',(-6.0667067105821,-1.11694903676676,11.1140861796581));
#57297=CARTESIAN_POINT('Ctrl Pts',(-4.78975823951158,-3.887251145731,11.2532596370801));
#57298=CARTESIAN_POINT('Ctrl Pts',(-2.34154601715145,-5.70698411707254,
11.3924330945021));
#57299=CARTESIAN_POINT('Ctrl Pts',(0.679256268156358,-6.13115946498918,
11.531606551924));
#57300=CARTESIAN_POINT('Ctrl Pts',(3.53395659070436,-5.05605145127828,11.670780009346));
#57301=CARTESIAN_POINT('Ctrl Pts',(5.52448067588446,-2.74456166349661,11.8099534667679));
#57302=CARTESIAN_POINT('Ctrl Pts',(6.16407562502046,0.238069636838827,11.9491269241898));
#57303=CARTESIAN_POINT('Ctrl Pts',(5.29633805782252,3.16248456758555,12.0883003816118));
#57304=CARTESIAN_POINT('Ctrl Pts',(3.13346022017625,5.31356118921473,12.2274738390338));
#57305=CARTESIAN_POINT('Ctrl Pts',(0.204341543540447,6.16528588116882,12.3666472964557));
#57306=CARTESIAN_POINT('Ctrl Pts',(-2.77474580183883,5.50938210674607,12.5058207538777));
#57307=CARTESIAN_POINT('Ctrl Pts',(-5.07531055500723,3.50624132557761,12.6449942112996));
#57308=CARTESIAN_POINT('Ctrl Pts',(-6.13478400828913,0.645701660673112,
12.7841676687216));
#57309=CARTESIAN_POINT('Ctrl Pts',(-5.69408777208102,-2.37273468950772,
12.9233411261435));
#57310=CARTESIAN_POINT('Ctrl Pts',(-3.8609875207634,-4.81095425331247,13.0625145835655));
#57311=CARTESIAN_POINT('Ctrl Pts',(-1.08374050856188,-6.07272689761841,
13.2016880409874));
#57312=CARTESIAN_POINT('Ctrl Pts',(1.95851903872161,-5.84950499084504,13.3408614984094));
#57313=CARTESIAN_POINT('Ctrl Pts',(4.52185204283595,-4.19587411222696,13.4800349558314));
#57314=CARTESIAN_POINT('Ctrl Pts',(5.97943374978069,-1.51620496468635,13.6192084132533));
#57315=CARTESIAN_POINT('Ctrl Pts',(5.97483434984145,1.53422943359551,13.7583818706753));
#57316=CARTESIAN_POINT('Ctrl Pts',(4.50917855749375,4.20949096680282,13.8975553280972));
#57317=CARTESIAN_POINT('Ctrl Pts',(1.94087057929726,5.8553844329279,14.0367287855192));
#57318=CARTESIAN_POINT('Ctrl Pts',(-1.10204827523175,6.06943119756825,14.1759022429411));
#57319=CARTESIAN_POINT('Ctrl Pts',(-3.87547770411452,4.79928932529257,14.315075700363));
#57320=CARTESIAN_POINT('Ctrl Pts',(-5.70121701446153,2.35555301722769,14.454249157785));
#57321=CARTESIAN_POINT('Ctrl Pts',(-6.13280896008574,-0.664198556192439,
14.5934226152069));
#57322=CARTESIAN_POINT('Ctrl Pts',(-5.06471418472317,-3.52153030514006,
14.7325960726289));
#57323=CARTESIAN_POINT('Ctrl Pts',(-2.75811929336864,-5.51772447903153,
14.8717695300509));
#57324=CARTESIAN_POINT('Ctrl Pts',(0.222932426183668,-6.16464164378691,
15.0109429874728));
#57325=CARTESIAN_POINT('Ctrl Pts',(3.14946935465071,-5.30408788078328,15.1501164448948));
#57326=CARTESIAN_POINT('Ctrl Pts',(5.30585064969353,-3.14649874401734,15.2892899023167));
#57327=CARTESIAN_POINT('Ctrl Pts',(6.16476551219756,-0.21948039223499,15.4284633597387));
#57328=CARTESIAN_POINT('Ctrl Pts',(5.51617915677505,2.7612086073523,15.5676368171606));
#57329=CARTESIAN_POINT('Ctrl Pts',(3.51869367766553,5.06668533320481,15.7068102745826));
#57330=CARTESIAN_POINT('Ctrl Pts',(0.660764278329698,6.13317992818077,15.8459837320045));
#57331=CARTESIAN_POINT('Ctrl Pts',(-2.35874514418357,5.69989708746978,15.9851571894265));
#57332=CARTESIAN_POINT('Ctrl Pts',(-4.8014587144297,3.8727896504436,16.1243306468484));
#57333=CARTESIAN_POINT('Ctrl Pts',(-6.07004735721424,1.09864941820965,16.2635041042704));
#57334=CARTESIAN_POINT('Ctrl Pts',(-5.85429669045541,-1.94414910001237,
16.4026775616923));
#57335=CARTESIAN_POINT('Ctrl Pts',(-4.20696531336737,-4.51153502868811,
16.5418510191143));
#57336=CARTESIAN_POINT('Ctrl Pts',(-1.53088347997605,-5.9756925317232,16.6810244765362));
#57337=CARTESIAN_POINT('Ctrl Pts',(1.51955301556766,-5.97858378680396,16.8201979339582));
#57338=CARTESIAN_POINT('Ctrl Pts',(4.19840554459396,-4.51950178073632,16.9593713913801));
#57339=CARTESIAN_POINT('Ctrl Pts',(5.85060078076748,-1.95524319894966,17.0985448488021));
#57340=CARTESIAN_POINT('Ctrl Pts',(6.07211908605725,1.0871408683769,17.2377183062241));
#57341=CARTESIAN_POINT('Ctrl Pts',(4.80879147149576,3.86368089347784,17.376891763646));
#57342=CARTESIAN_POINT('Ctrl Pts',(2.36954581338641,5.69541553367435,17.516065221068));
#57343=CARTESIAN_POINT('Ctrl Pts',(-0.649136839130126,6.13442147451903,
17.6552386784899));
#57344=CARTESIAN_POINT('Ctrl Pts',(-3.50908278484838,5.07334637808584,17.7944121359118));
#57345=CARTESIAN_POINT('Ctrl Pts',(-5.51093501045721,2.77166029185993,17.9335855933338));
#57346=CARTESIAN_POINT('Ctrl Pts',(-6.16517048993992,-0.20779387125234,
18.0727590507557));
#57347=CARTESIAN_POINT('Ctrl Pts',(-5.31180572024526,-3.13643515050539,
18.2119325081777));
#57348=CARTESIAN_POINT('Ctrl Pts',(-3.15951829456067,-5.29810811604411,
18.3511059655997));
#57349=CARTESIAN_POINT('Ctrl Pts',(-0.234617917469024,-6.16420796986592,
18.4902794230216));
#57350=CARTESIAN_POINT('Ctrl Pts',(2.74765476285655,-5.5229429444009,18.6294528804436));
#57351=CARTESIAN_POINT('Ctrl Pts',(5.05802955943419,-3.53112481213083,18.7686263378655));
#57352=CARTESIAN_POINT('Ctrl Pts',(6.1315388651722,-0.675822911596517,18.9077997952875));
#57353=CARTESIAN_POINT('Ctrl Pts',(5.70567203264151,2.3447413756934,19.0469732527094));
#57354=CARTESIAN_POINT('Ctrl Pts',(3.88456842731257,4.7919342228877,19.1861467101314));
#57355=CARTESIAN_POINT('Ctrl Pts',(1.11355170303273,6.06733121459748,19.3253201675533));
#57356=CARTESIAN_POINT('Ctrl Pts',(-1.92976743813947,5.85905308882354,19.4644936249753));
#57357=CARTESIAN_POINT('Ctrl Pts',(-4.50119081011263,4.21803114662679,19.6036670823972));
#57358=CARTESIAN_POINT('Ctrl Pts',(-5.97191528041001,1.54555276408195,19.7428405398192));
#57359=CARTESIAN_POINT('Ctrl Pts',(-5.9822971730766,-1.50486743467848,19.8820139972411));
#57360=CARTESIAN_POINT('Ctrl Pts',(-4.52979775151187,-4.18729480611934,
20.0211874546631));
#57361=CARTESIAN_POINT('Ctrl Pts',(-1.96960402854123,-5.84578184965109,
20.160360912085));
#57362=CARTESIAN_POINT('Ctrl Pts',(1.07222690609371,-6.07477035984117,20.299534369507));
#57363=CARTESIAN_POINT('Ctrl Pts',(3.85186078495554,-4.81826462082334,20.4387078269289));
#57364=CARTESIAN_POINT('Ctrl Pts',(5.6895797096938,-2.38352432125133,20.5778812843509));
#57365=CARTESIAN_POINT('Ctrl Pts',(6.13599699856562,0.634071207791177,20.7170547417728));
#57366=CARTESIAN_POINT('Ctrl Pts',(5.08194797931441,3.49661410488748,20.8562281991948));
#57367=CARTESIAN_POINT('Ctrl Pts',(2.78518457731863,5.50411231110181,20.9954016566167));
#57368=CARTESIAN_POINT('Ctrl Pts',(-0.192654063329878,6.16566216029053,
21.1345751140387));
#57369=CARTESIAN_POINT('Ctrl Pts',(-3.12338203374549,5.31949152967011,21.2737485714607));
#57370=CARTESIAN_POINT('Ctrl Pts',(-5.29033363495371,3.1725187932987,21.4129220288826));
#57371=CARTESIAN_POINT('Ctrl Pts',(-6.16361325753588,0.249754027963704,
21.5520954863046));
#57372=CARTESIAN_POINT('Ctrl Pts',(-5.52967342883816,-2.73408435008088,
21.6912689437265));
#57373=CARTESIAN_POINT('Ctrl Pts',(-3.54353465401414,-5.04934328588946,
21.8304424011485));
#57374=CARTESIAN_POINT('Ctrl Pts',(-0.69087746967043,-6.12986082915899,
21.9696158585704));
#57375=CARTESIAN_POINT('Ctrl Pts',(2.33072346847955,-5.71141257277345,22.1087893159923));
#57376=CARTESIAN_POINT('Ctrl Pts',(4.78238083611889,-3.89632378034461,22.2479627734144));
#57377=CARTESIAN_POINT('Ctrl Pts',(6.06457848614637,-1.12844727317076,22.3871362308362));
#57378=CARTESIAN_POINT('Ctrl Pts',(5.8637741572685,1.91537413982392,22.5263096882583));
#57379=CARTESIAN_POINT('Ctrl Pts',(4.22907154527857,4.49081944948481,22.6654831456801));
#57380=CARTESIAN_POINT('Ctrl Pts',(1.56021272854873,5.96810201861786,22.8046566031022));
#57381=CARTESIAN_POINT('Ctrl Pts',(-1.49017277948154,5.98597448626773,22.9438300605241));
#57382=CARTESIAN_POINT('Ctrl Pts',(-4.17615881837635,4.54006640773607,23.0830035179461));
#57383=CARTESIAN_POINT('Ctrl Pts',(-5.84092766863672,1.98395298147663,23.222176975368));
#57384=CARTESIAN_POINT('Ctrl Pts',(-6.07738500293291,-1.05730647831276,
23.36135043279));
#57385=CARTESIAN_POINT('Ctrl Pts',(-4.82770871615259,-3.84001744982238,
23.5005238902119));
#57386=CARTESIAN_POINT('Ctrl Pts',(-2.39748845653263,-5.68370957770968,
23.6396973476339));
#57387=CARTESIAN_POINT('Ctrl Pts',(0.619001753020852,-6.13753552272517,
23.7788708050558));
#57388=CARTESIAN_POINT('Ctrl Pts',(3.48412434044316,-5.0905189365415,23.9180442624778));
#57389=CARTESIAN_POINT('Ctrl Pts',(5.49725642210601,-2.79869206819369,24.0572177198997));
#57390=CARTESIAN_POINT('Ctrl Pts',(6.166116651874,0.177513093708911,24.1963911773217));
#57391=CARTESIAN_POINT('Ctrl Pts',(5.32714526271259,3.11031008308092,24.3355646347436));
#57392=CARTESIAN_POINT('Ctrl Pts',(3.18550016183881,5.28252725330224,24.4747380921656));
#57393=CARTESIAN_POINT('Ctrl Pts',(0.264888632448706,6.1629813787935,24.6139115495875));
#57394=CARTESIAN_POINT('Ctrl Pts',(-2.72049745085447,5.53637056950222,24.7530850070095));
#57395=CARTESIAN_POINT('Ctrl Pts',(-5.04062656494859,3.55592312848445,24.8922584644314));
#57396=CARTESIAN_POINT('Ctrl Pts',(-6.12814583025965,0.705927861772895,
25.0314319218534));
#57397=CARTESIAN_POINT('Ctrl Pts',(-5.71711867325033,-2.3166915070696,25.1706053792753));
#57398=CARTESIAN_POINT('Ctrl Pts',(-3.90805563865528,-4.77279861172988,
25.3097788366973));
#57399=CARTESIAN_POINT('Ctrl Pts',(-1.14333603880389,-6.06178918845982,
25.4489522941192));
#57400=CARTESIAN_POINT('Ctrl Pts',(1.90096929185687,-5.86845986732236,25.5881257515412));
#57401=CARTESIAN_POINT('Ctrl Pts',(4.48042100934369,-4.24008644274946,25.7272992089631));
#57402=CARTESIAN_POINT('Ctrl Pts',(5.96425276934059,-1.5748632849772,25.8664726663851));
#57403=CARTESIAN_POINT('Ctrl Pts',(5.98961570420329,1.47546913858521,26.0056461238071));
#57404=CARTESIAN_POINT('Ctrl Pts',(4.55030768748918,4.16499764851469,26.144819581229));
#57405=CARTESIAN_POINT('Ctrl Pts',(1.99828997123208,5.83603826699494,26.2839930386509));
#57406=CARTESIAN_POINT('Ctrl Pts',(-1.04237967500393,6.07996299956626,26.4231664960729));
#57407=CARTESIAN_POINT('Ctrl Pts',(-3.82815095949345,4.83712370053581,26.5623399534948));
#57408=CARTESIAN_POINT('Ctrl Pts',(-5.67780517311883,2.41143813502674,26.7015134109168));
#57409=CARTESIAN_POINT('Ctrl Pts',(-6.13903703772037,-0.603928565687683,
26.8406868683387));
#57410=CARTESIAN_POINT('Ctrl Pts',(-5.09905919808441,-3.47161356682837,
26.9798603257607));
#57411=CARTESIAN_POINT('Ctrl Pts',(-2.81218268303532,-5.49036738481062,
27.1190337831827));
#57412=CARTESIAN_POINT('Ctrl Pts',(0.162371053689043,-6.16653396194977,
27.2582072406046));
#57413=CARTESIAN_POINT('Ctrl Pts',(3.09721937733518,-5.33476687322094,27.3973806980266));
#57414=CARTESIAN_POINT('Ctrl Pts',(5.27468901816195,-3.19846232190371,27.5365541554485));
#57415=CARTESIAN_POINT('Ctrl Pts',(6.16231233744904,-0.280021639662804,
27.6757276128705));
#57416=CARTESIAN_POINT('Ctrl Pts',(5.54303432600949,2.70689414710596,27.8149010702924));
#57417=CARTESIAN_POINT('Ctrl Pts',(3.56829016083962,5.03187944917316,27.9540745277144));
#57418=CARTESIAN_POINT('Ctrl Pts',(0.720973997150462,6.12639387881557,28.0932479851363));
#57419=CARTESIAN_POINT('Ctrl Pts',(-2.30264557607587,5.72279029966451,28.2324214425583));
#57420=CARTESIAN_POINT('Ctrl Pts',(-4.76318760750126,3.9197639315018,28.3715948999802));
#57421=CARTESIAN_POINT('Ctrl Pts',(-6.05896333835717,1.15821791015328,28.5107683574022));
#57422=CARTESIAN_POINT('Ctrl Pts',(-5.87311019073044,-1.88655298109917,
28.6499418148241));
#57423=CARTESIAN_POINT('Ctrl Pts',(-4.25107577261991,-4.46999555239154,
28.7891152722461));
#57424=CARTESIAN_POINT('Ctrl Pts',(-1.58950434502494,-5.96036755578906,
28.9282887296681));
#57425=CARTESIAN_POINT('Ctrl Pts',(1.46075660065201,-5.99322080492681,29.06746218709));
#57426=CARTESIAN_POINT('Ctrl Pts',(4.15381136383588,-4.56052152901661,29.2066356445119));
#57427=CARTESIAN_POINT('Ctrl Pts',(5.8311136742087,-2.01261491135594,29.3458091019339));
#57428=CARTESIAN_POINT('Ctrl Pts',(6.08250433419597,1.02744658617533,29.4849825593558));
#57429=CARTESIAN_POINT('Ctrl Pts',(4.84650951720095,3.81626138552335,29.6241560167778));
#57430=CARTESIAN_POINT('Ctrl Pts',(2.42537327261766,5.67186653152452,29.7633294741997));
#57431=CARTESIAN_POINT('Ctrl Pts',(-0.588851736682384,6.14050153449717,
29.9025029316217));
#57432=CARTESIAN_POINT('Ctrl Pts',(-3.4590818594826,5.10756871244572,30.0416763890437));
#57433=CARTESIAN_POINT('Ctrl Pts',(-5.48344524075633,2.82565634049557,30.1808498464656));
#57434=CARTESIAN_POINT('Ctrl Pts',(-6.16691408800147,-0.147228034576321,
30.3200233038876));
#57435=CARTESIAN_POINT('Ctrl Pts',(-5.34235631523705,-3.08410999544485,
30.4591967613095));
#57436=CARTESIAN_POINT('Ctrl Pts',(-3.21140519533195,-5.26681897679718,
30.5983702187315));
#57437=CARTESIAN_POINT('Ctrl Pts',(-0.295152958354393,-6.16160613753677,
30.7375436761534));
#57438=CARTESIAN_POINT('Ctrl Pts',(2.69327452086287,-5.54966465817772,30.8767171335754));
#57439=CARTESIAN_POINT('Ctrl Pts',(5.02310199130804,-3.5806356765068,31.0158905909973));
#57440=CARTESIAN_POINT('Ctrl Pts',(6.12460498539096,-0.736015785075372,
31.1550640484193));
#57441=CARTESIAN_POINT('Ctrl Pts',(5.72842741781626,2.28858576019494,31.2942375058412));
#57442=CARTESIAN_POINT('Ctrl Pts',(3.9314485882835,4.75354788138709,31.4334109632632));
#57443=CARTESIAN_POINT('Ctrl Pts',(1.17309279748168,6.05610095287823,31.5725844206851));
#57444=CARTESIAN_POINT('Ctrl Pts',(-1.87212529448077,5.87772509945144,31.7117578781071));
#57445=CARTESIAN_POINT('Ctrl Pts',(-4.45954314149362,4.26203946862453,31.850931335529));
#57446=CARTESIAN_POINT('Ctrl Pts',(-5.95644640139103,1.6041358204067,31.990104792951));
#57447=CARTESIAN_POINT('Ctrl Pts',(-5.99678976669964,-1.44603525439822,
32.1292782503729));
#57448=CARTESIAN_POINT('Ctrl Pts',(-4.57070787072909,-4.14260003179297,
32.2684517077949));
#57449=CARTESIAN_POINT('Ctrl Pts',(-2.02692771546916,-5.82615391997319,
32.4076251652168));
#57450=CARTESIAN_POINT('Ctrl Pts',(1.0125073018732,-6.08500899149783,32.5467986226388));
#57451=CARTESIAN_POINT('Ctrl Pts',(3.80434879960589,-4.85586610955176,32.6859720800607));
#57452=CARTESIAN_POINT('Ctrl Pts',(5.66589368873668,-2.43929378527674,32.8251455374827));
#57453=CARTESIAN_POINT('Ctrl Pts',(6.14192900422469,0.573771356918033,32.9643189949047));
#57454=CARTESIAN_POINT('Ctrl Pts',(5.11604742831312,3.44652929397193,33.1034924523266));
#57455=CARTESIAN_POINT('Ctrl Pts',(2.83911295932849,5.47649003168353,33.2426659097486));
#57456=CARTESIAN_POINT('Ctrl Pts',(-0.132084127682804,6.16725702773691,
33.3818393671704));
#57457=CARTESIAN_POINT('Ctrl Pts',(-3.07098201645912,5.34991354299681,33.5210128245925));
#57458=CARTESIAN_POINT('Ctrl Pts',(-5.25891717666406,3.22432870407837,33.6601862820144));
#57459=CARTESIAN_POINT('Ctrl Pts',(-6.16086278331505,0.310282497282057,
33.7993597394364));
#57460=CARTESIAN_POINT('Ctrl Pts',(-5.5562615260262,-2.67963865425116,33.9385331968583));
#57461=CARTESIAN_POINT('Ctrl Pts',(-3.59295960104287,-5.01429424428103,
34.0777066542803));
#57462=CARTESIAN_POINT('Ctrl Pts',(-0.751053134846073,-6.12277916077282,
34.2168801117022));
#57463=CARTESIAN_POINT('Ctrl Pts',(2.27451214420708,-5.7340299937139,34.3560535691242));
#57464=CARTESIAN_POINT('Ctrl Pts',(4.74387949151463,-3.94310953854224,34.4952270265461));
#57465=CARTESIAN_POINT('Ctrl Pts',(6.05320204928312,-1.18796061109394,34.6344004839681));
#57466=CARTESIAN_POINT('Ctrl Pts',(5.88230456565756,1.85768631900013,34.7735739413901));
#57467=CARTESIAN_POINT('Ctrl Pts',(4.27297746465269,4.44906383967755,34.912747398812));
#57468=CARTESIAN_POINT('Ctrl Pts',(1.61875762289533,5.95248932979087,35.0519208562339));
#57469=CARTESIAN_POINT('Ctrl Pts',(-1.43130518859287,6.00032256800109,35.1910943136559));
#57470=CARTESIAN_POINT('Ctrl Pts',(-4.13136371998978,4.58086665120348,35.3302677710778));
#57471=CARTESIAN_POINT('Ctrl Pts',(-5.8211590341955,2.04122829726617,35.4694412284998));
#57472=CARTESIAN_POINT('Ctrl Pts',(-6.0874769563689,-0.997561912180709,
35.6086146859218));
#57473=CARTESIAN_POINT('Ctrl Pts',(-4.86519342116839,-3.79241327357342,
35.7477881433437));
#57474=CARTESIAN_POINT('Ctrl Pts',(-2.45319958906397,-5.65988668077129,
35.8869616007657));
#57475=CARTESIAN_POINT('Ctrl Pts',(0.558687517328578,-6.14331943829534,
36.0261350581876));
#57476=CARTESIAN_POINT('Ctrl Pts',(3.43395594598768,-5.12449529456042,36.1653085156095));
#57477=CARTESIAN_POINT('Ctrl Pts',(5.46950179953183,-2.85255245839129,36.3044819730315));
#57478=CARTESIAN_POINT('Ctrl Pts',(6.16756277908821,0.116939424325645,36.4436554304534));
#57479=CARTESIAN_POINT('Ctrl Pts',(5.3574385109304,3.05783551953926,36.5828288878754));
#57480=CARTESIAN_POINT('Ctrl Pts',(3.23723277021465,5.25098366541017,36.7220023452973));
#57481=CARTESIAN_POINT('Ctrl Pts',(0.32541016521519,6.1600822792663,36.8611758027193));
#57482=CARTESIAN_POINT('Ctrl Pts',(-2.66598662949465,5.56282488977604,37.0003492601412));
#57483=CARTESIAN_POINT('Ctrl Pts',(-5.00545626120256,3.605261860135,37.1395227175633));
#57484=CARTESIAN_POINT('Ctrl Pts',(-6.12091641597078,0.766085955787854,
37.2786961749851));
#57485=CARTESIAN_POINT('Ctrl Pts',(-5.73959799357409,-2.26042481297572,
37.4178696324071));
#57486=CARTESIAN_POINT('Ctrl Pts',(-3.95474671196289,-4.73418249618397,
37.5570430898291));
#57487=CARTESIAN_POINT('Ctrl Pts',(-1.20282126133765,-6.05026664505211,
37.6962165472511));
#57488=CARTESIAN_POINT('Ctrl Pts',(1.84323614172387,-5.88684856173478,37.8353900046729));
#57489=CARTESIAN_POINT('Ctrl Pts',(4.43855771013327,-4.28388969474851,37.974563462095));
#57490=CARTESIAN_POINT('Ctrl Pts',(5.94849636484969,-1.63336966432161,38.1137369195168));
#57491=CARTESIAN_POINT('Ctrl Pts',(6.00381918752842,1.41656649205803,38.2529103769389));
#57492=CARTESIAN_POINT('Ctrl Pts',(4.59099780918249,4.12010249618109,38.3920838343607));
#57493=CARTESIAN_POINT('Ctrl Pts',(2.05551657051471,5.8161290469947,38.5312572917828));
#57494=CARTESIAN_POINT('Ctrl Pts',(-0.982610507218312,6.08990821392738,
38.6704307492047));
#57495=CARTESIAN_POINT('Ctrl Pts',(-3.78045487939699,4.87449139580732,38.8096042066266));
#57496=CARTESIAN_POINT('Ctrl Pts',(-5.65384554385049,2.46709060012758,38.9487776640486));
#57497=CARTESIAN_POINT('Ctrl Pts',(-6.14467282832481,-0.54360030886931,
39.0879511214705));
#57498=CARTESIAN_POINT('Ctrl Pts',(-5.1329122602471,-3.42136189134693,39.2271245788925));
#57499=CARTESIAN_POINT('Ctrl Pts',(-2.86597475664404,-5.46248058644011,
39.3662980363144));
#57500=CARTESIAN_POINT('Ctrl Pts',(0.101794015827083,-6.16783134021171,
39.5054714937364));
#57501=CARTESIAN_POINT('Ctrl Pts',(3.04467058395836,-5.36493117366241,39.6446449511584));
#57502=CARTESIAN_POINT('Ctrl Pts',(5.24301849087439,-3.25011731592957,39.7838184085803));
#57503=CARTESIAN_POINT('Ctrl Pts',(6.15926463009694,-0.340535870934299,
39.9229918660023));
#57504=CARTESIAN_POINT('Ctrl Pts',(5.56935470985029,2.65231852891472,40.0621653234242));
#57505=CARTESIAN_POINT('Ctrl Pts',(3.61754237960085,4.99658809536546,40.2013387808462));
#57506=CARTESIAN_POINT('Ctrl Pts',(0.781114157253151,6.11901676221718,40.3405122382681));
#57507=CARTESIAN_POINT('Ctrl Pts',(-2.24632385144714,5.74513138382193,40.4796856956901));
#57508=CARTESIAN_POINT('Ctrl Pts',(-4.72445695386775,3.96636003837356,40.618859153112));
#57509=CARTESIAN_POINT('Ctrl Pts',(-6.04729475788563,1.21767465860342,40.758032610534));
#57510=CARTESIAN_POINT('Ctrl Pts',(-5.89135706028292,-1.8287748497862,40.8972060679559));
#57511=CARTESIAN_POINT('Ctrl Pts',(-4.29477609311154,-4.42802481621249,
41.0363795253779));
#57512=CARTESIAN_POINT('Ctrl Pts',(-1.64797185657537,-5.9444675306449,41.1755529827998));
#57513=CARTESIAN_POINT('Ctrl Pts',(1.4018192536676,-6.00727960419713,41.3147264402217));
#57514=CARTESIAN_POINT('Ctrl Pts',(4.10881642827179,-4.60110128357549,41.4538998976438));
#57515=CARTESIAN_POINT('Ctrl Pts',(5.81106398870155,-2.06979244905675,41.5930733550657));
#57516=CARTESIAN_POINT('Ctrl Pts',(6.09230274951283,0.967653177142854,41.7322468124877));
#57517=CARTESIAN_POINT('Ctrl Pts',(4.88375997740181,3.76847368918562,41.8714202699095));
#57518=CARTESIAN_POINT('Ctrl Pts',(2.48096673470485,5.64777031440231,42.0105937273315));
#57519=CARTESIAN_POINT('Ctrl Pts',(-0.528509822516023,6.14598916615219,
42.1497671847535));
#57520=CARTESIAN_POINT('Ctrl Pts',(-3.40874720599174,5.14129827461892,42.2889406421755));
#57521=CARTESIAN_POINT('Ctrl Pts',(-5.45542643474629,2.87937977315038,42.4281140995974));
#57522=CARTESIAN_POINT('Ctrl Pts',(-6.16806270948796,-0.0866479935138681,
42.5672875570194));
#57523=CARTESIAN_POINT('Ctrl Pts',(-5.37239148601215,-3.03148728910088,
42.7064610144413));
#57524=CARTESIAN_POINT('Ctrl Pts',(-3.26298226352938,-5.2350217010867,42.8456344718633));
#57525=CARTESIAN_POINT('Ctrl Pts',(-0.355659523231457,-6.15840984073736,
42.9848079292852));
#57526=CARTESIAN_POINT('Ctrl Pts',(2.63863443492995,-5.5758509468742,43.1239813867072));
#57527=CARTESIAN_POINT('Ctrl Pts',(4.98768980024473,-3.62980108538893,43.2631548441291));
#57528=CARTESIAN_POINT('Ctrl Pts',(6.11708021096689,-0.796137648621998,
43.402328301551));
#57529=CARTESIAN_POINT('Ctrl Pts',(5.7506301310911,2.23220934465008,43.541501758973));
#57530=CARTESIAN_POINT('Ctrl Pts',(3.97794944774594,4.71470292321093,43.680675216395));
#57531=CARTESIAN_POINT('Ctrl Pts',(1.23252071332536,6.04428640570416,43.8198486738169));
#57532=CARTESIAN_POINT('Ctrl Pts',(-1.81430253038862,5.89583003411575,43.9590221312389));
#57533=CARTESIAN_POINT('Ctrl Pts',(-4.41746522142847,4.30563659409686,44.0981955886608));
#57534=CARTESIAN_POINT('Ctrl Pts',(-5.94040285147039,1.66256411160545,44.2373690460828));
#57535=CARTESIAN_POINT('Ctrl Pts',(-6.01070379714092,-1.38706356234736,
44.3765425035047));
#57536=CARTESIAN_POINT('Ctrl Pts',(-4.61117701345869,-4.09750558431666,
44.5157159609267));
#57537=CARTESIAN_POINT('Ctrl Pts',(-2.08405584680928,-5.80596388985809,
44.6548894183486));
#57538=CARTESIAN_POINT('Ctrl Pts',(0.952690012146062,-6.0946605486863,44.7940628757706));
#57539=CARTESIAN_POINT('Ctrl Pts',(3.75646977518502,-4.89299911006301,44.9332363331926));
#57540=CARTESIAN_POINT('Ctrl Pts',(5.64166102905991,-2.49482790912372,45.0724097906145));
#57541=CARTESIAN_POINT('Ctrl Pts',(6.14726844384006,0.513416149263214,45.2115832480365));
#57542=CARTESIAN_POINT('Ctrl Pts',(5.14965328710884,3.39611196598774,45.3507567054584));
#57543=CARTESIAN_POINT('Ctrl Pts',(2.89276742707903,5.44833938698633,45.4899301628804));
#57544=CARTESIAN_POINT('Ctrl Pts',(-0.0715014487153603,6.16825688552184,
45.6291036203023));
#57545=CARTESIAN_POINT('Ctrl Pts',(-3.01828571446114,5.37981940299448,45.7682770777242));
#57546=CARTESIAN_POINT('Ctrl Pts',(-5.22699334426712,3.27582753543943,45.9074505351462));
#57547=CARTESIAN_POINT('Ctrl Pts',(-6.15751791634193,0.370781030912171,
46.0466239925682));
#57548=CARTESIAN_POINT('Ctrl Pts',(-5.58231356167591,-2.62493443005441,
46.1857974499901));
#57549=CARTESIAN_POINT('Ctrl Pts',(-3.64203790358019,-4.97876142949642,
46.3249709074121));
#57550=CARTESIAN_POINT('Ctrl Pts',(-0.811156339303846,-6.11510677389718,
46.464144364834));
#57551=CARTESIAN_POINT('Ctrl Pts',(2.21808137769395,-5.75609420222458,46.603317822256));
#57552=CARTESIAN_POINT('Ctrl Pts',(4.70492046302962,-3.98951487019676,46.7424912796779));
#57553=CARTESIAN_POINT('Ctrl Pts',(6.0412416066478,-1.24735933598286,46.8816647370999));
#57554=CARTESIAN_POINT('Ctrl Pts',(5.90026745626159,1.79981927079816,47.0208381945218));
#57555=CARTESIAN_POINT('Ctrl Pts',(4.31647113221644,4.4068789894548,47.1600116519438));
#57556=CARTESIAN_POINT('Ctrl Pts',(1.67714634142165,5.93630235183586,47.2991851093657));
#57557=CARTESIAN_POINT('Ctrl Pts',(-1.37229950707301,6.01409174571216,47.4383585667878));
#57558=CARTESIAN_POINT('Ctrl Pts',(-4.08617003251941,4.62122493807609,47.5775320242095));
#57559=CARTESIAN_POINT('Ctrl Pts',(-5.80082878121777,2.09830667776461,47.7167054816318));
#57560=CARTESIAN_POINT('Ctrl Pts',(-6.09698159723034,-0.937721102455593,
47.8558789390534));
#57561=CARTESIAN_POINT('Ctrl Pts',(-4.90220873807901,-3.74444320977871,
47.9950523964757));
#57562=CARTESIAN_POINT('Ctrl Pts',(-2.50867403980139,-5.63551772466226,
48.1342258538973));
#57563=CARTESIAN_POINT('Ctrl Pts',(0.498319380125655,-6.14851065367438,
48.2733993113196));
#57564=CARTESIAN_POINT('Ctrl Pts',(3.38345624752536,-5.15797724733616,48.4125727687412));
#57565=CARTESIAN_POINT('Ctrl Pts',(5.44121948589513,-2.90613763770253,48.5517462261634));
#57566=CARTESIAN_POINT('Ctrl Pts',(6.16841386714245,0.056354472765162,48.6909196835852));
#57567=CARTESIAN_POINT('Ctrl Pts',(5.38721487981911,3.00506593964454,48.8300931410073));
#57568=CARTESIAN_POINT('Ctrl Pts',(3.28865305420277,5.21893346882663,48.9692665984291));
#57569=CARTESIAN_POINT('Ctrl Pts',(0.385900302793842,6.1565888622889,49.1084400558511));
#57570=CARTESIAN_POINT('Ctrl Pts',(-2.61121859689906,5.58874251528593,49.247613513273));
#57571=CARTESIAN_POINT('Ctrl Pts',(-4.96980303695856,3.65425276038667,49.386786970695));
#57572=CARTESIAN_POINT('Ctrl Pts',(-6.11309646290787,0.826170138736081,
49.5259604281169));
#57573=CARTESIAN_POINT('Ctrl Pts',(-5.76152356427402,-2.20394003577031,
49.665133885539));
#57574=CARTESIAN_POINT('Ctrl Pts',(-4.00105623598661,-4.69510963231198,
49.8043073429608));
#57575=CARTESIAN_POINT('Ctrl Pts',(-1.2621904370991,-6.03816037907669,49.9434808003828));
#57576=CARTESIAN_POINT('Ctrl Pts',(1.78532515834877,-5.90466929996279,50.0826542578047));
#57577=CARTESIAN_POINT('Ctrl Pts',(4.39626618412638,-4.3272796421381,50.2218277152268));
#57578=CARTESIAN_POINT('Ctrl Pts',(5.93216605646731,-1.6917184580932,50.3610011726486));
#57579=CARTESIAN_POINT('Ctrl Pts',(6.01744342948154,1.35752717687174,50.5001746300706));
#57580=CARTESIAN_POINT('Ctrl Pts',(4.6312449968388,4.07480984123329,50.6393480874926));
#57581=CARTESIAN_POINT('Ctrl Pts',(2.11254485599046,5.7956586937452,50.7785215449145));
#57582=CARTESIAN_POINT('Ctrl Pts',(-0.922746538333597,6.09926588114908,
50.9176950023365));
#57583=CARTESIAN_POINT('Ctrl Pts',(-3.73239406548654,4.91138880591599,51.0568684597585));
#57584=CARTESIAN_POINT('Ctrl Pts',(-5.62934043825332,2.52250504324608,51.1960419171804));
#57585=CARTESIAN_POINT('Ctrl Pts',(-6.14971578816463,-0.483219606136435,
51.3352153746023));
#57586=CARTESIAN_POINT('Ctrl Pts',(-5.16627010510767,-3.37078012691822,
51.4743888320243));
#57587=CARTESIAN_POINT('Ctrl Pts',(-2.91949032439888,-5.43406677440547,
51.6135622894462));
#57588=CARTESIAN_POINT('Ctrl Pts',(0.0412071569990902,-6.16853365340321,
51.7527357468682));
#57589=CARTESIAN_POINT('Ctrl Pts',(2.99182804436595,-5.39457787189151,51.8919092042902));
#57590=CARTESIAN_POINT('Ctrl Pts',(5.21084212336603,-3.3014587424819,52.0310826617121));
#57591=CARTESIAN_POINT('Ctrl Pts',(6.15562268418046,-0.401017247707679,
52.170256119134));
#57592=CARTESIAN_POINT('Ctrl Pts',(5.59513776893782,2.59748701816997,52.3094295765561));
#57593=CARTESIAN_POINT('Ctrl Pts',(3.66644558215312,4.96081467664999,52.4486030339779));
#57594=CARTESIAN_POINT('Ctrl Pts',(0.84117895638593,6.11104929012109,52.5877764913999));
#57595=CARTESIAN_POINT('Ctrl Pts',(-2.18978540415105,5.76691818450055,52.7269499488218));
#57596=CARTESIAN_POINT('Ctrl Pts',(-4.68527049021703,4.01257347552135,52.8661234062438));
#57597=CARTESIAN_POINT('Ctrl Pts',(-6.03504274157056,1.27701392724298,53.0052968636658));
#57598=CARTESIAN_POINT('Ctrl Pts',(-5.90903553867634,-1.77082028043954,
53.1444703210877));
#57599=CARTESIAN_POINT('Ctrl Pts',(-4.33806205868681,-4.38562686943817,
53.2836437785097));
#57600=CARTESIAN_POINT('Ctrl Pts',(-1.70628037375065,-5.92799399030643,
53.4228172359316));
#57601=CARTESIAN_POINT('Ctrl Pts',(1.34274666082029,-6.02075882823852,53.5619906933536));
#57602=CARTESIAN_POINT('Ctrl Pts',(4.06342507895993,-4.64123712932612,53.7011641507755));
#57603=CARTESIAN_POINT('Ctrl Pts',(5.79045365861584,-2.12677029563103,53.8403376081975));
#57604=CARTESIAN_POINT('Ctrl Pts',(6.10151338666836,0.907766410076269,53.9795110656194));
#57605=CARTESIAN_POINT('Ctrl Pts',(4.92053925821843,3.7203224149645,54.1186845230414));
#57606=CARTESIAN_POINT('Ctrl Pts',(2.53632083605719,5.62312920708197,54.2578579804633));
#57607=CARTESIAN_POINT('Ctrl Pts',(-0.468116918346931,6.15088384004395,
54.3970314378853));
#57608=CARTESIAN_POINT('Ctrl Pts',(-3.35808368060321,5.17453181041749,54.5362048953072));
#57609=CARTESIAN_POINT('Ctrl Pts',(-5.42688129564815,2.93282540665145,54.6753783527292));
#57610=CARTESIAN_POINT('Ctrl Pts',(-6.16861624358182,-0.026059592755391,
54.8145518101512));
#57611=CARTESIAN_POINT('Ctrl Pts',(-5.40190833481288,-2.97857210844981,
54.9537252675732));
#57612=CARTESIAN_POINT('Ctrl Pts',(-3.3142445230586,-5.20271935667608,55.092898724995));
#57613=CARTESIAN_POINT('Ctrl Pts',(-0.416131774498588,-6.15461938784266,
55.232072182417));
#57614=CARTESIAN_POINT('Ctrl Pts',(2.58373977666849,-5.60149928406824,55.3712456398389));
#57615=CARTESIAN_POINT('Ctrl Pts',(4.95179640277048,-3.67861629535691,55.5104190972609));
#57616=CARTESIAN_POINT('Ctrl Pts',(6.10896526788126,-0.856182701750285,
55.6495925546829));
#57617=CARTESIAN_POINT('Ctrl Pts',(5.77227803037462,2.17561756818853,55.7887660121049));
#57618=CARTESIAN_POINT('Ctrl Pts',(4.0240665193521,4.67540309607475,55.9279394695267));
#57619=CARTESIAN_POINT('Ctrl Pts',(1.29182971702892,6.03188871292874,56.0671129269488));
#57620=CARTESIAN_POINT('Ctrl Pts',(-1.75630472453483,5.91336614607388,56.2062863843706));
#57621=CARTESIAN_POINT('Ctrl Pts',(-4.37496110954512,4.34881831684468,56.3454598417927));
#57622=CARTESIAN_POINT('Ctrl Pts',(-5.92378617851085,1.72083200058572,56.4846332992145));
#57623=CARTESIAN_POINT('Ctrl Pts',(-6.02403792199122,-1.32795804804506,
56.6238067566366));
#57624=CARTESIAN_POINT('Ctrl Pts',(-4.65120127528559,-4.0520158143494,56.7629802140584));
#57625=CARTESIAN_POINT('Ctrl Pts',(-2.14098291090698,-5.78521370721604,
56.9021536714805));
#57626=CARTESIAN_POINT('Ctrl Pts',(0.892780808013698,-6.10372410023572,
57.0413271289024));
#57627=CARTESIAN_POINT('Ctrl Pts',(3.7082283310046,-4.92966003980913,57.1805005863244));
#57628=CARTESIAN_POINT('Ctrl Pts',(5.6168840686018,-2.55012133492571,57.3196740437463));
#57629=CARTESIAN_POINT('Ctrl Pts',(6.15201480226891,0.453011407825745,57.4588475011683));
#57630=CARTESIAN_POINT('Ctrl Pts',(5.18276231344806,3.34536698513908,57.5980209585902));
#57631=CARTESIAN_POINT('Ctrl Pts',(2.9461428040507,5.4196630929511,57.7371944160122));
#57632=CARTESIAN_POINT('Ctrl Pts',(-0.0109118713727406,6.16866163718024,
57.8763678734341));
#57633=CARTESIAN_POINT('Ctrl Pts',(-2.96529821182842,5.4092062243811,58.0155413308561));
#57634=CARTESIAN_POINT('Ctrl Pts',(-5.19456521773649,3.32701031883556,58.154714788278));
#57635=CARTESIAN_POINT('Ctrl Pts',(-6.1535789793253,0.431243792027107,58.2938882457));
#57636=CARTESIAN_POINT('Ctrl Pts',(-5.60782702231775,-2.56997695528946,
58.4330617031219));
#57637=CARTESIAN_POINT('Ctrl Pts',(-3.69076482660954,-4.94274826969955,
58.5722351605439));
#57638=CARTESIAN_POINT('Ctrl Pts',(-0.871181284357699,-6.10684440875489,
58.7114086179658));
#57639=CARTESIAN_POINT('Ctrl Pts',(2.16143661331375,-5.77760306957677,58.8505820753878));
#57640=CARTESIAN_POINT('Ctrl Pts',(4.6655075093848,-4.03553529817666,58.9897555328097));
#57641=CARTESIAN_POINT('Ctrl Pts',(6.02869831216978,-1.30663771711886,59.1289289902318));
#57642=CARTESIAN_POINT('Ctrl Pts',(5.91766109604211,1.74177857816241,59.2681024476536));
#57643=CARTESIAN_POINT('Ctrl Pts',(4.35954835175235,4.36426896876084,59.4072759050756));
#57644=CARTESIAN_POINT('Ctrl Pts',(1.73537325085302,5.91954264645359,59.5464493624975));
#57645=CARTESIAN_POINT('Ctrl Pts',(-1.31316142771993,6.0272806909664,59.6856228199195));
#57646=CARTESIAN_POINT('Ctrl Pts',(-4.04058211619944,4.66113737463529,59.8247962773414));
#57647=CARTESIAN_POINT('Ctrl Pts',(-5.77993887114087,2.15518261611504,59.9639697347634));
#57648=CARTESIAN_POINT('Ctrl Pts',(-6.10589800852354,-0.877789822503519,
60.1031431921854));
#57649=CARTESIAN_POINT('Ctrl Pts',(-4.93875109568499,-3.69611188654187,
60.2423166496073));
#57650=CARTESIAN_POINT('Ctrl Pts',(-2.56390645664619,-5.61060506045379,
60.3814901070292));
#57651=CARTESIAN_POINT('Ctrl Pts',(0.437903165679336,-6.15310866805281,
60.5206635644512));
#57652=CARTESIAN_POINT('Ctrl Pts',(3.3326301171667,-5.19096156450552,60.6598370218731));
#57653=CARTESIAN_POINT('Ctrl Pts',(5.41241220991924,-2.95944243641773,60.7990104792952));
#57654=CARTESIAN_POINT('Ctrl Pts',(6.16866983377028,-0.00423591556452433,
60.938183936717));
#57655=CARTESIAN_POINT('Ctrl Pts',(5.41647149689117,2.95200643406812,61.077357394139));
#57656=CARTESIAN_POINT('Ctrl Pts',(3.3397560522476,5.18637975664333,61.2165308515609));
#57657=CARTESIAN_POINT('Ctrl Pts',(0.446353210313549,6.15250146309482,61.3557043089829));
#57658=CARTESIAN_POINT('Ctrl Pts',(-2.55619863925694,5.61412094905446,61.4948777664048));
#57659=CARTESIAN_POINT('Ctrl Pts',(-4.93367032764008,3.70289109578226,61.6340512238268));
#57660=CARTESIAN_POINT('Ctrl Pts',(-6.10468673402829,0.886174627170678,
61.7732246812487));
#57661=CARTESIAN_POINT('Ctrl Pts',(-5.78289325342531,-2.14724265117775,
61.9123981386708));
#57662=CARTESIAN_POINT('Ctrl Pts',(-4.04697977515619,-4.6555837388399,62.0515715960926));
#57663=CARTESIAN_POINT('Ctrl Pts',(-1.32143777519505,-6.02547165794721,
62.1907450535147));
#57664=CARTESIAN_POINT('Ctrl Pts',(1.72724180600375,-5.92192016880478,62.3299185109365));
#57665=CARTESIAN_POINT('Ctrl Pts',(4.35355075125749,-4.37025247680389,62.4690919683585));
#57666=CARTESIAN_POINT('Ctrl Pts',(5.91526295226815,-1.74990329951406,62.6082654257805));
#57667=CARTESIAN_POINT('Ctrl Pts',(6.03048802723082,1.29835545109493,62.7474388832024));
#57668=CARTESIAN_POINT('Ctrl Pts',(4.67104358963708,4.0291268577618,62.8866123406244));
#57669=CARTESIAN_POINT('Ctrl Pts',(2.16937279271135,5.77462371327947,63.0257857980464));
#57670=CARTESIAN_POINT('Ctrl Pts',(-0.862800305444146,6.10804576400077,
63.1649592554682));
#57671=CARTESIAN_POINT('Ctrl Pts',(-3.68395996768377,4.94779156902649,63.3041327128903));
#57672=CARTESIAN_POINT('Ctrl Pts',(-5.60431794598028,2.5777167089644,63.4433061703121));
#57673=CARTESIAN_POINT('Ctrl Pts',(-6.15411517187233,-0.422871685852421,
63.5824796277342));
#57674=CARTESIAN_POINT('Ctrl Pts',(-5.19922846621166,-3.3197157566242,63.7216530851561));
#57675=CARTESIAN_POINT('Ctrl Pts',(-2.97252143221046,-5.40546228751415,
63.8608265425781));
#57676=CARTESIAN_POINT('Ctrl Pts',(-1.00409531133336,-5.91362404918468,
63.953608847526));
#57677=CARTESIAN_POINT('Ctrl Pts',(-0.0185920708322156,-5.91672078920428,
64.));
#57678=CARTESIAN_POINT('Ctrl Pts',(3.24375760296866,-4.54512507566742,-0.384322829190561));
#57679=CARTESIAN_POINT('Ctrl Pts',(4.00080456363074,-4.00483701019733,-0.337931676716577));
#57680=CARTESIAN_POINT('Ctrl Pts',(5.23892931934964,-2.53920478472433,-0.245149371768609));
#57681=CARTESIAN_POINT('Ctrl Pts',(5.81483236077834,0.281981155041063,-0.105975914346657));
#57682=CARTESIAN_POINT('Ctrl Pts',(4.96885277875867,3.03344919454013,0.0331975430752952));
#57683=CARTESIAN_POINT('Ctrl Pts',(2.90779432331117,5.0435085486934,0.172371000497248));
#57684=CARTESIAN_POINT('Ctrl Pts',(0.135688220029282,5.82006202178721,0.311544457919199));
#57685=CARTESIAN_POINT('Ctrl Pts',(-2.66960348256184,5.17350430475029,0.450717915341153));
#57686=CARTESIAN_POINT('Ctrl Pts',(-4.82208097659197,3.26179326528778,0.589891372763104));
#57687=CARTESIAN_POINT('Ctrl Pts',(-5.79539200928568,0.552485204520095,
0.729064830185058));
#57688=CARTESIAN_POINT('Ctrl Pts',(-5.35152590761217,-2.2919380522483,0.868238287607008));
#57689=CARTESIAN_POINT('Ctrl Pts',(-3.59902452230347,-4.5758953628753,1.00741174502896));
#57690=CARTESIAN_POINT('Ctrl Pts',(-0.966435330409787,-5.74088936163419,
1.14658520245091));
#57691=CARTESIAN_POINT('Ctrl Pts',(1.90248107735391,-5.50203293656693,1.28575865987286));
#57692=CARTESIAN_POINT('Ctrl Pts',(4.30617423462377,-3.91773754708874,1.42493211729482));
#57693=CARTESIAN_POINT('Ctrl Pts',(5.65685685325898,-1.37541755843866,1.56410557471677));
#57694=CARTESIAN_POINT('Ctrl Pts',(5.62423973364523,1.50323998611993,1.70327903213872));
#57695=CARTESIAN_POINT('Ctrl Pts',(4.2162988858458,4.01430279461926,1.84245248956067));
#57696=CARTESIAN_POINT('Ctrl Pts',(1.77732519943232,5.54372782159637,1.98162594698263));
#57697=CARTESIAN_POINT('Ctrl Pts',(-1.09626678800386,5.71751714322285,2.12079940440458));
#57698=CARTESIAN_POINT('Ctrl Pts',(-3.70178312518057,4.49317313079981,2.25997286182653));
#57699=CARTESIAN_POINT('Ctrl Pts',(-5.40208375610618,2.17009082878763,2.39914631924848));
#57700=CARTESIAN_POINT('Ctrl Pts',(-5.78138558716672,-0.683654738165986,
2.53831977667044));
#57701=CARTESIAN_POINT('Ctrl Pts',(-4.74693602800832,-3.37022276005692,
2.67749323409239));
#57702=CARTESIAN_POINT('Ctrl Pts',(-2.55169424895947,-5.23265320553137,
2.81666669151434));
#57703=CARTESIAN_POINT('Ctrl Pts',(0.267526200532523,-5.815516558252,2.95584014893629));
#57704=CARTESIAN_POINT('Ctrl Pts',(3.02132711829442,-4.97628230235617,3.09501360635824));
#57705=CARTESIAN_POINT('Ctrl Pts',(5.03630767028235,-2.92017262473365,3.2341870637802));
#57706=CARTESIAN_POINT('Ctrl Pts',(5.81973449459707,-0.149978400157519,
3.37336052120215));
#57707=CARTESIAN_POINT('Ctrl Pts',(5.18003227673358,2.65689079943647,3.5125339786241));
#57708=CARTESIAN_POINT('Ctrl Pts',(3.27363062794811,4.81405708522912,3.65170743604605));
#57709=CARTESIAN_POINT('Ctrl Pts',(0.566711563064284,5.79401770038826,3.79088089346801));
#57710=CARTESIAN_POINT('Ctrl Pts',(-2.27878833994558,5.35713793081986,3.93005435088995));
#57711=CARTESIAN_POINT('Ctrl Pts',(-4.56704463148848,3.61025019106752,4.06922780831191));
#57712=CARTESIAN_POINT('Ctrl Pts',(-5.73849845411803,0.980529754873716,
4.20840126573386));
#57713=CARTESIAN_POINT('Ctrl Pts',(-5.50668829346455,-1.88896457000346,
4.34757472315581));
#57714=CARTESIAN_POINT('Ctrl Pts',(-3.92829985781997,-4.29654085691737,
4.48674818057777));
#57715=CARTESIAN_POINT('Ctrl Pts',(-1.38930443585496,-5.65346232786791,
4.62592163799971));
#57716=CARTESIAN_POINT('Ctrl Pts',(1.48942461019975,-5.62791412857727,4.76509509542168));
#57717=CARTESIAN_POINT('Ctrl Pts',(4.00393714072872,-4.22614368913331,4.90426855284362));
#57718=CARTESIAN_POINT('Ctrl Pts',(5.53934671848404,-1.79093300838651,5.04344201026558));
#57719=CARTESIAN_POINT('Ctrl Pts',(5.72019189178477,1.08222355789733,5.18261546768752));
#57720=CARTESIAN_POINT('Ctrl Pts',(4.50224967786418,3.69073853669968,5.32178892510949));
#57721=CARTESIAN_POINT('Ctrl Pts',(2.18334963199351,5.39673859776273,5.46096238253143));
#57722=CARTESIAN_POINT('Ctrl Pts',(-0.669455916507752,5.78304693772763,
5.60013583995339));
#57723=CARTESIAN_POINT('Ctrl Pts',(-3.35855603169015,4.75519762892206,5.73930929737534));
#57724=CARTESIAN_POINT('Ctrl Pts',(-5.22637149326653,2.56453584932617,5.87848275479729));
#57725=CARTESIAN_POINT('Ctrl Pts',(-5.81615596147474,-0.253244822079318,
6.01765621221924));
#57726=CARTESIAN_POINT('Ctrl Pts',(-4.98368646426841,-3.0090982592757,6.1568296696412));
#57727=CARTESIAN_POINT('Ctrl Pts',(-2.93253096841646,-5.02912171530841,
6.29600312706314));
#57728=CARTESIAN_POINT('Ctrl Pts',(-0.164268877390996,-5.81934866149373,
6.4351765844851));
#57729=CARTESIAN_POINT('Ctrl Pts',(2.6441627111189,-5.1865409152186,6.57435004190705));
#57730=CARTESIAN_POINT('Ctrl Pts',(4.80600384951016,-3.28544214780928,6.71352349932901));
#57731=CARTESIAN_POINT('Ctrl Pts',(5.79260861562399,-0.580937633749912,
6.85269695675095));
#57732=CARTESIAN_POINT('Ctrl Pts',(5.36271756762338,2.26562649128486,6.99187041417291));
#57733=CARTESIAN_POINT('Ctrl Pts',(3.62145413269375,4.55816553811986,7.13104387159486));
#57734=CARTESIAN_POINT('Ctrl Pts',(0.994618244943479,5.73607336554666,7.2702173290168));
#57735=CARTESIAN_POINT('Ctrl Pts',(-1.87543666105779,5.51131022883567,7.40939078643877));
#57736=CARTESIAN_POINT('Ctrl Pts',(-4.28688157693133,3.93883859195511,7.54856424386071));
#57737=CARTESIAN_POINT('Ctrl Pts',(-5.65003370931712,1.40318287891794,7.68773770128267));
#57738=CARTESIAN_POINT('Ctrl Pts',(-5.63155458885656,-1.47560022392137,
7.82691115870462));
#57739=CARTESIAN_POINT('Ctrl Pts',(-4.23596300812098,-3.99354735816903,
7.96608461612657));
#57740=CARTESIAN_POINT('Ctrl Pts',(-1.80453001846248,-5.53493220559892,
8.10525807354854));
#57741=CARTESIAN_POINT('Ctrl Pts',(1.06817380221706,-5.7228321516855,8.24443153097047));
#57742=CARTESIAN_POINT('Ctrl Pts',(3.67967169306626,-4.51129907447457,8.38360498839244));
#57743=CARTESIAN_POINT('Ctrl Pts',(5.3913608972928,-2.19659527069743,8.52277844581438));
#57744=CARTESIAN_POINT('Ctrl Pts',(5.78467341665285,0.655253058579685,8.66195190323633));
#57745=CARTESIAN_POINT('Ctrl Pts',(4.76343055614367,3.34686905105429,8.80112536065828));
#57746=CARTESIAN_POINT('Ctrl Pts',(2.57736198560756,5.22005826626995,8.94029881808025));
#57747=CARTESIAN_POINT('Ctrl Pts',(-0.238961916563357,5.81676029337126,
9.07947227550219));
#57748=CARTESIAN_POINT('Ctrl Pts',(-2.9968512554821,4.99106057472994,9.21864573292415));
#57749=CARTESIAN_POINT('Ctrl Pts',(-5.02190543487286,2.94487162900228,9.35781919034609));
#57750=CARTESIAN_POINT('Ctrl Pts',(-5.81892773788428,0.178558364097456,
9.49699264776805));
#57751=CARTESIAN_POINT('Ctrl Pts',(-5.19301827900942,-2.63141867858048,
9.63616610518999));
#57752=CARTESIAN_POINT('Ctrl Pts',(-3.29723385654803,-4.79792163372242,
9.77533956261196));
#57753=CARTESIAN_POINT('Ctrl Pts',(-0.595160201398069,-5.79116460159612,
9.9145130200339));
#57754=CARTESIAN_POINT('Ctrl Pts',(2.25245098096098,-5.36826486739209,10.0536864774559));
#57755=CARTESIAN_POINT('Ctrl Pts',(4.54925895914298,-3.63263623705505,10.1928599348778));
#57756=CARTESIAN_POINT('Ctrl Pts',(5.73361368861633,-1.00870073749333,10.3320333922998));
#57757=CARTESIAN_POINT('Ctrl Pts',(5.51589893116313,1.86189744328243,10.4712068497217));
#57758=CARTESIAN_POINT('Ctrl Pts',(3.94935357500579,4.27719644717158,10.6103803071437));
#57759=CARTESIAN_POINT('Ctrl Pts',(1.41705286082813,5.64657102122404,10.7495537645656));
#57760=CARTESIAN_POINT('Ctrl Pts',(-1.46176693981568,5.63516109102216,10.8887272219876));
#57761=CARTESIAN_POINT('Ctrl Pts',(-3.98313349463256,4.24575678437242,11.0279006794095));
#57762=CARTESIAN_POINT('Ctrl Pts',(-5.53048431723029,1.81811614727388,11.1670741368315));
#57763=CARTESIAN_POINT('Ctrl Pts',(-5.72543790307144,-1.05411760547914,
11.3062475942534));
#57764=CARTESIAN_POINT('Ctrl Pts',(-4.52032126808012,-3.66858266111734,
11.4454210516754));
#57765=CARTESIAN_POINT('Ctrl Pts',(-2.20982766399449,-5.38595068707029,
11.5845945090973));
#57766=CARTESIAN_POINT('Ctrl Pts',(0.641046249494328,-5.7862650141622,11.7237679665193));
#57767=CARTESIAN_POINT('Ctrl Pts',(3.33516188889343,-4.77163476001475,11.8629414239412));
#57768=CARTESIAN_POINT('Ctrl Pts',(5.21371356247076,-2.59017258046961,12.0021148813632));
#57769=CARTESIAN_POINT('Ctrl Pts',(5.81732955036896,0.224677570113848,12.1412883387851));
#57770=CARTESIAN_POINT('Ctrl Pts',(4.99840458923842,2.98458618076083,12.2804617962071));
#57771=CARTESIAN_POINT('Ctrl Pts',(2.9571945320961,5.01465887249064,12.419635253629));
#57772=CARTESIAN_POINT('Ctrl Pts',(0.192846774102069,5.81847172630637,12.558808711051));
#57773=CARTESIAN_POINT('Ctrl Pts',(-2.6186587786624,5.19946432904799,12.697982168473));
#57774=CARTESIAN_POINT('Ctrl Pts',(-4.78981048660394,3.30900568306057,12.8371556258949));
#57775=CARTESIAN_POINT('Ctrl Pts',(-5.78968566701073,0.60937918024717,12.9763290833169));
#57776=CARTESIAN_POINT('Ctrl Pts',(-5.37377979667661,-2.23926188842183,
13.1155025407388));
#57777=CARTESIAN_POINT('Ctrl Pts',(-3.64379643672339,-4.54032494826418,
13.2546759981608));
#57778=CARTESIAN_POINT('Ctrl Pts',(-1.02277714760654,-5.73111943815883,
13.3938494555827));
#57779=CARTESIAN_POINT('Ctrl Pts',(1.84834699831852,-5.52045437277723,13.5330229130047));
#57780=CARTESIAN_POINT('Ctrl Pts',(4.26748552603914,-3.95984474356694,13.6721963704266));
#57781=CARTESIAN_POINT('Ctrl Pts',(5.64307428446858,-1.43091429794995,13.8113698278486));
#57782=CARTESIAN_POINT('Ctrl Pts',(5.63873361332696,1.447924841297,13.9505432852705));
#57783=CARTESIAN_POINT('Ctrl Pts',(4.2555249588314,3.97269561291463,14.0897167426925));
#57784=CARTESIAN_POINT('Ctrl Pts',(1.83169131289668,5.52600308019885,14.2288902001144));
#57785=CARTESIAN_POINT('Ctrl Pts',(-1.04005505244218,5.72800913022995,14.3680636575364));
#57786=CARTESIAN_POINT('Ctrl Pts',(-3.65747150771956,4.52931620427717,14.5072371149583));
#57787=CARTESIAN_POINT('Ctrl Pts',(-5.38050799971861,2.22304673209365,14.6464105723803));
#57788=CARTESIAN_POINT('Ctrl Pts',(-5.78782172065838,-0.626835574918385,
14.7855840298022));
#57789=CARTESIAN_POINT('Ctrl Pts',(-4.7798101910642,-3.32343461580141,14.9247574872242));
#57790=CARTESIAN_POINT('Ctrl Pts',(-2.60296755666481,-5.20733742012736,
15.0639309446461));
#57791=CARTESIAN_POINT('Ctrl Pts',(0.21039186886499,-5.81786372903523,15.2031044020681));
#57792=CARTESIAN_POINT('Ctrl Pts',(2.97230310906994,-5.00571846350965,15.34227785949));
#57793=CARTESIAN_POINT('Ctrl Pts',(5.0073820718583,-2.96949960339115,15.481451316912));
#57794=CARTESIAN_POINT('Ctrl Pts',(5.81798062950974,-0.207134021246128,
15.620624774334));
#57795=CARTESIAN_POINT('Ctrl Pts',(5.20587902646482,2.60588308830651,15.7597982317559));
#57796=CARTESIAN_POINT('Ctrl Pts',(3.32075755636313,4.78167045706469,15.8989716891779));
#57797=CARTESIAN_POINT('Ctrl Pts',(0.623594484557181,5.78817182078575,16.0381451465998));
#57798=CARTESIAN_POINT('Ctrl Pts',(-2.22605929319732,5.37926232222207,16.1773186040218));
#57799=CARTESIAN_POINT('Ctrl Pts',(-4.53136355935532,3.65493466440303,16.3164920614437));
#57800=CARTESIAN_POINT('Ctrl Pts',(-5.72859062921443,1.03684739040267,16.4556655188657));
#57801=CARTESIAN_POINT('Ctrl Pts',(-5.52497652620875,-1.83478540787485,
16.5948389762876));
#57802=CARTESIAN_POINT('Ctrl Pts',(-3.97031203437715,-4.25774887209054,
16.7340124337096));
#57803=CARTESIAN_POINT('Ctrl Pts',(-1.44476710669936,-5.63954352013598,
16.8731858911315));
#57804=CARTESIAN_POINT('Ctrl Pts',(1.43407401183274,-5.64227213422874,17.0123593485535));
#57805=CARTESIAN_POINT('Ctrl Pts',(3.96223377595531,-4.2652674725962,17.1515328059754));
#57806=CARTESIAN_POINT('Ctrl Pts',(5.52148852152625,-1.84525543347313,17.2907062633974));
#57807=CARTESIAN_POINT('Ctrl Pts',(5.73054581765664,1.02598622790277,17.4298797208193));
#57808=CARTESIAN_POINT('Ctrl Pts',(4.53828382882664,3.64633829987275,17.5690531782413));
#57809=CARTESIAN_POINT('Ctrl Pts',(2.23625239528441,5.37503286805699,17.7082266356632));
#57810=CARTESIAN_POINT('Ctrl Pts',(-0.612621120541769,5.78934352675451,
17.8474000930852));
#57811=CARTESIAN_POINT('Ctrl Pts',(-3.31168730249335,4.78795679999438,17.9865735505071));
#57812=CARTESIAN_POINT('Ctrl Pts',(-5.20092987768768,2.61574683703981,18.1257470079291));
#57813=CARTESIAN_POINT('Ctrl Pts',(-5.81836282614899,-0.196104898959158,
18.264920465351));
#57814=CARTESIAN_POINT('Ctrl Pts',(-5.01300215344117,-2.96000211447599,
18.404093922773));
#57815=CARTESIAN_POINT('Ctrl Pts',(-2.98178676868822,-5.00007507685475,
18.5432673801949));
#57816=CARTESIAN_POINT('Ctrl Pts',(-0.221420019377939,-5.81745445045571,
18.6824408376169));
#57817=CARTESIAN_POINT('Ctrl Pts',(2.59309168454985,-5.21226233257945,18.8216142950388));
#57818=CARTESIAN_POINT('Ctrl Pts',(4.77350159418886,-3.33248940559225,18.9607877524608));
#57819=CARTESIAN_POINT('Ctrl Pts',(5.78662307204959,-0.637806028610215,
19.0999612098827));
#57820=CARTESIAN_POINT('Ctrl Pts',(5.38471241096902,2.21284327489869,19.2391346673047));
#57821=CARTESIAN_POINT('Ctrl Pts',(3.66605085293078,4.52237484645332,19.3783081247266));
#57822=CARTESIAN_POINT('Ctrl Pts',(1.05091138103857,5.72602727703176,19.5174815821486));
#57823=CARTESIAN_POINT('Ctrl Pts',(-1.82121275372749,5.52946536418925,19.6566550395706));
#57824=CARTESIAN_POINT('Ctrl Pts',(-4.24798654403758,3.98075538431889,19.7958284969925));
#57825=CARTESIAN_POINT('Ctrl Pts',(-5.63597874951666,1.45861120354425,19.9350019544145));
#57826=CARTESIAN_POINT('Ctrl Pts',(-5.64577663239032,-1.4202145349431,20.0741754118364));
#57827=CARTESIAN_POINT('Ctrl Pts',(-4.27498426691963,-3.95174804683925,
20.2133488692584));
#57828=CARTESIAN_POINT('Ctrl Pts',(-1.85880842721184,-5.51694066843522,
20.3525223266803));
#57829=CARTESIAN_POINT('Ctrl Pts',(1.01191121669575,-5.73304795005533,20.4916957841023));
#57830=CARTESIAN_POINT('Ctrl Pts',(3.63518310470994,-4.54722408765388,20.6308692415243));
#57831=CARTESIAN_POINT('Ctrl Pts',(5.36952532510035,-2.2494445739369,20.7700426989462));
#57832=CARTESIAN_POINT('Ctrl Pts',(5.79083042327413,0.598402972077256,20.9092161563682));
#57833=CARTESIAN_POINT('Ctrl Pts',(4.79607453768151,3.29992001980522,21.0483896137901));
#57834=CARTESIAN_POINT('Ctrl Pts',(2.62851034453592,5.19449097378905,21.187563071212));
#57835=CARTESIAN_POINT('Ctrl Pts',(-0.181816746546373,5.81882683870069,
21.326736528634));
#57836=CARTESIAN_POINT('Ctrl Pts',(-2.94768327115363,5.02025561511257,21.4659099860559));
#57837=CARTESIAN_POINT('Ctrl Pts',(-4.99273793154097,2.99405595389602,21.6050834434779));
#57838=CARTESIAN_POINT('Ctrl Pts',(-5.81689319231709,0.235704682353347,
21.7442569008998));
#57839=CARTESIAN_POINT('Ctrl Pts',(-5.21861420890074,-2.58028464452422,
21.8834303583218));
#57840=CARTESIAN_POINT('Ctrl Pts',(-3.34420116000522,-4.76530394723442,
22.0226038157437));
#57841=CARTESIAN_POINT('Ctrl Pts',(-0.65201372671107,-5.78503943014121,
22.1617772731657));
#57842=CARTESIAN_POINT('Ctrl Pts',(2.19961391321817,-5.39013003005356,22.3009507305877));
#57843=CARTESIAN_POINT('Ctrl Pts',(4.51335886375986,-3.67714493527635,22.4401241880096));
#57844=CARTESIAN_POINT('Ctrl Pts',(5.72342939706778,-1.06496903470879,22.5792976454316));
#57845=CARTESIAN_POINT('Ctrl Pts',(5.53392085965116,1.80762911771912,22.7184711028535));
#57846=CARTESIAN_POINT('Ctrl Pts',(3.99117473041909,4.23819860074681,22.8576445602755));
#57847=CARTESIAN_POINT('Ctrl Pts',(1.47244650500515,5.63237999410608,22.9968180176974));
#57848=CARTESIAN_POINT('Ctrl Pts',(-1.40634649420028,5.64924708667967,23.1359914751194));
#57849=CARTESIAN_POINT('Ctrl Pts',(-3.94123848879507,4.28467528320974,23.2751649325413));
#57850=CARTESIAN_POINT('Ctrl Pts',(-5.51235954834917,1.8723502123887,23.4143383899633));
#57851=CARTESIAN_POINT('Ctrl Pts',(-5.73551551233822,-0.997830103692873,
23.5535118473852));
#57852=CARTESIAN_POINT('Ctrl Pts',(-4.55613692684949,-3.62400598949653,
23.6926853048072));
#57853=CARTESIAN_POINT('Ctrl Pts',(-2.2626231885028,-5.36398540405897,23.8318587622291));
#57854=CARTESIAN_POINT('Ctrl Pts',(0.584181215259813,-5.79228240125133,
23.9710322196511));
#57855=CARTESIAN_POINT('Ctrl Pts',(3.28813283869339,-4.80416335517584,24.1102056770731));
#57856=CARTESIAN_POINT('Ctrl Pts',(5.18802074725785,-2.64125800218955,24.249379134495));
#57857=CARTESIAN_POINT('Ctrl Pts',(5.81925576389236,0.167527497783788,24.388552591917));
#57858=CARTESIAN_POINT('Ctrl Pts',(5.02747880478565,2.93534665338514,24.5277260493389));
#57859=CARTESIAN_POINT('Ctrl Pts',(3.00630708503173,4.98537068015971,24.6668995067608));
#57860=CARTESIAN_POINT('Ctrl Pts',(0.249987924036234,5.81629685847829,24.8060729641828));
#57861=CARTESIAN_POINT('Ctrl Pts',(-2.5674620454557,5.22493461712705,24.9452464216047));
#57862=CARTESIAN_POINT('Ctrl Pts',(-4.75707756563297,3.35589274898047,25.0844198790267));
#57863=CARTESIAN_POINT('Ctrl Pts',(-5.7834209046099,0.666217493187736,25.2235933364487));
#57864=CARTESIAN_POINT('Ctrl Pts',(-5.39551514680761,-2.18637128792844,
25.3627667938706));
#57865=CARTESIAN_POINT('Ctrl Pts',(-3.68821684454273,-4.50431566564105,
25.5019402512926));
#57866=CARTESIAN_POINT('Ctrl Pts',(-1.07902026664608,-5.72079700498761,
25.6411137087145));
#57867=CARTESIAN_POINT('Ctrl Pts',(1.79403458175868,-5.53834298572796,25.7802871661365));
#57868=CARTESIAN_POINT('Ctrl Pts',(4.22838510123925,-4.0015700098494,25.9194606235584));
#57869=CARTESIAN_POINT('Ctrl Pts',(5.62874727560461,-1.48627292765558,26.0586340809804));
#57870=CARTESIAN_POINT('Ctrl Pts',(5.65268347617007,1.39246997322817,26.1978075384023));
#57871=CARTESIAN_POINT('Ctrl Pts',(4.29434046302999,3.93070516519512,26.3369809958243));
#57872=CARTESIAN_POINT('Ctrl Pts',(1.88588070734713,5.5077451888921,26.4761544532462));
#57873=CARTESIAN_POINT('Ctrl Pts',(-0.983742973802929,5.73794848962602,
26.6153279106682));
#57874=CARTESIAN_POINT('Ctrl Pts',(-3.61280702163031,4.56502229266922,26.7545013680901));
#57875=CARTESIAN_POINT('Ctrl Pts',(-5.35841313833848,2.27578815951525,26.8936748255121));
#57876=CARTESIAN_POINT('Ctrl Pts',(-5.79369945193068,-0.569955935846374,
27.032848282934));
#57877=CARTESIAN_POINT('Ctrl Pts',(-4.81222320370199,-3.27632583023427,
27.172021740356));
#57878=CARTESIAN_POINT('Ctrl Pts',(-2.65398973313268,-5.18151923710938,
27.3111951977779));
#57879=CARTESIAN_POINT('Ctrl Pts',(0.153237238835168,-5.81964959913759,
27.4503686551999));
#57880=CARTESIAN_POINT('Ctrl Pts',(2.92299233555996,-5.03467167890479,27.5895421126218));
#57881=CARTESIAN_POINT('Ctrl Pts',(4.97797336713532,-3.01854008822139,27.7287155700438));
#57882=CARTESIAN_POINT('Ctrl Pts',(5.81566545253513,-0.264269658299064,
27.8678890274657));
#57883=CARTESIAN_POINT('Ctrl Pts',(5.23122351914651,2.55462396466421,28.0070624848877));
#57884=CARTESIAN_POINT('Ctrl Pts',(3.36756410201807,4.74882249898934,28.1462359423097));
#57885=CARTESIAN_POINT('Ctrl Pts',(0.680417242391902,5.78176750521534,28.2854093997316));
#57886=CARTESIAN_POINT('Ctrl Pts',(-2.17311547888214,5.40086772875906,28.4245828571536));
#57887=CARTESIAN_POINT('Ctrl Pts',(-4.49524530662713,3.69926651396665,28.5637563145755));
#57888=CARTESIAN_POINT('Ctrl Pts',(-5.71813011666452,1.0930649921219,28.7029297719975));
#57889=CARTESIAN_POINT('Ctrl Pts',(-5.54273171575438,-1.78042922782082,
28.8421032294194));
#57890=CARTESIAN_POINT('Ctrl Pts',(-4.01194115992657,-4.21854610469001,
28.9812766868414));
#57891=CARTESIAN_POINT('Ctrl Pts',(-1.50009038812259,-5.62508061591747,
29.1204501442633));
#57892=CARTESIAN_POINT('Ctrl Pts',(1.37858505570179,-5.65608578014017,29.2596236016853));
#57893=CARTESIAN_POINT('Ctrl Pts',(3.92014813955503,-4.3039797480996,29.3987970591072));
#57894=CARTESIAN_POINT('Ctrl Pts',(5.50309761788848,-1.89939983049864,29.5379705165292));
#57895=CARTESIAN_POINT('Ctrl Pts',(5.74034686724793,0.969649911970882,29.6771439739511));
#57896=CARTESIAN_POINT('Ctrl Pts',(4.5738801315346,3.60158626864069,29.8163174313731));
#57897=CARTESIAN_POINT('Ctrl Pts',(2.28893940758999,5.35280856153943,29.955490888795));
#57898=CARTESIAN_POINT('Ctrl Pts',(-0.555727219614797,5.79508156676741,
30.094664346217));
#57899=CARTESIAN_POINT('Ctrl Pts',(-3.26449906562366,4.82025403465942,30.2338378036389));
#57900=CARTESIAN_POINT('Ctrl Pts',(-5.17498648254752,2.6667054605934,30.3730112610609));
#57901=CARTESIAN_POINT('Ctrl Pts',(-5.82000834206158,-0.138946055870331,
30.5121847184828));
#57902=CARTESIAN_POINT('Ctrl Pts',(-5.04183419409715,-2.9106203921743,30.6513581759048));
#57903=CARTESIAN_POINT('Ctrl Pts',(-3.03075488970033,-4.97054603707336,
30.7905316333267));
#57904=CARTESIAN_POINT('Ctrl Pts',(-0.27854979902338,-5.81499897829503,
30.9297050907487));
#57905=CARTESIAN_POINT('Ctrl Pts',(2.541770479563,-5.23748087703718,31.0688785481706));
#57906=CARTESIAN_POINT('Ctrl Pts',(4.74053879708136,-3.3792151487401,31.2080520055926));
#57907=CARTESIAN_POINT('Ctrl Pts',(5.78007924192746,-0.694612888699475,
31.3472254630146));
#57908=CARTESIAN_POINT('Ctrl Pts',(5.406187743632,2.15984656601141,31.4863989204365));
#57909=CARTESIAN_POINT('Ctrl Pts',(3.71029387691888,4.48614784141211,31.6255723778585));
#57910=CARTESIAN_POINT('Ctrl Pts',(1.10710312644696,5.71542874817974,31.7647458352804));
#57911=CARTESIAN_POINT('Ctrl Pts',(-1.76681313794548,5.5470870232665,31.9039192927023));
#57912=CARTESIAN_POINT('Ctrl Pts',(-4.20868167042801,4.02228811811282,32.0430927501244));
#57913=CARTESIAN_POINT('Ctrl Pts',(-5.62138003715451,1.51389880308725,32.1822662075462));
#57914=CARTESIAN_POINT('Ctrl Pts',(-5.65945397807416,-1.3646918253469,32.3214396649683));
#57915=CARTESIAN_POINT('Ctrl Pts',(-4.31359308029392,-3.9095674755334,32.4606131223902));
#57916=CARTESIAN_POINT('Ctrl Pts',(-1.9129075003232,-5.49841686336308,32.5997865798122));
#57917=CARTESIAN_POINT('Ctrl Pts',(0.955551003177575,-5.74271063074177,
32.7389600372341));
#57918=CARTESIAN_POINT('Ctrl Pts',(3.59034379818857,-4.58271039003308,32.8781334946561));
#57919=CARTESIAN_POINT('Ctrl Pts',(5.34717170745731,-2.30207685342522,33.017306952078));
#57920=CARTESIAN_POINT('Ctrl Pts',(5.79642873742743,0.541495152364058,33.1564804095));
#57921=CARTESIAN_POINT('Ctrl Pts',(4.82825579962227,3.25265261617684,33.2956538669219));
#57922=CARTESIAN_POINT('Ctrl Pts',(2.67940510789608,5.16842252296468,33.4348273243439));
#57923=CARTESIAN_POINT('Ctrl Pts',(-0.124654035064796,5.82033199050108,
33.5740007817657));
#57924=CARTESIAN_POINT('Ctrl Pts',(-2.89823089783061,5.048966307173,33.7131742391878));
#57925=CARTESIAN_POINT('Ctrl Pts',(-4.96308873476043,3.04295141581364,33.8523476966097));
#57926=CARTESIAN_POINT('Ctrl Pts',(-5.81429743977679,0.292828260100349,
33.9915211540317));
#57927=CARTESIAN_POINT('Ctrl Pts',(-5.24370665306742,-2.52890166765823,
34.1306946114536));
#57928=CARTESIAN_POINT('Ctrl Pts',(-3.39084581889107,-4.73222650985951,
34.2698680688756));
#57929=CARTESIAN_POINT('Ctrl Pts',(-0.708804346511129,-5.77835612492646,
34.4090415262975));
#57930=CARTESIAN_POINT('Ctrl Pts',(2.14656462932744,-5.4114751593469,34.5482149837194));
#57931=CARTESIAN_POINT('Ctrl Pts',(4.47702332485341,-3.72129886690476,34.6873884411414));
#57932=CARTESIAN_POINT('Ctrl Pts',(5.71269291582249,-1.12113458497172,34.8265618985634));
#57933=CARTESIAN_POINT('Ctrl Pts',(5.55140888200191,1.75318639423721,34.9657353559853));
#57934=CARTESIAN_POINT('Ctrl Pts',(4.0326108220164,4.19879185793537,35.1049088134072));
#57935=CARTESIAN_POINT('Ctrl Pts',(1.52769808928541,5.61764556163005,35.2440822708293));
#57936=CARTESIAN_POINT('Ctrl Pts',(-1.35079036593903,5.66278804966198,35.3832557282512));
#57937=CARTESIAN_POINT('Ctrl Pts',(-3.89896323693118,4.32318040164498,35.5224291856731));
#57938=CARTESIAN_POINT('Ctrl Pts',(-5.4937029535406,1.92640363537021,35.6616026430951));
#57939=CARTESIAN_POINT('Ctrl Pts',(-5.74503976585416,-0.941446332438793,
35.800776100517));
#57940=CARTESIAN_POINT('Ctrl Pts',(-4.59151301491858,-3.57907967806551,
35.939949557939));
#57941=CARTESIAN_POINT('Ctrl Pts',(-2.31520041780278,-5.34150261008211,
36.0791230153609));
#57942=CARTESIAN_POINT('Ctrl Pts',(0.527259819912814,-5.79774095578733,
36.2182964727829));
#57943=CARTESIAN_POINT('Ctrl Pts',(3.2407865533273,-4.83622845034032,36.3574699302048));
#57944=CARTESIAN_POINT('Ctrl Pts',(5.16182739794124,-2.69208859846242,36.4966433876268));
#57945=CARTESIAN_POINT('Ctrl Pts',(5.82062054250453,0.110361262598867,36.6358168450488));
#57946=CARTESIAN_POINT('Ctrl Pts',(5.05606797512593,2.88582392723711,36.7749903024707));
#57947=CARTESIAN_POINT('Ctrl Pts',(3.05512959301669,4.95560150516381,36.9141637598927));
#57948=CARTESIAN_POINT('Ctrl Pts',(0.307104955431337,5.81356084121064,37.0533372173146));
#57949=CARTESIAN_POINT('Ctrl Pts',(-2.51601760654839,5.24990080969599,37.1925106747365));
#57950=CARTESIAN_POINT('Ctrl Pts',(-4.72388568744661,3.40245604233844,37.3316841321585));
#57951=CARTESIAN_POINT('Ctrl Pts',(-5.77659816460266,0.722991530252853,
37.4708575895804));
#57952=CARTESIAN_POINT('Ctrl Pts',(-5.41672994402081,-2.13326974891985,
37.6100310470024));
#57953=CARTESIAN_POINT('Ctrl Pts',(-3.73228141756457,-4.46787181197159,
37.7492045044243));
#57954=CARTESIAN_POINT('Ctrl Pts',(-1.13515928308697,-5.70992263608972,
37.8883779618464));
#57955=CARTESIAN_POINT('Ctrl Pts',(1.73954907886489,-5.55569726589998,38.0275514192682));
#57956=CARTESIAN_POINT('Ctrl Pts',(4.18887672684745,-4.04290920939167,38.1667248766903));
#57957=CARTESIAN_POINT('Ctrl Pts',(5.61387721186295,-1.54148816350762,38.3058983341121));
#57958=CARTESIAN_POINT('Ctrl Pts',(5.6660879747992,1.33688076130373,38.4450717915342));
#57959=CARTESIAN_POINT('Ctrl Pts',(4.33274165434142,3.88833548769174,38.584245248956));
#57960=CARTESIAN_POINT('Ctrl Pts',(1.93988815425818,5.48895591684585,38.723418706378));
#57961=CARTESIAN_POINT('Ctrl Pts',(-0.927335984805442,5.74733425854047,
38.8625921638));
#57962=CARTESIAN_POINT('Ctrl Pts',(-3.56779397619399,4.60028795311144,39.0017656212219));
#57963=CARTESIAN_POINT('Ctrl Pts',(-5.33580130359836,2.32831002158779,39.1409390786439));
#57964=CARTESIAN_POINT('Ctrl Pts',(-5.79901821393447,-0.513021308099881,
39.2801125360658));
#57965=CARTESIAN_POINT('Ctrl Pts',(-4.84417193873862,-3.22890094862718,
39.4192859934878));
#57966=CARTESIAN_POINT('Ctrl Pts',(-2.70475585581123,-5.15520114724567,
39.5584594509097));
#57967=CARTESIAN_POINT('Ctrl Pts',(0.0960678246576714,-5.82087399633197,
39.6976329083317));
#57968=CARTESIAN_POINT('Ctrl Pts',(2.87339955520757,-5.06313915513303,39.8368063657536));
#57969=CARTESIAN_POINT('Ctrl Pts',(4.94808439343132,-3.06728934787535,39.9759798231756));
#57970=CARTESIAN_POINT('Ctrl Pts',(5.81278918703828,-0.32137979892819,40.1151532805975));
#57971=CARTESIAN_POINT('Ctrl Pts',(5.25606330957228,2.50311837392407,40.2543267380195));
#57972=CARTESIAN_POINT('Ctrl Pts',(3.41404574907282,4.71551638013761,40.3935001954414));
#57973=CARTESIAN_POINT('Ctrl Pts',(0.73717435437625,5.77480537155652,40.5326736528634));
#57974=CARTESIAN_POINT('Ctrl Pts',(-2.11996200495645,5.4219520659675,40.6718471102854));
#57975=CARTESIAN_POINT('Ctrl Pts',(-4.45869335795006,3.74324146267378,40.8110205677073));
#57976=CARTESIAN_POINT('Ctrl Pts',(-5.70711792568614,1.14917713622408,40.9501940251293));
#57977=CARTESIAN_POINT('Ctrl Pts',(-5.55995214910184,-1.72590127406118,
41.0893674825512));
#57978=CARTESIAN_POINT('Ctrl Pts',(-4.0531832181396,-4.17893633695223,41.2285409399732));
#57979=CARTESIAN_POINT('Ctrl Pts',(-1.55526894260013,-5.61007501057621,
41.3677143973951));
#57980=CARTESIAN_POINT('Ctrl Pts',(1.32296309531554,-5.66935373358739,41.506887854817));
#57981=CARTESIAN_POINT('Ctrl Pts',(3.87768429190016,-4.34227678072911,41.646061312239));
#57982=CARTESIAN_POINT('Ctrl Pts',(5.4841757819034,-1.95336097567572,41.7852347696609));
#57983=CARTESIAN_POINT('Ctrl Pts',(5.74959409496496,0.913220045362813,41.924408227083));
#57984=CARTESIAN_POINT('Ctrl Pts',(4.6090351516988,3.55648676062669,42.0635816845048));
#57985=CARTESIAN_POINT('Ctrl Pts',(2.34140558572941,5.33006782238494,42.2027551419269));
#57986=CARTESIAN_POINT('Ctrl Pts',(-0.49877970278341,5.80026050416698,42.3419285993487));
#57987=CARTESIAN_POINT('Ctrl Pts',(-3.21699587374662,4.85208621691798,42.4811020567708));
#57988=CARTESIAN_POINT('Ctrl Pts',(-5.14854381083423,2.717406803559,42.6202755141927));
#57989=CARTESIAN_POINT('Ctrl Pts',(-5.82109235045507,-0.0817738074305616,
42.7594489716147));
#57990=CARTESIAN_POINT('Ctrl Pts',(-5.07017980455513,-2.86095785666086,
42.8986224290365));
#57991=CARTESIAN_POINT('Ctrl Pts',(-3.07943060706636,-4.9405374448911,43.0377958864585));
#57992=CARTESIAN_POINT('Ctrl Pts',(-0.335652704513683,-5.81198248191277,
43.1769693438805));
#57993=CARTESIAN_POINT('Ctrl Pts',(2.49020404756757,-5.26219411553643,43.3161428013024));
#57994=CARTESIAN_POINT('Ctrl Pts',(4.70711863839939,-3.42561486920834,43.4553162587244));
#57995=CARTESIAN_POINT('Ctrl Pts',(5.7729777565986,-0.751352733358968,43.5944897161463));
#57996=CARTESIAN_POINT('Ctrl Pts',(5.42714149369761,2.10664147768288,43.7336631735683));
#57997=CARTESIAN_POINT('Ctrl Pts',(3.75417893614339,4.44948801813483,43.8728366309902));
#57998=CARTESIAN_POINT('Ctrl Pts',(1.16318805985547,5.70427880152416,44.0120100884122));
#57999=CARTESIAN_POINT('Ctrl Pts',(-1.71224306212229,5.56417350595057,44.1511835458341));
#58000=CARTESIAN_POINT('Ctrl Pts',(-4.16897074819021,4.06343278630797,44.2903570032561));
#58001=CARTESIAN_POINT('Ctrl Pts',(-5.6062389806971,1.56904034346491,44.429530460678));
#58002=CARTESIAN_POINT('Ctrl Pts',(-5.67258530633404,-1.30903745189791,
44.5687039181));
#58003=CARTESIAN_POINT('Ctrl Pts',(-4.35178572331137,-3.86700971378293,
44.707877375522));
#58004=CARTESIAN_POINT('Ctrl Pts',(-1.96682201838221,-5.47936257753721,
44.8470508329439));
#58005=CARTESIAN_POINT('Ctrl Pts',(0.899098599229094,-5.75181926150087,
44.9862242903659));
#58006=CARTESIAN_POINT('Ctrl Pts',(3.54515809954533,-4.61775455793575,45.1253977477878));
#58007=CARTESIAN_POINT('Ctrl Pts',(5.32430220101428,-2.35448703126236,45.2645712052098));
#58008=CARTESIAN_POINT('Ctrl Pts',(5.80146781899398,0.484535089839209,45.4037446626317));
#58009=CARTESIAN_POINT('Ctrl Pts',(4.85997123715588,3.20507140047233,45.5429181200536));
#58010=CARTESIAN_POINT('Ctrl Pts',(2.73004136542148,5.14185542885016,45.6820915774757));
#58011=CARTESIAN_POINT('Ctrl Pts',(-0.0674792971093948,5.82127560355717,
45.8212650348976));
#58012=CARTESIAN_POINT('Ctrl Pts',(-2.84849890661951,5.07718988093764,45.9604384923196));
#58013=CARTESIAN_POINT('Ctrl Pts',(-4.93296070505069,3.09155329737884,46.0996119497415));
#58014=CARTESIAN_POINT('Ctrl Pts',(-5.81114073069848,0.349923586123267,
46.2387854071635));
#58015=CARTESIAN_POINT('Ctrl Pts',(-5.26829319062015,-2.47727470535134,
46.3779588645854));
#58016=CARTESIAN_POINT('Ctrl Pts',(-3.43716333298409,-4.69869251286972,
46.5171323220073));
#58017=CARTESIAN_POINT('Ctrl Pts',(-0.765526581706437,-5.77111533074925,
46.6563057794293));
#58018=CARTESIAN_POINT('Ctrl Pts',(2.09330824742092,-5.43229819591927,46.7954792368513));
#58019=CARTESIAN_POINT('Ctrl Pts',(4.44025584803343,-3.76509377202123,46.9346526942732));
#58020=CARTESIAN_POINT('Ctrl Pts',(5.70140528072348,-1.17719196949634,47.0738261516952));
#58021=CARTESIAN_POINT('Ctrl Pts',(5.5683613109917,1.69857452540621,47.2129996091171));
#58022=CARTESIAN_POINT('Ctrl Pts',(4.07365785209267,4.15898002065313,47.3521730665391));
#58023=CARTESIAN_POINT('Ctrl Pts',(1.58280228306146,5.6023691453566,47.4913465239609));
#58024=CARTESIAN_POINT('Ctrl Pts',(-1.29510391502142,5.675782673553,47.630519981383));
#58025=CARTESIAN_POINT('Ctrl Pts',(-3.85631181770711,4.36126842474991,47.7696934388049));
#58026=CARTESIAN_POINT('Ctrl Pts',(-5.47451633277077,1.98027120120814,47.9088668962269));
#58027=CARTESIAN_POINT('Ctrl Pts',(-5.75400974473055,-0.884971731556399,
48.0480403536488));
#58028=CARTESIAN_POINT('Ctrl Pts',(-4.62644611924429,-3.53380806126163,
48.1872138110708));
#58029=CARTESIAN_POINT('Ctrl Pts',(-2.36755427930561,-5.31850447425306,
48.3263872684927));
#58030=CARTESIAN_POINT('Ctrl Pts',(0.47028755516223,-5.80264015113532,48.4655607259147));
#58031=CARTESIAN_POINT('Ctrl Pts',(3.19312760070882,-4.86782695190572,48.6047341833366));
#58032=CARTESIAN_POINT('Ctrl Pts',(5.13513604162437,-2.7426594652123,48.7439076407586));
#58033=CARTESIAN_POINT('Ctrl Pts',(5.82142375453324,0.0531843798899842,
48.8830810981805));
#58034=CARTESIAN_POINT('Ctrl Pts',(5.08416934200986,2.83602278021093,49.0222545556025));
#58035=CARTESIAN_POINT('Ctrl Pts',(3.10365734571302,4.92535421959779,49.1614280130244));
#58036=CARTESIAN_POINT('Ctrl Pts',(0.364192357703599,5.81026393847117,49.3006014704464));
#58037=CARTESIAN_POINT('Ctrl Pts',(-2.46433042523922,5.27436049804604,49.4397749278683));
#58038=CARTESIAN_POINT('Ctrl Pts',(-4.69023805435808,3.44869107076287,49.5789483852903));
#58039=CARTESIAN_POINT('Ctrl Pts',(-5.7692181052389,0.779695813950434,49.7181218427123));
#58040=CARTESIAN_POINT('Ctrl Pts',(-5.4374221415376,-2.07996239456987,49.8572953001342));
#58041=CARTESIAN_POINT('Ctrl Pts',(-3.77598590449091,-4.43099690331579,
49.9964687575561));
#58042=CARTESIAN_POINT('Ctrl Pts',(-1.19118878070317,-5.69849738061141,
50.1356422149781));
#58043=CARTESIAN_POINT('Ctrl Pts',(1.68489574633413,-5.5725155389728,50.2748156724));
#58044=CARTESIAN_POINT('Ctrl Pts',(4.14896421458505,-4.08385835383659,50.413989129822));
#58045=CARTESIAN_POINT('Ctrl Pts',(5.59846552788978,-1.59655467840533,50.553162587244));
#58046=CARTESIAN_POINT('Ctrl Pts',(5.67894581596416,1.28116256870522,50.6923360446659));
#58047=CARTESIAN_POINT('Ctrl Pts',(4.37072482786413,3.84559066818093,50.8315095020879));
#58048=CARTESIAN_POINT('Ctrl Pts',(1.99370844305515,5.46963707682683,50.9706829595098));
#58049=CARTESIAN_POINT('Ctrl Pts',(-0.870839527529374,5.75616553144545,
51.1098564169318));
#58050=CARTESIAN_POINT('Ctrl Pts',(-3.52243671421602,4.63510978321455,51.2490298743537));
#58051=CARTESIAN_POINT('Ctrl Pts',(-5.31267467706141,2.38060725106401,51.3882033317757));
#58052=CARTESIAN_POINT('Ctrl Pts',(-5.8037774935219,-0.456037184664693,
51.5273767891976));
#58053=CARTESIAN_POINT('Ctrl Pts',(-4.87565331379773,-3.18116454647687,
51.6665502466195));
#58054=CARTESIAN_POINT('Ctrl Pts',(-2.75526102684471,-5.12838568967457,
51.8057237040416));
#58055=CARTESIAN_POINT('Ctrl Pts',(0.038889141970282,-5.82153680248996,
51.9448971614634));
#58056=CARTESIAN_POINT('Ctrl Pts',(2.82352955266579,-5.09111814568579,52.0840706188855));
#58057=CARTESIAN_POINT('Ctrl Pts',(4.91771803439929,-3.11574267908185,52.2232440763073));
#58058=CARTESIAN_POINT('Ctrl Pts',(5.80935211051787,-0.378458933214385,
52.3624175337294));
#58059=CARTESIAN_POINT('Ctrl Pts',(5.28039600122842,2.45137128528485,52.5015909911512));
#58060=CARTESIAN_POINT('Ctrl Pts',(3.46019801303277,4.68175531384462,52.6407644485732));
#58061=CARTESIAN_POINT('Ctrl Pts',(0.793860344650892,5.76728609150777,52.7799379059952));
#58062=CARTESIAN_POINT('Ctrl Pts',(-2.06660399960485,5.44251329965536,52.9191113634171));
#58063=CARTESIAN_POINT('Ctrl Pts',(-4.42171123981307,3.78685526787318,53.0582848208391));
#58064=CARTESIAN_POINT('Ctrl Pts',(-5.69555511872252,1.2051784090756,53.197458278261));
#58065=CARTESIAN_POINT('Ctrl Pts',(-5.57663616484398,-1.67120680738872,
53.336631735683));
#58066=CARTESIAN_POINT('Ctrl Pts',(-4.09403423003101,-4.13892339038096,
53.475805193105));
#58067=CARTESIAN_POINT('Ctrl Pts',(-1.61029744656999,-5.59452815183536,
53.6149786505269));
#58068=CARTESIAN_POINT('Ctrl Pts',(1.26721349701524,-5.68207471449387,53.7541521079489));
#58069=CARTESIAN_POINT('Ctrl Pts',(3.83484632985259,-4.38015487563218,53.8933255653708));
#58070=CARTESIAN_POINT('Ctrl Pts',(5.46472483912719,-2.00713366289706,54.0324990227928));
#58071=CARTESIAN_POINT('Ctrl Pts',(5.75828660864619,0.856702072364817,54.1716724802147));
#58072=CARTESIAN_POINT('Ctrl Pts',(4.6437454976049,3.51104412697739,54.3108459376366));
#58073=CARTESIAN_POINT('Ctrl Pts',(2.39364586782849,5.30681284459288,54.4500193950587));
#58074=CARTESIAN_POINT('Ctrl Pts',(-0.441784064276092,5.80487983929558,
54.5891928524805));
#58075=CARTESIAN_POINT('Ctrl Pts',(-3.16918230991358,4.88345027563905,54.7283663099026));
#58076=CARTESIAN_POINT('Ctrl Pts',(-5.12160441370534,2.76784597433134,54.8675397673244));
#58077=CARTESIAN_POINT('Ctrl Pts',(-5.82161474674563,-0.0245936695504916,
55.0067132247464));
#58078=CARTESIAN_POINT('Ctrl Pts',(-5.09803625006422,-2.81101929931819,
55.1458866821684));
#58079=CARTESIAN_POINT('Ctrl Pts',(-3.12780922461082,-4.91005219550135,
55.2850601395903));
#58080=CARTESIAN_POINT('Ctrl Pts',(-0.392723226628261,-5.80840525233691,
55.4242335970124));
#58081=CARTESIAN_POINT('Ctrl Pts',(2.43839736363178,-5.28639966377323,55.5634070544342));
#58082=CARTESIAN_POINT('Ctrl Pts',(4.67324434248021,-3.47168409040697,55.7025805118563));
#58083=CARTESIAN_POINT('Ctrl Pts',(5.76531930120589,-0.808020088395763,
55.8417539692781));
#58084=CARTESIAN_POINT('Ctrl Pts',(5.44757163957287,2.05323314307691,55.9809274267001));
#58085=CARTESIAN_POINT('Ctrl Pts',(3.79770179662585,4.41239891351779,56.120100884122));
#58086=CARTESIAN_POINT('Ctrl Pts',(1.21916077025623,5.69257851279861,56.259274341544));
#58087=CARTESIAN_POINT('Ctrl Pts',(-1.6575077911142,5.58072316375789,56.3984477989659));
#58088=CARTESIAN_POINT('Ctrl Pts',(-4.128857608587,4.10418541931544,56.5376212563879));
#58089=CARTESIAN_POINT('Ctrl Pts',(-5.59055704093568,1.6240305046866,56.6767947138098));
#58090=CARTESIAN_POINT('Ctrl Pts',(-5.68516935027489,-1.2532567840643,56.8159681712319));
#58091=CARTESIAN_POINT('Ctrl Pts',(-4.38955851119091,-3.8240788675104,56.9551416286537));
#58092=CARTESIAN_POINT('Ctrl Pts',(-2.02054677977986,-5.45977964929258,
57.0943150860758));
#58093=CARTESIAN_POINT('Ctrl Pts',(0.842559451311496,-5.76037296354271,
57.2334885434976));
#58094=CARTESIAN_POINT('Ctrl Pts',(3.49963036824299,-4.65235321034202,57.3726620009197));
#58095=CARTESIAN_POINT('Ctrl Pts',(5.30091901219416,-2.40667005097636,57.5118354583415));
#58096=CARTESIAN_POINT('Ctrl Pts',(5.80594718180918,0.427528279942165,57.6510089157636));
#58097=CARTESIAN_POINT('Ctrl Pts',(4.89121779041446,3.15718096327107,57.7901823731854));
#58098=CARTESIAN_POINT('Ctrl Pts',(2.7804142317859,5.11479225460728,57.9293558306075));
#58099=CARTESIAN_POINT('Ctrl Pts',(-0.0102980488312426,5.82165758683027,
58.0685292880293));
#58100=CARTESIAN_POINT('Ctrl Pts',(-2.79849209560402,5.1049236134295,58.2077027454514));
#58101=CARTESIAN_POINT('Ctrl Pts',(-4.9023567491284,3.13985690953957,58.3468762028732));
#58102=CARTESIAN_POINT('Ctrl Pts',(-5.80742336963775,0.406985151932601,
58.4860496602953));
#58103=CARTESIAN_POINT('Ctrl Pts',(-5.29237144947885,-2.42540873851179,
58.6252231177171));
#58104=CARTESIAN_POINT('Ctrl Pts',(-3.4831492336253,-4.66470519158539,58.7643965751392));
#58105=CARTESIAN_POINT('Ctrl Pts',(-0.822174959802854,-5.76331774619284,
58.9035700325611));
#58106=CARTESIAN_POINT('Ctrl Pts',(2.03984990561131,-5.45259713078876,59.042743489983));
#58107=CARTESIAN_POINT('Ctrl Pts',(4.40305998058257,-3.80852542534511,59.181916947405));
#58108=CARTESIAN_POINT('Ctrl Pts',(5.68956758078844,-1.23313577993252,59.321090404827));
#58109=CARTESIAN_POINT('Ctrl Pts',(5.58477651107019,1.64379878011469,59.4602638622489));
#58110=CARTESIAN_POINT('Ctrl Pts',(4.11431186047907,4.11876692989892,59.5994373196709));
#58111=CARTESIAN_POINT('Ctrl Pts',(1.63775376994569,5.58655221913655,59.7386107770928));
#58112=CARTESIAN_POINT('Ctrl Pts',(-1.23929251400999,5.68822970464623,59.8777842345147));
#58113=CARTESIAN_POINT('Ctrl Pts',(-3.81328834608205,4.39893567783821,60.0169576919367));
#58114=CARTESIAN_POINT('Ctrl Pts',(-5.45480153714079,2.03394771282132,60.1561311493587));
#58115=CARTESIAN_POINT('Ctrl Pts',(-5.7624245835571,-0.828411749644193,
60.2953046067806));
#58116=CARTESIAN_POINT('Ctrl Pts',(-4.66093286951688,-3.48819550684506,
60.4344780642026));
#58117=CARTESIAN_POINT('Ctrl Pts',(-2.41967972198274,-5.29499321538886,
60.5736515216245));
#58118=CARTESIAN_POINT('Ctrl Pts',(0.413269917644382,-5.80697951465775,
60.7128249790465));
#58119=CARTESIAN_POINT('Ctrl Pts',(3.14516057887895,-4.89895581122554,60.8519984364683));
#58120=CARTESIAN_POINT('Ctrl Pts',(5.10794925353242,-2.79296572353979,60.9911718938905));
#58121=CARTESIAN_POINT('Ctrl Pts',(5.82166532233976,-0.00399763375499086,
61.1303453513122));
#58122=CARTESIAN_POINT('Ctrl Pts',(5.11178019453513,2.78594801661381,61.2695188087344));
#58123=CARTESIAN_POINT('Ctrl Pts',(3.15188566066619,4.8946317425585,61.4086922661561));
#58124=CARTESIAN_POINT('Ctrl Pts',(0.421244624209318,5.8064064666356,61.5478657235783));
#58125=CARTESIAN_POINT('Ctrl Pts',(-2.41240549035484,5.29831132566154,61.6870391810001));
#58126=CARTESIAN_POINT('Ctrl Pts',(-4.65613790853897,3.49459336706648,61.8262126384222));
#58127=CARTESIAN_POINT('Ctrl Pts',(-5.76128144655755,0.836324886168248,
61.965386095844));
#58128=CARTESIAN_POINT('Ctrl Pts',(-5.45758972735978,-2.02645439257844,
62.104559553266));
#58129=CARTESIAN_POINT('Ctrl Pts',(-3.81932611926446,-4.39369444921115,
62.2437330106879));
#58130=CARTESIAN_POINT('Ctrl Pts',(-1.24710329435501,-5.68652243467089,
62.3829064681099));
#58131=CARTESIAN_POINT('Ctrl Pts',(1.6300797410584,-5.58879599936766,62.5220799255319));
#58132=CARTESIAN_POINT('Ctrl Pts',(4.10865164137838,-4.12441384928666,62.6612533829538));
#58133=CARTESIAN_POINT('Ctrl Pts',(5.58251326942761,-1.65146646371945,62.8004268403757));
#58134=CARTESIAN_POINT('Ctrl Pts',(5.69125661949348,1.22531941397321,62.9396002977978));
#58135=CARTESIAN_POINT('Ctrl Pts',(4.40828464121373,3.80247747719103,63.0787737552196));
#58136=CARTESIAN_POINT('Ctrl Pts',(2.04733965326144,5.44978537141329,63.2179472126416));
#58137=CARTESIAN_POINT('Ctrl Pts',(-0.814265433823321,5.76445152192786,
63.3571206700635));
#58138=CARTESIAN_POINT('Ctrl Pts',(-3.47672716658331,4.66946479156297,63.4962941274855));
#58139=CARTESIAN_POINT('Ctrl Pts',(-5.28905976826099,2.43271310992216,63.6354675849074));
#58140=CARTESIAN_POINT('Ctrl Pts',(-5.80792939989083,-0.399083999576159,
63.7746410423294));
#58141=CARTESIAN_POINT('Ctrl Pts',(-4.90675767715171,-3.13297268635812,
63.9138144997514));
#58142=CARTESIAN_POINT('Ctrl Pts',(-2.80530899012875,-5.1013902832278,64.0529879571733));
#58143=CARTESIAN_POINT('Ctrl Pts',(-0.947612210060709,-5.58096655911489,
64.1457702621213));
#58144=CARTESIAN_POINT('Ctrl Pts',(-0.0175462161132968,-5.58388909905792,
64.1921614145953));
#58145=CARTESIAN_POINT('Ctrl Pts',(3.05041111877654,-4.27420965560366,-0.192161414595281));
#58146=CARTESIAN_POINT('Ctrl Pts',(3.76233375569806,-3.7661258454127,-0.145770262121297));
#58147=CARTESIAN_POINT('Ctrl Pts',(4.92665920277249,-2.38785367349441,-0.0529879571733284));
#58148=CARTESIAN_POINT('Ctrl Pts',(5.46823513289247,0.26517346728844,0.0861855002486236));
#58149=CARTESIAN_POINT('Ctrl Pts',(4.67268076690381,2.85263829294777,0.225358957670576));
#58150=CARTESIAN_POINT('Ctrl Pts',(2.73447316988989,4.74288662645417,0.364532415092528));
#58151=CARTESIAN_POINT('Ctrl Pts',(0.127600426951083,5.47315307622901,0.50370587251448));
#58152=CARTESIAN_POINT('Ctrl Pts',(-2.51047986399426,4.86513389280572,0.642879329936433));
#58153=CARTESIAN_POINT('Ctrl Pts',(-4.53465740262938,3.0673717525868,0.782052787358385));
#58154=CARTESIAN_POINT('Ctrl Pts',(-5.44995353740829,0.51955393007344,0.921226244780337));
#58155=CARTESIAN_POINT('Ctrl Pts',(-5.03254439112882,-2.15532545086806,
1.06039970220229));
#58156=CARTESIAN_POINT('Ctrl Pts',(-3.38450210013749,-4.30314585790824,
1.19957315962424));
#58157=CARTESIAN_POINT('Ctrl Pts',(-0.908830263630935,-5.39869955892152,
1.3387466170462));
#58158=CARTESIAN_POINT('Ctrl Pts',(1.78908233658119,-5.17408034133589,1.47792007446815));
#58159=CARTESIAN_POINT('Ctrl Pts',(4.04950164977306,-3.68421800789032,1.6170935318901));
#58160=CARTESIAN_POINT('Ctrl Pts',(5.3196758681094,-1.29343481442091,1.75626698931205));
#58161=CARTESIAN_POINT('Ctrl Pts',(5.28900291516093,1.41363829518363,1.895440446734));
#58162=CARTESIAN_POINT('Ctrl Pts',(3.9649833852255,3.77502741500648,2.03461390415595));
#58163=CARTESIAN_POINT('Ctrl Pts',(1.67138646397891,5.21328997302147,2.17378736157791));
#58164=CARTESIAN_POINT('Ctrl Pts',(-1.0309230246464,5.37672045824918,2.31296081899986));
#58165=CARTESIAN_POINT('Ctrl Pts',(-3.48113570323994,4.22535434344311,2.45213427642181));
#58166=CARTESIAN_POINT('Ctrl Pts',(-5.08008870302382,2.04074101801902,2.59130773384376));
#58167=CARTESIAN_POINT('Ctrl Pts',(-5.43678197806404,-0.642905010163819,
2.73048119126572));
#58168=CARTESIAN_POINT('Ctrl Pts',(-4.46399152227217,-3.16933823002763,
2.86965464868767));
#58169=CARTESIAN_POINT('Ctrl Pts',(-2.39959869431088,-4.92075718119219,
3.00882810610962));
#58170=CARTESIAN_POINT('Ctrl Pts',(0.251580110647388,-5.468878548288,3.14800156353158));
#58171=CARTESIAN_POINT('Ctrl Pts',(2.84123876169776,-4.67966744845125,3.28717502095352));
#58172=CARTESIAN_POINT('Ctrl Pts',(4.73611496153384,-2.74611365383239,3.42634847837548));
#58173=CARTESIAN_POINT('Ctrl Pts',(5.47284507153052,-0.141038830706225,
3.56552193579743));
#58174=CARTESIAN_POINT('Ctrl Pts',(4.87127276036557,2.49852492940865,3.70469539321938));
#58175=CARTESIAN_POINT('Ctrl Pts',(3.07850354080767,4.52711178103092,3.84386885064134));
#58176=CARTESIAN_POINT('Ctrl Pts',(0.532932316375539,5.44866114517237,3.98304230806329));
#58177=CARTESIAN_POINT('Ctrl Pts',(-2.14295953654073,5.03782190569276,4.12221576548524));
#58178=CARTESIAN_POINT('Ctrl Pts',(-4.29482268067486,3.3950586549128,4.26138922290719));
#58179=CARTESIAN_POINT('Ctrl Pts',(-5.39645116315218,0.922084579877679,
4.40056268032915));
#58180=CARTESIAN_POINT('Ctrl Pts',(-5.17845821236713,-1.77637149028642,
4.53973613775109));
#58181=CARTESIAN_POINT('Ctrl Pts',(-3.69415074456122,-4.04044247641186,
4.67890959517305));
#58182=CARTESIAN_POINT('Ctrl Pts',(-1.30649395460974,-5.316483675824,4.818083052595));
#58183=CARTESIAN_POINT('Ctrl Pts',(1.40064639459327,-5.29245829516381,4.95725651001695));
#58184=CARTESIAN_POINT('Ctrl Pts',(3.76527961330509,-3.97424138199533,5.0964299674389));
#58185=CARTESIAN_POINT('Ctrl Pts',(5.20917000868316,-1.68418316978025,5.23560342486086));
#58186=CARTESIAN_POINT('Ctrl Pts',(5.37923577651641,1.01771685128088,5.37477688228281));
#58187=CARTESIAN_POINT('Ctrl Pts',(4.23388987644961,3.47074943532844,5.51395033970476));
#58188=CARTESIAN_POINT('Ctrl Pts',(2.05320952080847,5.07506214665364,5.65312379712671));
#58189=CARTESIAN_POINT('Ctrl Pts',(-0.629552519391957,5.4383443026405,5.79229725454867));
#58190=CARTESIAN_POINT('Ctrl Pts',(-3.15836690532162,4.47176068457429,5.93147071197062));
#58191=CARTESIAN_POINT('Ctrl Pts',(-4.91484989486473,2.41167486193376,6.07064416939257));
#58192=CARTESIAN_POINT('Ctrl Pts',(-5.46947983942586,-0.238149983937169,
6.20981762681453));
#58193=CARTESIAN_POINT('Ctrl Pts',(-4.68663028001475,-2.82973881253801,
6.34899108423647));
#58194=CARTESIAN_POINT('Ctrl Pts',(-2.75773536963051,-4.72935733052854,
6.48816454165843));
#58195=CARTESIAN_POINT('Ctrl Pts',(-0.154477513857432,-5.47248223628434,
6.62733799908038));
#58196=CARTESIAN_POINT('Ctrl Pts',(2.48655550786828,-4.87739344681409,6.76651145650233));
#58197=CARTESIAN_POINT('Ctrl Pts',(4.51953856416763,-3.08961102660784,6.90568491392428));
#58198=CARTESIAN_POINT('Ctrl Pts',(5.44733604990991,-0.546310431977095,
7.04485837134624));
#58199=CARTESIAN_POINT('Ctrl Pts',(5.04306896426723,2.13058220925168,7.18403182876818));
#58200=CARTESIAN_POINT('Ctrl Pts',(3.40559477761184,4.2864728319958,7.32320528619014));
#58201=CARTESIAN_POINT('Ctrl Pts',(0.935333315454048,5.3941706237138,7.46237874361209));
#58202=CARTESIAN_POINT('Ctrl Pts',(-1.76364992199664,5.18280465398576,7.60155220103404));
#58203=CARTESIAN_POINT('Ctrl Pts',(-4.03135894469488,3.70406130993586,7.74072565845601));
#58204=CARTESIAN_POINT('Ctrl Pts',(-5.31325942252598,1.31954516318089,7.87989911587794));
#58205=CARTESIAN_POINT('Ctrl Pts',(-5.2958817632131,-1.38764602071352,8.01907257329991));
#58206=CARTESIAN_POINT('Ctrl Pts',(-3.98347541347518,-3.75550912114109,
8.15824603072185));
#58207=CARTESIAN_POINT('Ctrl Pts',(-1.6969697203782,-5.20501862598538,8.29741948814381));
#58208=CARTESIAN_POINT('Ctrl Pts',(1.00450454130311,-5.38171866184369,8.43659294556577));
#58209=CARTESIAN_POINT('Ctrl Pts',(3.46034223879862,-4.2423998773243,8.5757664029877));
#58210=CARTESIAN_POINT('Ctrl Pts',(5.07000498785365,-2.06566564377547,8.71493986040967));
#58211=CARTESIAN_POINT('Ctrl Pts',(5.43987383412996,0.616196232935,8.8541133178316));
#58212=CARTESIAN_POINT('Ctrl Pts',(4.47950288230013,3.14737653549747,8.99328677525359));
#58213=CARTESIAN_POINT('Ctrl Pts',(2.42373648721916,4.90891297226358,9.13246023267551));
#58214=CARTESIAN_POINT('Ctrl Pts',(-0.224718421185856,5.4700481496889,9.27163369009748));
#58215=CARTESIAN_POINT('Ctrl Pts',(-2.81822180013563,4.69356485136569,9.41080714751942));
#58216=CARTESIAN_POINT('Ctrl Pts',(-4.72257118163238,2.76934045634526,9.54998060494138));
#58217=CARTESIAN_POINT('Ctrl Pts',(-5.47208640212667,0.167915265522693,
9.68915406236333));
#58218=CARTESIAN_POINT('Ctrl Pts',(-4.88348472271888,-2.47457109247371,
9.82832751978529));
#58219=CARTESIAN_POINT('Ctrl Pts',(-3.10069988214165,-4.5119380946132,9.96750097720723));
#58220=CARTESIAN_POINT('Ctrl Pts',(-0.559685253342231,-5.44597810736753,
10.1066744346292));
#58221=CARTESIAN_POINT('Ctrl Pts',(2.11819203461263,-5.04828561327891,10.2458478920511));
#58222=CARTESIAN_POINT('Ctrl Pts',(4.27809713600777,-3.41611036467168,10.3850213494731));
#58223=CARTESIAN_POINT('Ctrl Pts',(5.39185755758026,-0.94857641099696,10.524194806895));
#58224=CARTESIAN_POINT('Ctrl Pts',(5.18711984344,1.75091771894802,10.663368264317));
#58225=CARTESIAN_POINT('Ctrl Pts',(3.71394953992634,4.02225110399837,10.8025417217389));
#58226=CARTESIAN_POINT('Ctrl Pts',(1.3325884149323,5.31000313042501,10.9417151791609));
#58227=CARTESIAN_POINT('Ctrl Pts',(-1.37463727936781,5.29927329724628,11.0808886365828));
#58228=CARTESIAN_POINT('Ctrl Pts',(-3.74571598336408,3.9926854247118,11.2200620940048));
#58229=CARTESIAN_POINT('Ctrl Pts',(-5.20083585717358,1.70974603829712,11.3592355514267));
#58230=CARTESIAN_POINT('Ctrl Pts',(-5.38416909556079,-0.991286174191518,
11.4984090088487));
#58231=CARTESIAN_POINT('Ctrl Pts',(-4.25088429664866,-3.44991417650368,
11.6375824662706));
#58232=CARTESIAN_POINT('Ctrl Pts',(-2.07810931083753,-5.06491725706803,
11.7767559236926));
#58233=CARTESIAN_POINT('Ctrl Pts',(0.6028362308323,-5.44137056333522,11.9159293811146));
#58234=CARTESIAN_POINT('Ctrl Pts',(3.13636718708249,-4.48721806875122,12.0551028385365));
#58235=CARTESIAN_POINT('Ctrl Pts',(4.90294644905707,-2.43578349744261,12.1942762959585));
#58236=CARTESIAN_POINT('Ctrl Pts',(5.47058347571745,0.211285503388863,12.3334497533804));
#58237=CARTESIAN_POINT('Ctrl Pts',(4.70047112065431,2.80668779393611,12.4726232108024));
#58238=CARTESIAN_POINT('Ctrl Pts',(2.78092884401596,4.71575655576655,12.6117966682243));
#58239=CARTESIAN_POINT('Ctrl Pts',(0.181352004663688,5.47165757144393,12.7509701256463));
#58240=CARTESIAN_POINT('Ctrl Pts',(-2.46257175548597,4.88954655134992,12.8901435830682));
#58241=CARTESIAN_POINT('Ctrl Pts',(-4.50431041820064,3.11177004054354,13.0293170404902));
#58242=CARTESIAN_POINT('Ctrl Pts',(-5.44458732573234,0.57305669982123,13.1684904979121));
#58243=CARTESIAN_POINT('Ctrl Pts',(-5.05347182127219,-2.10578908733594,
13.3076639553341));
#58244=CARTESIAN_POINT('Ctrl Pts',(-3.4266053526834,-4.26969564321588,13.446837412756));
#58245=CARTESIAN_POINT('Ctrl Pts',(-0.961813786651197,-5.38951197869926,
13.586010870178));
#58246=CARTESIAN_POINT('Ctrl Pts',(1.73817495791542,-5.19140375470941,13.7251843276));
#58247=CARTESIAN_POINT('Ctrl Pts',(4.01311900924231,-3.72381537490692,13.8643577850219));
#58248=CARTESIAN_POINT('Ctrl Pts',(5.30671481915647,-1.34562363121355,14.0035312424439));
#58249=CARTESIAN_POINT('Ctrl Pts',(5.30263287681247,1.36162024899849,14.1427046998658));
#58250=CARTESIAN_POINT('Ctrl Pts',(4.00187136016905,3.73590025902645,14.2818781572877));
#58251=CARTESIAN_POINT('Ctrl Pts',(1.7225120464961,5.19662172746978,14.4210516147097));
#58252=CARTESIAN_POINT('Ctrl Pts',(-0.97806182965262,5.38658706289165,14.5602250721317));
#58253=CARTESIAN_POINT('Ctrl Pts',(-3.43946531132461,4.25934308326177,14.6993985295536));
#58254=CARTESIAN_POINT('Ctrl Pts',(-5.05979898497569,2.09054044695961,14.8385719869756));
#58255=CARTESIAN_POINT('Ctrl Pts',(-5.44283448123103,-0.589472593644336,
14.9777454443975));
#58256=CARTESIAN_POINT('Ctrl Pts',(-4.49490619740522,-3.12533892646274,
15.1169189018195));
#58257=CARTESIAN_POINT('Ctrl Pts',(-2.44781581996098,-4.89695036122319,
15.2560923592414));
#58258=CARTESIAN_POINT('Ctrl Pts',(0.197851311546307,-5.47108581428354,
15.3952658166634));
#58259=CARTESIAN_POINT('Ctrl Pts',(2.79513686348917,-4.70734904623601,15.5344392740853));
#58260=CARTESIAN_POINT('Ctrl Pts',(4.70891349402307,-2.79250046276497,15.6736127315073));
#58261=CARTESIAN_POINT('Ctrl Pts',(5.47119574682194,-0.194787650257265,
15.8127861889292));
#58262=CARTESIAN_POINT('Ctrl Pts',(4.89557889615458,2.45055756926072,15.9519596463512));
#58263=CARTESIAN_POINT('Ctrl Pts',(3.12282143506075,4.49665558092459,16.0911331037731));
#58264=CARTESIAN_POINT('Ctrl Pts',(0.586424690784659,5.44316371339071,16.2303065611951));
#58265=CARTESIAN_POINT('Ctrl Pts',(-2.09337344221106,5.05862755697437,16.369480018617));
#58266=CARTESIAN_POINT('Ctrl Pts',(-4.26126840428094,3.43707967836246,16.508653476039));
#58267=CARTESIAN_POINT('Ctrl Pts',(-5.38713390121461,0.975045362595692,
16.6478269334609));
#58268=CARTESIAN_POINT('Ctrl Pts',(-5.19565636196209,-1.72542171573735,
16.7870003908829));
#58269=CARTESIAN_POINT('Ctrl Pts',(-3.73365875538693,-4.00396271549296,
16.9261738483048));
#58270=CARTESIAN_POINT('Ctrl Pts',(-1.35865073342267,-5.30339450854876,
17.0653473057268));
#58271=CARTESIAN_POINT('Ctrl Pts',(1.34859500809782,-5.30596048165352,17.2045207631488));
#58272=CARTESIAN_POINT('Ctrl Pts',(3.72606200731666,-4.01103316445607,17.3436942205707));
#58273=CARTESIAN_POINT('Ctrl Pts',(5.192376262285,-1.7352676679966,17.4828676779927));
#58274=CARTESIAN_POINT('Ctrl Pts',(5.38897254925603,0.964831587428646,17.6220411354146));
#58275=CARTESIAN_POINT('Ctrl Pts',(4.26777618615752,3.42899570626765,17.7612145928366));
#58276=CARTESIAN_POINT('Ctrl Pts',(2.10295897718242,5.05465020243964,17.9003880502585));
#58277=CARTESIAN_POINT('Ctrl Pts',(-0.576105401953414,5.44426557899,18.0395615076805));
#58278=CARTESIAN_POINT('Ctrl Pts',(-3.11429182013832,4.50256722190293,18.1787349651024));
#58279=CARTESIAN_POINT('Ctrl Pts',(-4.89092474491816,2.4598333822197,18.3179084225244));
#58280=CARTESIAN_POINT('Ctrl Pts',(-5.47155516235805,-0.184415926665981,
18.4570818799463));
#58281=CARTESIAN_POINT('Ctrl Pts',(-4.7141985866371,-2.78356907844658,18.5962553373683));
#58282=CARTESIAN_POINT('Ctrl Pts',(-2.80405524281576,-4.7020420376654,18.7354287947902));
#58283=CARTESIAN_POINT('Ctrl Pts',(-0.208222121286857,-5.47070093104549,
18.8746022522122));
#58284=CARTESIAN_POINT('Ctrl Pts',(2.43852860624314,-4.90158172075801,19.0137757096341));
#58285=CARTESIAN_POINT('Ctrl Pts',(4.48897362894353,-3.13385399905368,19.1529491670561));
#58286=CARTESIAN_POINT('Ctrl Pts',(5.44170727892698,-0.599789145623911,
19.2921226244781));
#58287=CARTESIAN_POINT('Ctrl Pts',(5.06375278929654,2.08094517410398,19.4312960819));
#58288=CARTESIAN_POINT('Ctrl Pts',(3.44753327854899,4.25281547001894,19.5704695393219));
#58289=CARTESIAN_POINT('Ctrl Pts',(0.988271059044424,5.38472333946605,19.7096429967439));
#58290=CARTESIAN_POINT('Ctrl Pts',(-1.71265806931551,5.19987763955496,19.8488164541658));
#58291=CARTESIAN_POINT('Ctrl Pts',(-3.99478227796254,3.74347962201099,19.9879899115878));
#58292=CARTESIAN_POINT('Ctrl Pts',(-5.3000422186233,1.37166964300655,20.1271633690097));
#58293=CARTESIAN_POINT('Ctrl Pts',(-5.30925609170404,-1.33556163520771,
20.2663368264317));
#58294=CARTESIAN_POINT('Ctrl Pts',(-4.02017078232737,-3.71620128755917,
20.4055102838536));
#58295=CARTESIAN_POINT('Ctrl Pts',(-1.74801282588246,-5.18809948721934,
20.5446837412756));
#58296=CARTESIAN_POINT('Ctrl Pts',(0.951595527297795,-5.39132554026949,
20.6838571986976));
#58297=CARTESIAN_POINT('Ctrl Pts',(3.41850542446435,-4.27618355448442,20.8230306561195));
#58298=CARTESIAN_POINT('Ctrl Pts',(5.0494709405069,-2.11536482662247,20.9622041135415));
#58299=CARTESIAN_POINT('Ctrl Pts',(5.44566384798265,0.562734736363337,21.1013775709634));
#58300=CARTESIAN_POINT('Ctrl Pts',(4.5102010960486,3.10322593472296,21.2405510283854));
#58301=CARTESIAN_POINT('Ctrl Pts',(2.47183611175321,4.88486963647629,21.3797244858073));
#58302=CARTESIAN_POINT('Ctrl Pts',(-0.170979429762869,5.47199151711085,
21.5188979432293));
#58303=CARTESIAN_POINT('Ctrl Pts',(-2.77198450856176,4.72101970055504,21.6580714006512));
#58304=CARTESIAN_POINT('Ctrl Pts',(-4.69514222812823,2.81559311449334,21.7972448580732));
#58305=CARTESIAN_POINT('Ctrl Pts',(-5.47017312709831,0.221655336742991,
21.9364183154951));
#58306=CARTESIAN_POINT('Ctrl Pts',(-4.90755498896332,-2.42648493896755,
22.0755917729171));
#58307=CARTESIAN_POINT('Ctrl Pts',(-3.14486766599629,-4.48126460857939,
22.214765230339));
#58308=CARTESIAN_POINT('Ctrl Pts',(-0.613149983751713,-5.44021803112342,
22.353938687761));
#58309=CARTESIAN_POINT('Ctrl Pts',(2.0685043579568,-5.06884748733368,22.4931121451829));
#58310=CARTESIAN_POINT('Ctrl Pts',(4.24433689140084,-3.45796609020809,22.6322856026049));
#58311=CARTESIAN_POINT('Ctrl Pts',(5.38228030798918,-1.00149079624683,22.7714590600268));
#58312=CARTESIAN_POINT('Ctrl Pts',(5.20406756203382,1.69988409561432,22.9106325174488));
#58313=CARTESIAN_POINT('Ctrl Pts',(3.75327791555961,3.98557775200882,23.0498059748707));
#58314=CARTESIAN_POINT('Ctrl Pts',(1.38468028146157,5.29665796959428,23.1889794322927));
#58315=CARTESIAN_POINT('Ctrl Pts',(-1.322520208919,5.31251968709162,23.3281528897146));
#58316=CARTESIAN_POINT('Ctrl Pts',(-3.70631815921382,4.02928415868341,23.4673263471366));
#58317=CARTESIAN_POINT('Ctrl Pts',(-5.1837914280616,1.76074744330078,23.6064998045585));
#58318=CARTESIAN_POINT('Ctrl Pts',(-5.39364602174355,-0.938353729072977,
23.7456732619805));
#58319=CARTESIAN_POINT('Ctrl Pts',(-4.28456513754638,-3.40799452917068,
23.8848467194025));
#58320=CARTESIAN_POINT('Ctrl Pts',(-2.12775792047298,-5.04426123040824,
24.0240201768244));
#58321=CARTESIAN_POINT('Ctrl Pts',(0.549360677498777,-5.44702927977749,
24.1631936342464));
#58322=CARTESIAN_POINT('Ctrl Pts',(3.09214133694363,-4.51780777381018,24.3023670916683));
#58323=CARTESIAN_POINT('Ctrl Pts',(4.87878507240969,-2.4838239361854,24.4415405490903));
#58324=CARTESIAN_POINT('Ctrl Pts',(5.47239487591072,0.157541901858669,24.5807140065122));
#58325=CARTESIAN_POINT('Ctrl Pts',(4.7278123468587,2.76038322368935,24.7198874639342));
#58326=CARTESIAN_POINT('Ctrl Pts',(2.82711400822466,4.6882141070172,24.8590609213561));
#58327=CARTESIAN_POINT('Ctrl Pts',(0.235087215623762,5.46961233816304,24.9982343787781));
#58328=CARTESIAN_POINT('Ctrl Pts',(-2.41442664005693,4.91349866475189,25.1374078362));
#58329=CARTESIAN_POINT('Ctrl Pts',(-4.47352856631735,3.15586236947649,25.276581293622));
#58330=CARTESIAN_POINT('Ctrl Pts',(-5.43869597896016,0.626507124602579,
25.4157547510439));
#58331=CARTESIAN_POINT('Ctrl Pts',(-5.07391162036489,-2.05605106878728,
25.5549282084659));
#58332=CARTESIAN_POINT('Ctrl Pts',(-3.4683780504302,-4.23583271955223,25.6941016658878));
#58333=CARTESIAN_POINT('Ctrl Pts',(-1.01470449448827,-5.37980482151541,
25.8332751233098));
#58334=CARTESIAN_POINT('Ctrl Pts',(1.68709987166048,-5.20822610413357,25.9724485807317));
#58335=CARTESIAN_POINT('Ctrl Pts',(3.97634919313482,-3.76305357694934,26.1116220381537));
#58336=CARTESIAN_POINT('Ctrl Pts',(5.29324178186864,-1.39768257033394,26.2507954955757));
#58337=CARTESIAN_POINT('Ctrl Pts',(5.31575124813685,1.30947080787112,26.3899689529976));
#58338=CARTESIAN_POINT('Ctrl Pts',(4.03837323857078,3.69641268187557,26.5291424104196));
#58339=CARTESIAN_POINT('Ctrl Pts',(1.77347144346219,5.17945211078925,26.6683158678415));
#58340=CARTESIAN_POINT('Ctrl Pts',(-0.925106272601936,5.3959339796858,26.8074893252635));
#58341=CARTESIAN_POINT('Ctrl Pts',(-3.39746308376715,4.29292088480261,26.9466627826854));
#58342=CARTESIAN_POINT('Ctrl Pts',(-5.03902110355814,2.14013818400377,27.0858362401074));
#58343=CARTESIAN_POINT('Ctrl Pts',(-5.44836186614097,-0.535983306005068,
27.2250096975293));
#58344=CARTESIAN_POINT('Ctrl Pts',(-4.52538720931959,-3.08103809364017,
27.3641831549512));
#58345=CARTESIAN_POINT('Ctrl Pts',(-2.49579678323004,-4.87267108940813,
27.5033566123732));
#58346=CARTESIAN_POINT('Ctrl Pts',(0.144103423981289,-5.47276523632542,
27.6425300697952));
#58347=CARTESIAN_POINT('Ctrl Pts',(2.74876529378475,-4.73457648458863,27.7817035272171));
#58348=CARTESIAN_POINT('Ctrl Pts',(4.68125771610869,-2.83861785453907,27.9208769846391));
#58349=CARTESIAN_POINT('Ctrl Pts',(5.46901856762123,-0.248517676935322,
28.060050442061));
#58350=CARTESIAN_POINT('Ctrl Pts',(4.91941271228352,2.40235378222246,28.199223899483));
#58351=CARTESIAN_POINT('Ctrl Pts',(3.16683804319653,4.46576554880552,28.3383973569049));
#58352=CARTESIAN_POINT('Ctrl Pts',(0.639860487633334,5.43714113161511,28.4775708143269));
#58353=CARTESIAN_POINT('Ctrl Pts',(-2.04358538168839,5.07894515785361,28.6167442717489));
#58354=CARTESIAN_POINT('Ctrl Pts',(-4.227303005753,3.4787690964315,28.7559177291708));
#58355=CARTESIAN_POINT('Ctrl Pts',(-5.37729689497187,1.02791207409051,28.8950911865928));
#58356=CARTESIAN_POINT('Ctrl Pts',(-5.21235324077832,-1.67430547454247,
29.0342646440147));
#58357=CARTESIAN_POINT('Ctrl Pts',(-3.77280654723323,-3.96709665698849,
29.1734381014367));
#58358=CARTESIAN_POINT('Ctrl Pts',(-1.41067643122025,-5.28979367604586,
29.3126115588586));
#58359=CARTESIAN_POINT('Ctrl Pts',(1.29641351075158,-5.31895075535353,29.4517850162806));
#58360=CARTESIAN_POINT('Ctrl Pts',(3.68648491527416,-4.04743796718259,29.5909584737025));
#58361=CARTESIAN_POINT('Ctrl Pts',(5.17508156156827,-1.78618474964133,29.7301319311244));
#58362=CARTESIAN_POINT('Ctrl Pts',(5.39818940029989,0.911853237766431,29.8693053885464));
#58363=CARTESIAN_POINT('Ctrl Pts',(4.30125074586824,3.38691115175804,30.0084788459683));
#58364=CARTESIAN_POINT('Ctrl Pts',(2.15250554256233,5.03375059155434,30.1476523033903));
#58365=CARTESIAN_POINT('Ctrl Pts',(-0.522602702547216,5.44966159903764,
30.2868257608122));
#58366=CARTESIAN_POINT('Ctrl Pts',(-3.06991627176472,4.53293935687313,30.4259992182342));
#58367=CARTESIAN_POINT('Ctrl Pts',(-4.86652772433872,2.50775458069123,30.5651726756561));
#58368=CARTESIAN_POINT('Ctrl Pts',(-5.47310259612169,-0.130664077164341,
30.7043461330782));
#58369=CARTESIAN_POINT('Ctrl Pts',(-4.74131207295726,-2.73713078890376,
30.8435195905001));
#58370=CARTESIAN_POINT('Ctrl Pts',(-2.85010458406871,-4.67427309734954,
30.982693047922));
#58371=CARTESIAN_POINT('Ctrl Pts',(-0.261946639692367,-5.4683918190533,
31.121866505344));
#58372=CARTESIAN_POINT('Ctrl Pts',(2.39026643826314,-4.92529709589665,31.2610399627659));
#58373=CARTESIAN_POINT('Ctrl Pts',(4.45797560285469,-3.17779462097341,31.4002134201879));
#58374=CARTESIAN_POINT('Ctrl Pts',(5.43555349846396,-0.653209992323582,
31.5393868776099));
#58375=CARTESIAN_POINT('Ctrl Pts',(5.08394806944776,2.03110737182789,31.6785603350317));
#58376=CARTESIAN_POINT('Ctrl Pts',(3.48913916555426,4.21874780143712,31.8177337924538));
#58377=CARTESIAN_POINT('Ctrl Pts',(1.04111345541225,5.37475654348126,31.9569072498757));
#58378=CARTESIAN_POINT('Ctrl Pts',(-1.66150098141019,5.21644894708155,32.0960807072976));
#58379=CARTESIAN_POINT('Ctrl Pts',(-3.95782019936239,3.78253676760111,32.2352541647196));
#58380=CARTESIAN_POINT('Ctrl Pts',(-5.28631367291798,1.42366178576779,32.3744276221416));
#58381=CARTESIAN_POINT('Ctrl Pts',(-5.3221181894487,-1.28334839629558,32.5136010795635));
#58382=CARTESIAN_POINT('Ctrl Pts',(-4.05647828985874,-3.67653491927384,
32.6527745369854));
#58383=CARTESIAN_POINT('Ctrl Pts',(-1.79888728517725,-5.17067980675295,
32.7919479944074));
#58384=CARTESIAN_POINT('Ctrl Pts',(0.898594704481963,-5.4004122699857,32.9311214518293));
#58385=CARTESIAN_POINT('Ctrl Pts',(3.37633879677125,-4.30955467051439,33.0702949092513));
#58386=CARTESIAN_POINT('Ctrl Pts',(5.02844972617794,-2.16485992157371,33.2094683666733));
#58387=CARTESIAN_POINT('Ctrl Pts',(5.45092847063015,0.509218947810083,33.3486418240952));
#58388=CARTESIAN_POINT('Ctrl Pts',(4.54046417093141,3.05877593838176,33.4878152815172));
#58389=CARTESIAN_POINT('Ctrl Pts',(2.51969725646367,4.86035501424583,33.6269887389391));
#58390=CARTESIAN_POINT('Ctrl Pts',(-0.117223942446786,5.47340695326525,
33.766162196361));
#58391=CARTESIAN_POINT('Ctrl Pts',(-2.7254797792021,4.7480190713492,33.9053356537831));
#58392=CARTESIAN_POINT('Ctrl Pts',(-4.66726029285681,2.86157412754891,34.0445091112049));
#58393=CARTESIAN_POINT('Ctrl Pts',(-5.46773209623851,0.275374022918645,
34.183682568627));
#58394=CARTESIAN_POINT('Ctrl Pts',(-4.93115178010865,-2.3781646810653,34.3228560260488));
#58395=CARTESIAN_POINT('Ctrl Pts',(-3.18873203673927,-4.450158775438,34.4620294834708));
#58396=CARTESIAN_POINT('Ctrl Pts',(-0.666555558176188,-5.4339330890801,
34.6012029408928));
#58397=CARTESIAN_POINT('Ctrl Pts',(2.01861711444781,-5.0889203249799,34.7403763983148));
#58398=CARTESIAN_POINT('Ctrl Pts',(4.21016715819219,-3.49948819526728,34.8795498557366));
#58399=CARTESIAN_POINT('Ctrl Pts',(5.37218378236186,-1.05430855884951,35.0187233131587));
#58400=CARTESIAN_POINT('Ctrl Pts',(5.22051319834627,1.64868646947428,35.1578967705805));
#58401=CARTESIAN_POINT('Ctrl Pts',(3.79224417938013,3.94851987619319,35.2970702280026));
#58402=CARTESIAN_POINT('Ctrl Pts',(1.43663855567549,5.28280179346924,35.4362436854244));
#58403=CARTESIAN_POINT('Ctrl Pts',(-1.27027554328518,5.32525353132287,35.5754171428465));
#58404=CARTESIAN_POINT('Ctrl Pts',(-3.66656275387258,4.06549415208649,35.7145906002684));
#58405=CARTESIAN_POINT('Ctrl Pts',(-5.16624687288569,1.81157897347425,35.8537640576904));
#58406=CARTESIAN_POINT('Ctrl Pts',(-5.40260257533944,-0.885330752696877,
35.9929375151123));
#58407=CARTESIAN_POINT('Ctrl Pts',(-4.31783260866877,-3.3657460825576,36.1321109725343));
#58408=CARTESIAN_POINT('Ctrl Pts',(-2.17720124654159,-5.02311853939292,
36.2712844299562));
#58409=CARTESIAN_POINT('Ctrl Pts',(0.495832122497053,-5.45216247327932,
36.4104578873782));
#58410=CARTESIAN_POINT('Ctrl Pts',(3.04761716066692,-4.54796160612022,36.5496313448001));
#58411=CARTESIAN_POINT('Ctrl Pts',(4.85415299635065,-2.53162473853356,36.6888048022221));
#58412=CARTESIAN_POINT('Ctrl Pts',(5.47367830592085,0.103783100872094,36.827978259644));
#58413=CARTESIAN_POINT('Ctrl Pts',(4.75469743932145,2.71381233493496,36.967151717066));
#58414=CARTESIAN_POINT('Ctrl Pts',(2.87302641581874,4.66021934491746,37.1063251744879));
#58415=CARTESIAN_POINT('Ctrl Pts',(0.288799745647482,5.46703940315497,37.2454986319099));
#58416=CARTESIAN_POINT('Ctrl Pts',(-2.36604858360213,4.93697672961596,37.3846720893318));
#58417=CARTESIAN_POINT('Ctrl Pts',(-4.44231511369065,3.19965022454186,37.5238455467538));
#58418=CARTESIAN_POINT('Ctrl Pts',(-5.43227991323453,0.679897104717855,
37.6630190041757));
#58419=CARTESIAN_POINT('Ctrl Pts',(-5.09386189446753,-2.00611468486398,
37.8021924615977));
#58420=CARTESIAN_POINT('Ctrl Pts',(-3.50981612316625,-4.20156112775922,
37.9413659190196));
#58421=CARTESIAN_POINT('Ctrl Pts',(-1.06749730483629,-5.36957862712731,
38.0805393764416));
#58422=CARTESIAN_POINT('Ctrl Pts',(1.6358620160059,-5.22454597006517,38.2197128338635));
#58423=CARTESIAN_POINT('Ctrl Pts',(3.93919574356163,-3.80192872403483,38.3588862912855));
#58424=CARTESIAN_POINT('Ctrl Pts',(5.27925805887621,-1.44960666269362,38.4980597487074));
#58425=CARTESIAN_POINT('Ctrl Pts',(5.32835676206999,1.25719503054944,38.6372332061295));
#58426=CARTESIAN_POINT('Ctrl Pts',(4.07448549950035,3.6565684792024,38.7764066635512));
#58427=CARTESIAN_POINT('Ctrl Pts',(1.82425973800165,5.16178278669699,38.9155801209734));
#58428=CARTESIAN_POINT('Ctrl Pts',(-0.872061462392577,5.40476030315358,
39.0547535783952));
#58429=CARTESIAN_POINT('Ctrl Pts',(-3.35513307299098,4.32608451041554,39.1939270358173));
#58430=CARTESIAN_POINT('Ctrl Pts',(-5.01775706334624,2.18952944304799,39.3331004932391));
#58431=CARTESIAN_POINT('Ctrl Pts',(-5.45336359954413,-0.482442307330456,
39.4722739506611));
#58432=CARTESIAN_POINT('Ctrl Pts',(-4.55543161723014,-3.03644000590743,
39.611447408083));
#58433=CARTESIAN_POINT('Ctrl Pts',(-2.54353695497842,-4.84792170805123,
39.750620865505));
#58434=CARTESIAN_POINT('Ctrl Pts',(0.0903416334882624,-5.47391665245223,
39.8897943229269));
#58435=CARTESIAN_POINT('Ctrl Pts',(2.70212852645677,-4.76134713660365,40.028967780349));
#58436=CARTESIAN_POINT('Ctrl Pts',(4.65315029598825,-2.88446137982113,40.1681412377708));
#58437=CARTESIAN_POINT('Ctrl Pts',(5.46631374397962,-0.302223726922086,
40.3073146951928));
#58438=CARTESIAN_POINT('Ctrl Pts',(4.94277190929426,2.35391821893342,40.4464881526148));
#58439=CARTESIAN_POINT('Ctrl Pts',(3.21054911854478,4.43444466490975,40.5856616100367));
#58440=CARTESIAN_POINT('Ctrl Pts',(0.693234551499346,5.43059398089589,40.7248350674587));
#58441=CARTESIAN_POINT('Ctrl Pts',(-1.99360015846576,5.09877274811306,40.8640085248806));
#58442=CARTESIAN_POINT('Ctrl Pts',(-4.19292976203238,3.52012288697402,41.0031819823026));
#58443=CARTESIAN_POINT('Ctrl Pts',(-5.36694109348664,1.08067961384472,41.1423554397246));
#58444=CARTESIAN_POINT('Ctrl Pts',(-5.22854723792075,-1.62302769833616,
41.2815288971464));
#58445=CARTESIAN_POINT('Ctrl Pts',(-3.81159034316765,-3.92984785769199,
41.4207023545685));
#58446=CARTESIAN_POINT('Ctrl Pts',(-1.46256602862488,-5.27568249050751,
41.5598758119903));
#58447=CARTESIAN_POINT('Ctrl Pts',(1.24410693696348,-5.33142786297766,41.6990492694124));
#58448=CARTESIAN_POINT('Ctrl Pts',(3.64655215552852,-4.08345227788271,41.8382227268343));
#58449=CARTESIAN_POINT('Ctrl Pts',(5.15728757510524,-1.83692950229468,41.9773961842562));
#58450=CARTESIAN_POINT('Ctrl Pts',(5.40688544041709,0.858786913582771,42.1165696416783));
#58451=CARTESIAN_POINT('Ctrl Pts',(4.3343103259958,3.34449983206777,42.2557430991001));
#58452=CARTESIAN_POINT('Ctrl Pts',(2.20184443675396,5.01236533036757,42.3949165565222));
#58453=CARTESIAN_POINT('Ctrl Pts',(-0.469049583050801,5.45453184218179,
42.534090013944));
#58454=CARTESIAN_POINT('Ctrl Pts',(-3.02524454150149,4.56287415921704,42.673263471366));
#58455=CARTESIAN_POINT('Ctrl Pts',(-4.84166118692218,2.55543383396763,42.812436928788));
#58456=CARTESIAN_POINT('Ctrl Pts',(-5.47412199142217,-0.0768996213472616,
42.9516103862099));
#58457=CARTESIAN_POINT('Ctrl Pts',(-4.76796812309811,-2.69042842422083,
43.0907838436319));
#58458=CARTESIAN_POINT('Ctrl Pts',(-2.89587895060334,-4.64605318869551,
43.2299573010538));
#58459=CARTESIAN_POINT('Ctrl Pts',(-0.315645885795919,-5.46555512308816,
43.3691307584758));
#58460=CARTESIAN_POINT('Ctrl Pts',(2.34177366020521,-4.94853728419866,43.5083042158978));
#58461=CARTESIAN_POINT('Ctrl Pts',(4.42654747655404,-3.22142865302774,43.6474776733197));
#58462=CARTESIAN_POINT('Ctrl Pts',(5.42887530223032,-0.706567818095944,
43.7866511307416));
#58463=CARTESIAN_POINT('Ctrl Pts',(5.10365285630411,1.98107361071568,43.9258245881636));
#58464=CARTESIAN_POINT('Ctrl Pts',(3.53040842454084,4.18427311305873,44.0649980455855));
#58465=CARTESIAN_POINT('Ctrl Pts',(1.09385540638558,5.36427119734416,44.2041715030075));
#58466=CARTESIAN_POINT('Ctrl Pts',(-1.61018359385595,5.23251697778539,44.3433449604294));
#58467=CARTESIAN_POINT('Ctrl Pts',(-3.92047627495196,3.82122897851909,44.4825184178514));
#58468=CARTESIAN_POINT('Ctrl Pts',(-5.2720751099238,1.47551657532438,44.6216918752733));
#58469=CARTESIAN_POINT('Ctrl Pts',(-5.33446681552716,-1.23101134144846,
44.7608653326954));
#58470=CARTESIAN_POINT('Ctrl Pts',(-4.09239443316404,-3.6365138432492,44.9000387901172));
#58471=CARTESIAN_POINT('Ctrl Pts',(-1.84958818995514,-5.15276126521632,
45.0392122475392));
#58472=CARTESIAN_POINT('Ctrl Pts',(0.845507186312134,-5.40897797431545,
45.1783857049612));
#58473=CARTESIAN_POINT('Ctrl Pts',(3.33384642390563,-4.34251000580848,45.3175591623831));
#58474=CARTESIAN_POINT('Ctrl Pts',(5.00694337296865,-2.214146153401,45.4567326198051));
#58475=CARTESIAN_POINT('Ctrl Pts',(5.45566719414789,0.455654030415216,45.595906077227));
#58476=CARTESIAN_POINT('Ctrl Pts',(4.57028918720294,3.01403083495691,45.735079534649));
#58477=CARTESIAN_POINT('Ctrl Pts',(2.56731530376392,4.83537147071399,45.874252992071));
#58478=CARTESIAN_POINT('Ctrl Pts',(-0.0634571455034273,5.47429432159248,
46.0134264494928));
#58479=CARTESIAN_POINT('Ctrl Pts',(-2.67871209877789,4.77456035888081,46.1525999069149));
#58480=CARTESIAN_POINT('Ctrl Pts',(-4.63892806583425,2.90727905931825,46.2917733643367));
#58481=CARTESIAN_POINT('Ctrl Pts',(-5.46476354505504,0.329066141334365,
46.4309468217588));
#58482=CARTESIAN_POINT('Ctrl Pts',(-4.95427281956437,-2.32961498064827,
46.5701202791806));
#58483=CARTESIAN_POINT('Ctrl Pts',(-3.23228876238798,-4.41862359624302,
46.7092937366026));
#58484=CARTESIAN_POINT('Ctrl Pts',(-0.719896824109031,-5.42712388760133,
46.8484671940246));
#58485=CARTESIAN_POINT('Ctrl Pts',(1.96853511714788,-5.10850218961397,46.9876406514465));
#58486=CARTESIAN_POINT('Ctrl Pts',(4.17559123303725,-3.5406726738457,47.1268141088685));
#58487=CARTESIAN_POINT('Ctrl Pts',(5.36156895479916,-1.10702460300981,47.2659875662904));
#58488=CARTESIAN_POINT('Ctrl Pts',(5.23645516572182,1.59732978001426,47.4051610237123));
#58489=CARTESIAN_POINT('Ctrl Pts',(3.8308445719689,3.91108105185148,47.5443344811344));
#58490=CARTESIAN_POINT('Ctrl Pts',(1.48845822470126,5.26843593887734,47.6835079385562));
#58491=CARTESIAN_POINT('Ctrl Pts',(-1.21790832296982,5.33747360139383,47.8226813959783));
#58492=CARTESIAN_POINT('Ctrl Pts',(-3.62645360289483,4.10131191142374,47.9618548534001));
#58493=CARTESIAN_POINT('Ctrl Pts',(-5.14820388432376,1.86223572465166,48.1010283108222));
#58494=CARTESIAN_POINT('Ctrl Pts',(-5.41103789223077,-0.832222360657202,
48.240201768244));
#58495=CARTESIAN_POINT('Ctrl Pts',(-4.35068350040957,-3.32317291274456,
48.3793752256661));
#58496=CARTESIAN_POINT('Ctrl Pts',(-2.22643451880982,-5.00149122384386,
48.5185486830879));
#58497=CARTESIAN_POINT('Ctrl Pts',(0.442255730198809,-5.45676964859627,
48.65772214051));
#58498=CARTESIAN_POINT('Ctrl Pts',(3.00279895389227,-4.57767665647527,48.7968955979318));
#58499=CARTESIAN_POINT('Ctrl Pts',(4.82905259735361,-2.57918129272208,48.936069055354));
#58500=CARTESIAN_POINT('Ctrl Pts',(5.47443364192402,0.0500142870148103,
49.0752425127757));
#58501=CARTESIAN_POINT('Ctrl Pts',(4.7811238042006,2.66697962077732,49.2144159701978));
#58502=CARTESIAN_POINT('Ctrl Pts',(2.91866163722327,4.63177497036894,49.3535894276197));
#58503=CARTESIAN_POINT('Ctrl Pts',(0.342484412613354,5.46393901465346,49.4927628850417));
#58504=CARTESIAN_POINT('Ctrl Pts',(-2.31744225357938,4.95997848080615,49.6319363424636));
#58505=CARTESIAN_POINT('Ctrl Pts',(-4.4106730717576,3.24312938113907,49.7711097998856));
#58506=CARTESIAN_POINT('Ctrl Pts',(-5.42533974756993,0.733221489164787,
49.9102832573075));
#58507=CARTESIAN_POINT('Ctrl Pts',(-5.11332071880119,-1.95598475336943,
50.0494567147295));
#58508=CARTESIAN_POINT('Ctrl Pts',(-3.55091557299522,-4.1668841743196,50.1886301721514));
#58509=CARTESIAN_POINT('Ctrl Pts',(-1.12018712430723,-5.35883438214613,
50.3278036295734));
#58510=CARTESIAN_POINT('Ctrl Pts',(1.5844663343195,-5.24036177798281,50.4669770869953));
#58511=CARTESIAN_POINT('Ctrl Pts',(3.9016622450437,-3.84043706553509,50.6061505444173));
#58512=CARTESIAN_POINT('Ctrl Pts',(5.26476499931227,-1.50139089871746,50.7453240018392));
#58513=CARTESIAN_POINT('Ctrl Pts',(5.34044820244678,1.20479796053868,50.8844974592612));
#58514=CARTESIAN_POINT('Ctrl Pts',(4.11020465888946,3.61637149512858,51.0236709166831));
#58515=CARTESIAN_POINT('Ctrl Pts',(1.87487203011983,5.14361545990847,51.1628443741051));
#58516=CARTESIAN_POINT('Ctrl Pts',(-0.818932516725154,5.4130651817418,51.3020178315271));
#58517=CARTESIAN_POINT('Ctrl Pts',(-3.3124793629455,4.35883076051311,51.4411912889489));
#58518=CARTESIAN_POINT('Ctrl Pts',(-4.99600891586951,2.23870945888194,51.580364746371));
#58519=CARTESIAN_POINT('Ctrl Pts',(-5.45783919887916,-0.428854763192953,
51.7195382037929));
#58520=CARTESIAN_POINT('Ctrl Pts',(-4.58503652248779,-2.99154896603551,
51.8587116612149));
#58521=CARTESIAN_POINT('Ctrl Pts',(-2.59103172929054,-4.82270460494367,
51.9978851186368));
#58522=CARTESIAN_POINT('Ctrl Pts',(0.0365711269414716,-5.47453995157669,
52.1370585760588));
#58523=CARTESIAN_POINT('Ctrl Pts',(2.65523106096563,-4.78765841948008,52.2762320334807));
#58524=CARTESIAN_POINT('Ctrl Pts',(4.62459394543255,-2.93002661568179,52.4154054909026));
#58525=CARTESIAN_POINT('Ctrl Pts',(5.46308153685529,-0.355900618721091,
52.5545789483246));
#58526=CARTESIAN_POINT('Ctrl Pts',(4.96565423351902,2.30525555239972,52.6937524057466));
#58527=CARTESIAN_POINT('Ctrl Pts',(3.25395044391241,4.40269595103925,52.8329258631685));
#58528=CARTESIAN_POINT('Ctrl Pts',(0.746541732915853,5.42352289289444,52.9720993205905));
#58529=CARTESIAN_POINT('Ctrl Pts',(-1.94342259505864,5.11810841481017,53.1112727780124));
#58530=CARTESIAN_POINT('Ctrl Pts',(-4.15815198940913,3.56113706022502,53.2504462354344));
#58531=CARTESIAN_POINT('Ctrl Pts',(-5.35606749587446,1.13334289090821,53.3896196928563));
#58532=CARTESIAN_POINT('Ctrl Pts',(-5.24423679101162,-1.5715933343379,53.5287931502783));
#58533=CARTESIAN_POINT('Ctrl Pts',(-3.85000640137521,-3.89221991132376,
53.6679666077002));
#58534=CARTESIAN_POINT('Ctrl Pts',(-1.51431451938932,-5.26106231336427,
53.8071400651222));
#58535=CARTESIAN_POINT('Ctrl Pts',(1.19168033321019,-5.34339060074923,53.9463135225442));
#58536=CARTESIAN_POINT('Ctrl Pts',(3.60626758074524,-4.11907262193822,54.085486979966));
#58537=CARTESIAN_POINT('Ctrl Pts',(5.13899601963854,-1.88749703016309,54.2246604373881));
#58538=CARTESIAN_POINT('Ctrl Pts',(5.41505983062401,0.805637734653367,54.36383389481));
#58539=CARTESIAN_POINT('Ctrl Pts',(4.36695173699138,3.30176583899027,54.5030073522319));
#58540=CARTESIAN_POINT('Ctrl Pts',(2.25097089959977,4.99049648210379,54.6421808096539));
#58541=CARTESIAN_POINT('Ctrl Pts',(-0.415451210205248,5.4588758385472,54.7813542670759));
#58542=CARTESIAN_POINT('Ctrl Pts',(-2.98028093922396,4.59236874086062,54.9205277244978));
#58543=CARTESIAN_POINT('Ctrl Pts',(-4.81632753176252,2.60286654201122,55.0597011819197));
#58544=CARTESIAN_POINT('Ctrl Pts',(-5.47461324990945,-0.0231277463455877,
55.1988746393417));
#58545=CARTESIAN_POINT('Ctrl Pts',(-4.79416416531556,-2.64346649018657,
55.3380480967637));
#58546=CARTESIAN_POINT('Ctrl Pts',(-2.94137392616304,-4.61738503432661,
55.4772215541856));
#58547=CARTESIAN_POINT('Ctrl Pts',(-0.369314678757935,-5.46219111683115,
55.6163950116077));
#58548=CARTESIAN_POINT('Ctrl Pts',(2.29305495059507,-4.97130004347822,55.7555684690294));
#58549=CARTESIAN_POINT('Ctrl Pts',(4.39469228218995,-3.26475188545704,55.8947419264516));
#58550=CARTESIAN_POINT('Ctrl Pts',(5.4216733345305,-0.759857475041239,56.0339153838733));
#58551=CARTESIAN_POINT('Ctrl Pts',(5.12286524877114,1.93084871796528,56.1730888412955));
#58552=CARTESIAN_POINT('Ctrl Pts',(3.57133707389957,4.14939473096083,56.3122622987172));
#58553=CARTESIAN_POINT('Ctrl Pts',(1.14649182348355,5.3532683126685,56.4514357561394));
#58554=CARTESIAN_POINT('Ctrl Pts',(-1.55871085769357,5.2480801814419,56.5906092135611));
#58555=CARTESIAN_POINT('Ctrl Pts',(-3.88275410762888,3.85955252178621,56.7297826709834));
#58556=CARTESIAN_POINT('Ctrl Pts',(-5.25732790336052,1.52722900878748,56.868956128405));
#58557=CARTESIAN_POINT('Ctrl Pts',(-5.34630077855855,-1.17855552008353,
57.0081295858272));
#58558=CARTESIAN_POINT('Ctrl Pts',(-4.12791574709623,-3.5961419206714,57.1473030432489));
#58559=CARTESIAN_POINT('Ctrl Pts',(-1.90011064865274,-5.13434559136913,
57.2864765006711));
#58560=CARTESIAN_POINT('Ctrl Pts',(0.792338094609303,-5.4170218268497,57.4256499580929));
#58561=CARTESIAN_POINT('Ctrl Pts',(3.29103240548137,-4.37504638087491,57.5648234155149));
#58562=CARTESIAN_POINT('Ctrl Pts',(4.98495395578654,-2.26321876702701,57.7039968729369));
#58563=CARTESIAN_POINT('Ctrl Pts',(5.45987956134944,0.402045152058584,57.8431703303588));
#58564=CARTESIAN_POINT('Ctrl Pts',(4.59967326738087,2.96899494140306,57.9823437877808));
#58565=CARTESIAN_POINT('Ctrl Pts',(2.6146856595211,4.80992141626346,58.1215172452027));
#58566=CARTESIAN_POINT('Ctrl Pts',(-0.00968422628974487,5.47465353648031,
58.2606907026247));
#58567=CARTESIAN_POINT('Ctrl Pts',(-2.63168597937963,4.80064100247788,58.3998641600466));
#58568=CARTESIAN_POINT('Ctrl Pts',(-4.61014828052031,2.95270350024359,58.5390376174686));
#58569=CARTESIAN_POINT('Ctrl Pts',(-5.46126775995019,0.382726511838092,
58.6782110748906));
#58570=CARTESIAN_POINT('Ctrl Pts',(-4.97691587663996,-2.28084052173411,
58.8173845323124));
#58571=CARTESIAN_POINT('Ctrl Pts',(-3.27553364064106,-4.38666211347123,
58.9565579897345));
#58572=CARTESIAN_POINT('Ctrl Pts',(-0.773168635248014,-5.41979108363079,
59.0957314471564));
#58573=CARTESIAN_POINT('Ctrl Pts',(1.91826319790888,-5.12759119200075,59.2349049045783));
#58574=CARTESIAN_POINT('Ctrl Pts',(4.14061245178034,-3.58151555251356,59.3740783620003));
#58575=CARTESIAN_POINT('Ctrl Pts',(5.35043684940709,-1.1596338427462,59.5132518194222));
#58576=CARTESIAN_POINT('Ctrl Pts',(5.25189192609828,1.54581898206696,59.6524252768443));
#58577=CARTESIAN_POINT('Ctrl Pts',(3.86907536920578,3.873264891037,59.7915987342661));
#58578=CARTESIAN_POINT('Ctrl Pts',(1.54013428903837,5.25356179181951,59.9307721916881));
#58579=CARTESIAN_POINT('Ctrl Pts',(-1.16542360030005,5.34917871832605,60.06994564911));
#58580=CARTESIAN_POINT('Ctrl Pts',(-3.58599457596465,4.13673398104114,60.209119106532));
#58581=CARTESIAN_POINT('Ctrl Pts',(-5.12966420314073,1.9127128095276,60.3482925639539));
#58582=CARTESIAN_POINT('Ctrl Pts',(-5.41895115859066,-0.779033676784864,
60.4874660213759));
#58583=CARTESIAN_POINT('Ctrl Pts',(-4.38311464334877,-3.28027912714825,
60.6266394787978));
#58584=CARTESIAN_POINT('Ctrl Pts',(-2.2754529873193,-4.97938137032394,60.7658129362198));
#58585=CARTESIAN_POINT('Ctrl Pts',(0.388636669609436,-5.46085036126269,
60.9049863936417));
#58586=CARTESIAN_POINT('Ctrl Pts',(2.95769104059119,-4.60695005794557,61.0441598510637));
#58587=CARTESIAN_POINT('Ctrl Pts',(4.8034862971456,-2.62648901066184,61.1833333084856));
#58588=CARTESIAN_POINT('Ctrl Pts',(5.47466081090924,-0.00375935194546259,
61.3225067659076));
#58589=CARTESIAN_POINT('Ctrl Pts',(4.8070888921791,2.6198895991595,61.4616802233296));
#58590=CARTESIAN_POINT('Ctrl Pts',(2.96401526908478,4.60288372847367,61.6008536807515));
#58591=CARTESIAN_POINT('Ctrl Pts',(0.396136038105091,5.46031147017638,61.7400271381735));
#58592=CARTESIAN_POINT('Ctrl Pts',(-2.26861234145274,4.98250170226862,61.8792005955954));
#58593=CARTESIAN_POINT('Ctrl Pts',(-4.37860548943786,3.28629563835069,62.0183740530173));
#58594=CARTESIAN_POINT('Ctrl Pts',(-5.4178761590868,0.786475145165815,62.1575475104394));
#58595=CARTESIAN_POINT('Ctrl Pts',(-5.13228620129426,-1.90566613397912,
62.2967209678612));
#58596=CARTESIAN_POINT('Ctrl Pts',(-3.59167246337271,-4.13180515958241,
62.4358944252833));
#58597=CARTESIAN_POINT('Ctrl Pts',(-1.17276881351499,-5.34757321139456,
62.5750678827051));
#58598=CARTESIAN_POINT('Ctrl Pts',(1.53291767611305,-5.25567182993055,62.7142413401272));
#58599=CARTESIAN_POINT('Ctrl Pts',(3.86375253149927,-3.87857522176944,62.853414797549));
#58600=CARTESIAN_POINT('Ctrl Pts',(5.24976358658708,-1.55302962792484,62.9925882549711));
#58601=CARTESIAN_POINT('Ctrl Pts',(5.35202521175614,1.15228337685149,63.131761712393));
#58602=CARTESIAN_POINT('Ctrl Pts',(4.14552569279038,3.57582809662026,63.2709351698149));
#58603=CARTESIAN_POINT('Ctrl Pts',(1.92530651381152,5.12494702954711,63.410108627237));
#58604=CARTESIAN_POINT('Ctrl Pts',(-0.765730562202499,5.42085727985497,
63.5492820846588));
#58605=CARTESIAN_POINT('Ctrl Pts',(-3.26949436548285,4.39113801409943,63.6884555420809));
#58606=CARTESIAN_POINT('Ctrl Pts',(-4.97380159054169,2.28770951087992,63.8276289995027));
#58607=CARTESIAN_POINT('Ctrl Pts',(-5.46174362790934,-0.375296313299901,
63.9668024569247));
#58608=CARTESIAN_POINT('Ctrl Pts',(-4.61428688809175,-2.94622961609203,
64.1059759143467));
#58609=CARTESIAN_POINT('Ctrl Pts',(-2.63809654804704,-4.79731827894146,
64.2451493717686));
#58610=CARTESIAN_POINT('Ctrl Pts',(-0.891129108788059,-5.24830906904511,
64.3379316767166));
#58611=CARTESIAN_POINT('Ctrl Pts',(-0.016500361394378,-5.25105740891156,
64.3843228291906));
#58612=CARTESIAN_POINT('Ctrl Pts',(2.85706463458441,-4.0032942355399,0.));
#58613=CARTESIAN_POINT('Ctrl Pts',(3.52386294776537,-3.52741468062806,0.046391152473984));
#58614=CARTESIAN_POINT('Ctrl Pts',(4.61438908619534,-2.23650256226449,0.139173457421952));
#58615=CARTESIAN_POINT('Ctrl Pts',(5.12163790500659,0.248365779535813,0.278346914843904));
#58616=CARTESIAN_POINT('Ctrl Pts',(4.37650875504895,2.67182739135543,0.417520372265856));
#58617=CARTESIAN_POINT('Ctrl Pts',(2.56115201646861,4.44226470421493,0.556693829687809));
#58618=CARTESIAN_POINT('Ctrl Pts',(0.119512633872891,5.12624413067081,0.695867287109761));
#58619=CARTESIAN_POINT('Ctrl Pts',(-2.35135624542669,4.55676348086115,0.835040744531713));
#58620=CARTESIAN_POINT('Ctrl Pts',(-4.24723382866677,2.87295023988583,0.974214201953666));
#58621=CARTESIAN_POINT('Ctrl Pts',(-5.10451506553093,0.486622655626781,
1.11338765937562));
#58622=CARTESIAN_POINT('Ctrl Pts',(-4.71356287464545,-2.01871284948783,
1.25256111679757));
#58623=CARTESIAN_POINT('Ctrl Pts',(-3.16997967797153,-4.03039635294118,
1.39173457421952));
#58624=CARTESIAN_POINT('Ctrl Pts',(-0.85122519685208,-5.05650975620884,
1.53090803164147));
#58625=CARTESIAN_POINT('Ctrl Pts',(1.67568359580848,-4.84612774610485,1.67008148906343));
#58626=CARTESIAN_POINT('Ctrl Pts',(3.79282906492235,-3.45069846869191,1.80925494648538));
#58627=CARTESIAN_POINT('Ctrl Pts',(4.98249488295983,-1.21145207040314,1.94842840390733));
#58628=CARTESIAN_POINT('Ctrl Pts',(4.95376609667662,1.32403660424732,2.08760186132928));
#58629=CARTESIAN_POINT('Ctrl Pts',(3.71366788460521,3.5357520353937,2.22677531875123));
#58630=CARTESIAN_POINT('Ctrl Pts',(1.56544772852549,4.88285212444658,2.36594877617319));
#58631=CARTESIAN_POINT('Ctrl Pts',(-0.965579261288932,5.03592377327551,
2.50512223359514));
#58632=CARTESIAN_POINT('Ctrl Pts',(-3.26048828129931,3.9575355560864,2.6442956910171));
#58633=CARTESIAN_POINT('Ctrl Pts',(-4.75809364994143,1.91139120725042,2.78346914843904));
#58634=CARTESIAN_POINT('Ctrl Pts',(-5.09217836896138,-0.602155282161658,
2.922642605861));
#58635=CARTESIAN_POINT('Ctrl Pts',(-4.18104701653603,-2.96845369999834,
3.06181606328295));
#58636=CARTESIAN_POINT('Ctrl Pts',(-2.24750313966228,-4.60886115685302,
3.2009895207049));
#58637=CARTESIAN_POINT('Ctrl Pts',(0.235634020762259,-5.12224053832399,
3.34016297812685));
#58638=CARTESIAN_POINT('Ctrl Pts',(2.66115040510108,-4.38305259454633,3.47933643554881));
#58639=CARTESIAN_POINT('Ctrl Pts',(4.43592225278534,-2.57205468293112,3.61850989297076));
#58640=CARTESIAN_POINT('Ctrl Pts',(5.12595564846396,-0.132099261254929,
3.75768335039271));
#58641=CARTESIAN_POINT('Ctrl Pts',(4.56251324399756,2.34015905938081,3.89685680781466));
#58642=CARTESIAN_POINT('Ctrl Pts',(2.88337645366723,4.24016647683272,4.03603026523662));
#58643=CARTESIAN_POINT('Ctrl Pts',(0.499153069686797,5.10330458995647,4.17520372265857));
#58644=CARTESIAN_POINT('Ctrl Pts',(-2.00713073313589,4.71850588056565,4.31437718008052));
#58645=CARTESIAN_POINT('Ctrl Pts',(-4.02260072986122,3.17986711875809,4.45355063750247));
#58646=CARTESIAN_POINT('Ctrl Pts',(-5.05440387218634,0.86363940488164,4.59272409492443));
#58647=CARTESIAN_POINT('Ctrl Pts',(-4.85022813126969,-1.66377841056938,
4.73189755234637));
#58648=CARTESIAN_POINT('Ctrl Pts',(-3.46000163130249,-3.78434409590636,
4.87107100976833));
#58649=CARTESIAN_POINT('Ctrl Pts',(-1.22368347336451,-4.9795050237801,5.01024446719028));
#58650=CARTESIAN_POINT('Ctrl Pts',(1.31186817898678,-4.95700246175034,5.14941792461223));
#58651=CARTESIAN_POINT('Ctrl Pts',(3.52662208588147,-3.72233907485736,5.28859138203419));
#58652=CARTESIAN_POINT('Ctrl Pts',(4.87899329888229,-1.57743333117398,5.42776483945614));
#58653=CARTESIAN_POINT('Ctrl Pts',(5.03827966124805,0.953210144664441,5.56693829687808));
#58654=CARTESIAN_POINT('Ctrl Pts',(3.96553007503505,3.25076033395718,5.70611175430005));
#58655=CARTESIAN_POINT('Ctrl Pts',(1.92306940962342,4.75338569554455,5.84528521172199));
#58656=CARTESIAN_POINT('Ctrl Pts',(-0.589649122276164,5.09364166755337,
5.98445866914395));
#58657=CARTESIAN_POINT('Ctrl Pts',(-2.9581777789531,4.18832374022651,6.1236321265659));
#58658=CARTESIAN_POINT('Ctrl Pts',(-4.60332829646294,2.25881387454135,6.26280558398785));
#58659=CARTESIAN_POINT('Ctrl Pts',(-5.12280371737697,-0.223055145795024,
6.4019790414098));
#58660=CARTESIAN_POINT('Ctrl Pts',(-4.3895740957611,-2.65037936580031,6.54115249883176));
#58661=CARTESIAN_POINT('Ctrl Pts',(-2.58293977084456,-4.42959294574867,
6.68032595625371));
#58662=CARTESIAN_POINT('Ctrl Pts',(-0.14468615032387,-5.12561581107493,
6.81949941367566));
#58663=CARTESIAN_POINT('Ctrl Pts',(2.32894830461766,-4.5682459784096,6.95867287109761));
#58664=CARTESIAN_POINT('Ctrl Pts',(4.2330732788251,-2.89377990540639,7.09784632851956));
#58665=CARTESIAN_POINT('Ctrl Pts',(5.10206348419584,-0.51168323020428,7.23701978594152));
#58666=CARTESIAN_POINT('Ctrl Pts',(4.72342036091109,1.9955379272185,7.37619324336347));
#58667=CARTESIAN_POINT('Ctrl Pts',(3.18973542252992,4.01478012587175,7.51536670078542));
#58668=CARTESIAN_POINT('Ctrl Pts',(0.876048385964622,5.05226788188094,7.65454015820737));
#58669=CARTESIAN_POINT('Ctrl Pts',(-1.65186318293549,4.85429907913586,7.79371361562932));
#58670=CARTESIAN_POINT('Ctrl Pts',(-3.77583631245843,3.46928402791661,7.93288707305128));
#58671=CARTESIAN_POINT('Ctrl Pts',(-4.97648513573483,1.23590744744384,8.07206053047323));
#58672=CARTESIAN_POINT('Ctrl Pts',(-4.96020893756964,-1.29969181750568,
8.21123398789518));
#58673=CARTESIAN_POINT('Ctrl Pts',(-3.73098781882938,-3.51747088411314,
8.35040744531713));
#58674=CARTESIAN_POINT('Ctrl Pts',(-1.58940942229392,-4.87510504637185,
8.48958090273909));
#58675=CARTESIAN_POINT('Ctrl Pts',(0.940835280389158,-5.04060517200187,
8.62875436016105));
#58676=CARTESIAN_POINT('Ctrl Pts',(3.24101278453099,-3.97350068017404,8.76792781758299));
#58677=CARTESIAN_POINT('Ctrl Pts',(4.74864907841449,-1.93473601685351,8.90710127500494));
#58678=CARTESIAN_POINT('Ctrl Pts',(5.09507425160708,0.577139407290319,9.04627473242689));
#58679=CARTESIAN_POINT('Ctrl Pts',(4.19557520845658,2.94788401994064,9.18544818984885));
#58680=CARTESIAN_POINT('Ctrl Pts',(2.27011098883077,4.59776767825721,9.3246216472708));
#58681=CARTESIAN_POINT('Ctrl Pts',(-0.210474925808355,5.12333600600652,
9.46379510469275));
#58682=CARTESIAN_POINT('Ctrl Pts',(-2.63959234478916,4.39606912800144,9.60296856211471));
#58683=CARTESIAN_POINT('Ctrl Pts',(-4.42323692839189,2.59380928368822,9.74214201953665));
#58684=CARTESIAN_POINT('Ctrl Pts',(-5.12524506636906,0.157272166947933,
9.88131547695861));
#58685=CARTESIAN_POINT('Ctrl Pts',(-4.57395116642832,-2.31772350636695,
10.0204889343806));
#58686=CARTESIAN_POINT('Ctrl Pts',(-2.90416590773529,-4.225954555504,10.1596623918025));
#58687=CARTESIAN_POINT('Ctrl Pts',(-0.524210305286386,-5.10079161313893,
10.2988358492245));
#58688=CARTESIAN_POINT('Ctrl Pts',(1.98393308826428,-4.72830635916573,10.4380093066464));
#58689=CARTESIAN_POINT('Ctrl Pts',(4.00693531287256,-3.1995844922883,10.5771827640684));
#58690=CARTESIAN_POINT('Ctrl Pts',(5.05010142654417,-0.888452084500591,
10.7163562214903));
#58691=CARTESIAN_POINT('Ctrl Pts',(4.85834075571687,1.63993799461361,10.8555296789123));
#58692=CARTESIAN_POINT('Ctrl Pts',(3.47854550484689,3.76730576082515,10.9947031363342));
#58693=CARTESIAN_POINT('Ctrl Pts',(1.24812396903648,4.97343523962598,11.1338765937562));
#58694=CARTESIAN_POINT('Ctrl Pts',(-1.28750761891996,4.96338550347039,11.2730500511781));
#58695=CARTESIAN_POINT('Ctrl Pts',(-3.5082984720956,3.73961406505117,11.4122235086001));
#58696=CARTESIAN_POINT('Ctrl Pts',(-4.87118739711688,1.60137592932035,11.551396966022));
#58697=CARTESIAN_POINT('Ctrl Pts',(-5.04290028805014,-0.928454742903895,
11.690570423444));
#58698=CARTESIAN_POINT('Ctrl Pts',(-3.98144732521719,-3.23124569189002,
11.829743880866));
#58699=CARTESIAN_POINT('Ctrl Pts',(-1.94639095768057,-4.74388382706577,
11.9689173382879));
#58700=CARTESIAN_POINT('Ctrl Pts',(0.564626212170274,-5.09647611250825,
12.1080907957099));
#58701=CARTESIAN_POINT('Ctrl Pts',(2.93757248527155,-4.20280137748769,12.2472642531318));
#58702=CARTESIAN_POINT('Ctrl Pts',(4.59217933564339,-2.28139441441562,12.3864377105538));
#58703=CARTESIAN_POINT('Ctrl Pts',(5.12383740106595,0.197893436663885,12.5256111679757));
#58704=CARTESIAN_POINT('Ctrl Pts',(4.40253765207021,2.62878940711139,12.6647846253977));
#58705=CARTESIAN_POINT('Ctrl Pts',(2.60466315593581,4.41685423904247,12.8039580828196));
#58706=CARTESIAN_POINT('Ctrl Pts',(0.169857235225308,5.12484341658148,12.9431315402416));
#58707=CARTESIAN_POINT('Ctrl Pts',(-2.30648473230954,4.57962877365185,13.0823049976635));
#58708=CARTESIAN_POINT('Ctrl Pts',(-4.21881034979734,2.9145343980265,13.2214784550854));
#58709=CARTESIAN_POINT('Ctrl Pts',(-5.09948898445394,0.536734219395287,
13.3606519125074));
#58710=CARTESIAN_POINT('Ctrl Pts',(-4.73316384586776,-1.97231628625004,
13.4998253699294));
#58711=CARTESIAN_POINT('Ctrl Pts',(-3.20941426864339,-3.99906633816759,
13.6389988273513));
#58712=CARTESIAN_POINT('Ctrl Pts',(-0.900850425695856,-5.04790451923969,
13.7781722847733));
#58713=CARTESIAN_POINT('Ctrl Pts',(1.62800291751233,-4.86235313664159,13.9173457421952));
#58714=CARTESIAN_POINT('Ctrl Pts',(3.75875249244549,-3.4877860062469,14.0565191996172));
#58715=CARTESIAN_POINT('Ctrl Pts',(4.97035535384435,-1.26033296447714,14.1956926570391));
#58716=CARTESIAN_POINT('Ctrl Pts',(4.96653214029797,1.27531565669998,14.3348661144611));
#58717=CARTESIAN_POINT('Ctrl Pts',(3.7482177615067,3.49910490513827,14.474039571883));
#58718=CARTESIAN_POINT('Ctrl Pts',(1.61333278009552,4.86724037474072,14.613213029305));
#58719=CARTESIAN_POINT('Ctrl Pts',(-0.916068606863061,5.04516499555335,
14.7523864867269));
#58720=CARTESIAN_POINT('Ctrl Pts',(-3.22145911492965,3.98936996224636,14.8915599441489));
#58721=CARTESIAN_POINT('Ctrl Pts',(-4.73908997023278,1.95803416182558,15.0307334015708));
#58722=CARTESIAN_POINT('Ctrl Pts',(-5.09784724180366,-0.552109612370288,
15.1699068589928));
#58723=CARTESIAN_POINT('Ctrl Pts',(-4.21000220374625,-2.92724323712408,
15.3090803164148));
#58724=CARTESIAN_POINT('Ctrl Pts',(-2.29266408325714,-4.58656330231903,
15.4482537738367));
#58725=CARTESIAN_POINT('Ctrl Pts',(0.185310754227624,-5.12430789953185,
15.5874272312587));
#58726=CARTESIAN_POINT('Ctrl Pts',(2.6179706179084,-4.40897962896238,15.7266006886806));
#58727=CARTESIAN_POINT('Ctrl Pts',(4.41044491618784,-2.61550132213878,15.8657741461026));
#58728=CARTESIAN_POINT('Ctrl Pts',(5.12441086413413,-0.182441279268398,
16.0049476035245));
#58729=CARTESIAN_POINT('Ctrl Pts',(4.58527876584435,2.29523205021492,16.1441210609465));
#58730=CARTESIAN_POINT('Ctrl Pts',(2.92488531375835,4.21164070478449,16.2832945183684));
#58731=CARTESIAN_POINT('Ctrl Pts',(0.549254897012139,5.09815560599567,16.4224679757903));
#58732=CARTESIAN_POINT('Ctrl Pts',(-1.96068759122481,4.73799279172668,16.5616414332123));
#58733=CARTESIAN_POINT('Ctrl Pts',(-3.99117324920656,3.21922469232187,16.7008148906343));
#58734=CARTESIAN_POINT('Ctrl Pts',(-5.0456771732148,0.913243334788716,16.8399883480562));
#58735=CARTESIAN_POINT('Ctrl Pts',(-4.86633619771543,-1.61605802359984,
16.9791618054782));
#58736=CARTESIAN_POINT('Ctrl Pts',(-3.4970054763967,-3.75017655889538,17.1183352629001));
#58737=CARTESIAN_POINT('Ctrl Pts',(-1.27253436014598,-4.96724549696155,
17.2575087203221));
#58738=CARTESIAN_POINT('Ctrl Pts',(1.2631160043629,-4.96964882907829,17.3966821777441));
#58739=CARTESIAN_POINT('Ctrl Pts',(3.48989023867801,-3.75679885631596,17.535855635166));
#58740=CARTESIAN_POINT('Ctrl Pts',(4.86326400304377,-1.62527990252007,17.675029092588));
#58741=CARTESIAN_POINT('Ctrl Pts',(5.04739928085542,0.903676946954519,17.8142025500099));
#58742=CARTESIAN_POINT('Ctrl Pts',(3.9972685434884,3.21165311266256,17.9533760074318));
#58743=CARTESIAN_POINT('Ctrl Pts',(1.96966555908043,4.73426753682229,18.0925494648538));
#58744=CARTESIAN_POINT('Ctrl Pts',(-0.539589683365057,5.09918763122548,
18.2317229222758));
#58745=CARTESIAN_POINT('Ctrl Pts',(-2.91689633778329,4.21717764381148,18.3708963796977));
#58746=CARTESIAN_POINT('Ctrl Pts',(-4.58091961214863,2.30391992739958,18.5100698371197));
#58747=CARTESIAN_POINT('Ctrl Pts',(-5.12474749856713,-0.1727269543728,18.6492432945416));
#58748=CARTESIAN_POINT('Ctrl Pts',(-4.41539501983301,-2.60713604241717,
18.7884167519636));
#58749=CARTESIAN_POINT('Ctrl Pts',(-2.62632371694331,-4.40400899847605,
18.9275902093855));
#58750=CARTESIAN_POINT('Ctrl Pts',(-0.195024223195767,-5.12394741163527,
19.0667636668075));
#58751=CARTESIAN_POINT('Ctrl Pts',(2.28396552793643,-4.59090110893657,19.2059371242294));
#58752=CARTESIAN_POINT('Ctrl Pts',(4.2044456636982,-2.9352185925151,19.3451105816514));
#58753=CARTESIAN_POINT('Ctrl Pts',(5.09679148580437,-0.561772262637615,
19.4842840390733));
#58754=CARTESIAN_POINT('Ctrl Pts',(4.74279316762406,1.94904707330927,19.6234574964953));
#58755=CARTESIAN_POINT('Ctrl Pts',(3.22901570416719,3.98325609358456,19.7626309539172));
#58756=CARTESIAN_POINT('Ctrl Pts',(0.925630737050274,5.04341940190033,19.9018044113392));
#58757=CARTESIAN_POINT('Ctrl Pts',(-1.60410338490353,4.87028991492066,20.0409778687611));
#58758=CARTESIAN_POINT('Ctrl Pts',(-3.7415780118875,3.5062038597031,20.1801513261831));
#58759=CARTESIAN_POINT('Ctrl Pts',(-4.96410568772994,1.28472808246885,20.319324783605));
#58760=CARTESIAN_POINT('Ctrl Pts',(-4.97273555101776,-1.25090873547233,
20.458498241027));
#58761=CARTESIAN_POINT('Ctrl Pts',(-3.76535729773513,-3.48065452827909,
20.5976716984489));
#58762=CARTESIAN_POINT('Ctrl Pts',(-1.63721722455307,-4.85925830600346,
20.7368451558709));
#58763=CARTESIAN_POINT('Ctrl Pts',(0.891279837899838,-5.04960313048365,
20.8760186132929));
#58764=CARTESIAN_POINT('Ctrl Pts',(3.20182774421876,-4.00514302131496,21.0151920707148));
#58765=CARTESIAN_POINT('Ctrl Pts',(4.72941655591346,-1.98128507930803,21.1543655281368));
#58766=CARTESIAN_POINT('Ctrl Pts',(5.10049727269117,0.527066500649415,21.2935389855586));
#58767=CARTESIAN_POINT('Ctrl Pts',(4.22432765441569,2.9065318496407,21.4327124429807));
#58768=CARTESIAN_POINT('Ctrl Pts',(2.3151618789705,4.57524829916352,21.5718859004026));
#58769=CARTESIAN_POINT('Ctrl Pts',(-0.160142112979361,5.12515619552101,
21.7110593578246));
#58770=CARTESIAN_POINT('Ctrl Pts',(-2.5962857459699,4.4217837859975,21.8502328152465));
#58771=CARTESIAN_POINT('Ctrl Pts',(-4.39754652471548,2.63713027509066,21.9894062726684));
#58772=CARTESIAN_POINT('Ctrl Pts',(-5.12345306187953,0.207605991132635,
22.1285797300904));
#58773=CARTESIAN_POINT('Ctrl Pts',(-4.5964957690259,-2.27268523341089,22.2677531875124));
#58774=CARTESIAN_POINT('Ctrl Pts',(-2.94553417198737,-4.19722526992435,
22.4069266449343));
#58775=CARTESIAN_POINT('Ctrl Pts',(-0.57428624079235,-5.09539663210565,
22.5461001023563));
#58776=CARTESIAN_POINT('Ctrl Pts',(1.93739480269542,-4.74756494461378,22.6852735597782));
#58777=CARTESIAN_POINT('Ctrl Pts',(3.97531491904182,-3.23878724513983,22.8244470172002));
#58778=CARTESIAN_POINT('Ctrl Pts',(5.04113121891057,-0.938012557784862,
22.9636204746221));
#58779=CARTESIAN_POINT('Ctrl Pts',(4.87421426441648,1.59213907350953,23.1027939320441));
#58780=CARTESIAN_POINT('Ctrl Pts',(3.51538110070013,3.73295690327082,23.241967389466));
#58781=CARTESIAN_POINT('Ctrl Pts',(1.29691405791799,4.9609359450825,23.381140846888));
#58782=CARTESIAN_POINT('Ctrl Pts',(-1.23869392363774,4.97579228750355,23.52031430431));
#58783=CARTESIAN_POINT('Ctrl Pts',(-3.47139782963254,3.77389303415709,23.6594877617318));
#58784=CARTESIAN_POINT('Ctrl Pts',(-4.85522330777404,1.64914467421285,23.7986612191539));
#58785=CARTESIAN_POINT('Ctrl Pts',(-5.05177653114886,-0.878877354453079,
23.9378346765758));
#58786=CARTESIAN_POINT('Ctrl Pts',(-4.01299334824328,-3.19198306884484,
24.0770081339978));
#58787=CARTESIAN_POINT('Ctrl Pts',(-1.99289265244315,-4.72453705675752,
24.2161815914197));
#58788=CARTESIAN_POINT('Ctrl Pts',(0.514540139737736,-5.10177615830366,
24.3553550488417));
#58789=CARTESIAN_POINT('Ctrl Pts',(2.89614983519387,-4.23145219244452,24.4945285062636));
#58790=CARTESIAN_POINT('Ctrl Pts',(4.56954939756152,-2.32638987018126,24.6337019636856));
#58791=CARTESIAN_POINT('Ctrl Pts',(5.12553398792908,0.147556305933546,24.7728754211075));
#58792=CARTESIAN_POINT('Ctrl Pts',(4.42814588893175,2.58541979399356,24.9120488785295));
#58793=CARTESIAN_POINT('Ctrl Pts',(2.64792093141759,4.39105753387467,25.0512223359514));
#58794=CARTESIAN_POINT('Ctrl Pts',(0.220186507211287,5.12292781784782,25.1903957933734));
#58795=CARTESIAN_POINT('Ctrl Pts',(-2.26139123465815,4.60206271237672,25.3295692507953));
#58796=CARTESIAN_POINT('Ctrl Pts',(-4.18997956700173,2.95583198997252,25.4687427082172));
#58797=CARTESIAN_POINT('Ctrl Pts',(-5.09397105331041,0.586796756017421,
25.6079161656392));
#58798=CARTESIAN_POINT('Ctrl Pts',(-4.75230809392217,-1.92573084964611,
25.7470896230612));
#58799=CARTESIAN_POINT('Ctrl Pts',(-3.24853925631766,-3.96734977346339,
25.8862630804831));
#58800=CARTESIAN_POINT('Ctrl Pts',(-0.950388722330458,-5.03881263804321,
26.0254365379051));
#58801=CARTESIAN_POINT('Ctrl Pts',(1.58016516156227,-4.87810922253918,26.164609995327));
#58802=CARTESIAN_POINT('Ctrl Pts',(3.72431328503039,-3.52453714404928,26.303783452749));
#58803=CARTESIAN_POINT('Ctrl Pts',(4.95773628813266,-1.30909221301232,26.4429569101709));
#58804=CARTESIAN_POINT('Ctrl Pts',(4.97881902010364,1.22647164251408,26.5821303675929));
#58805=CARTESIAN_POINT('Ctrl Pts',(3.78240601411158,3.462120198556,26.7213038250149));
#58806=CARTESIAN_POINT('Ctrl Pts',(1.66106217957725,4.85115903268642,26.8604772824368));
#58807=CARTESIAN_POINT('Ctrl Pts',(-0.866469571400946,5.05391946974555,
26.9996507398587));
#58808=CARTESIAN_POINT('Ctrl Pts',(-3.182119145904,4.02081947693602,27.1388241972807));
#58809=CARTESIAN_POINT('Ctrl Pts',(-4.7196290687778,2.00448820849228,27.2779976547026));
#58810=CARTESIAN_POINT('Ctrl Pts',(-5.10302428035127,-0.502010676163758,
27.4171711121246));
#58811=CARTESIAN_POINT('Ctrl Pts',(-4.23855121493717,-2.88575035704607,
27.5563445695465));
#58812=CARTESIAN_POINT('Ctrl Pts',(-2.33760383332739,-4.56382294170687,
27.6955180269685));
#58813=CARTESIAN_POINT('Ctrl Pts',(0.134969609127406,-5.12588087351325,
27.8346914843905));
#58814=CARTESIAN_POINT('Ctrl Pts',(2.57453825200954,-4.43448129027247,27.9738649418124));
#58815=CARTESIAN_POINT('Ctrl Pts',(4.38454206508205,-2.65869562085676,28.1130383992344));
#58816=CARTESIAN_POINT('Ctrl Pts',(5.12237168270734,-0.232765695571575,
28.2522118566563));
#58817=CARTESIAN_POINT('Ctrl Pts',(4.60760190542052,2.25008359978071,28.3913853140782));
#58818=CARTESIAN_POINT('Ctrl Pts',(2.96611198437499,4.18270859862171,28.5305587715002));
#58819=CARTESIAN_POINT('Ctrl Pts',(0.59930373287477,5.09251475801487,28.6697322289221));
#58820=CARTESIAN_POINT('Ctrl Pts',(-1.91405528449465,4.75702258694817,28.8089056863441));
#58821=CARTESIAN_POINT('Ctrl Pts',(-3.95936070487888,3.25827167889634,28.948079143766));
#58822=CARTESIAN_POINT('Ctrl Pts',(-5.03646367327922,0.962759156059136,
29.0872526011881));
#58823=CARTESIAN_POINT('Ctrl Pts',(-4.88197476580226,-1.56818172126413,
29.22642605861));
#58824=CARTESIAN_POINT('Ctrl Pts',(-3.5336719345399,-3.71564720928695,29.3655995160319));
#58825=CARTESIAN_POINT('Ctrl Pts',(-1.3212624743179,-4.95450673617428,29.5047729734539));
#58826=CARTESIAN_POINT('Ctrl Pts',(1.21424196580137,-4.98181573056689,29.6439464308758));
#58827=CARTESIAN_POINT('Ctrl Pts',(3.45282169099331,-3.79089618626559,29.7831198882978));
#58828=CARTESIAN_POINT('Ctrl Pts',(4.84706550524806,-1.67296966878402,29.9222933457197));
#58829=CARTESIAN_POINT('Ctrl Pts',(5.05603193335185,0.854056563561975,30.0614668031417));
#58830=CARTESIAN_POINT('Ctrl Pts',(4.02862136020189,3.17223603487539,30.2006402605636));
#58831=CARTESIAN_POINT('Ctrl Pts',(2.01607167753466,4.71469262156925,30.3398137179856));
#58832=CARTESIAN_POINT('Ctrl Pts',(-0.48947818547963,5.10424163130788,30.4789871754075));
#58833=CARTESIAN_POINT('Ctrl Pts',(-2.87533347790578,4.24562467908683,30.6181606328295));
#58834=CARTESIAN_POINT('Ctrl Pts',(-4.55806896612991,2.34880370078906,30.7573340902515));
#58835=CARTESIAN_POINT('Ctrl Pts',(-5.12619685018181,-0.122382098458352,
30.8965075476734));
#58836=CARTESIAN_POINT('Ctrl Pts',(-4.44078995181737,-2.56364118563321,
31.0356810050954));
#58837=CARTESIAN_POINT('Ctrl Pts',(-2.66945427843709,-4.37800015762571,
31.1748544625173));
#58838=CARTESIAN_POINT('Ctrl Pts',(-0.245343480361355,-5.12178465981157,
31.3140279199393));
#58839=CARTESIAN_POINT('Ctrl Pts',(2.23876239696327,-4.61311331475612,31.4532013773612));
#58840=CARTESIAN_POINT('Ctrl Pts',(4.17541240862802,-2.97637409320671,31.5923748347831));
#58841=CARTESIAN_POINT('Ctrl Pts',(5.09102775500046,-0.611807095947689,
31.7315482922051));
#58842=CARTESIAN_POINT('Ctrl Pts',(4.7617083952635,1.90236817764437,31.8707217496271));
#58843=CARTESIAN_POINT('Ctrl Pts',(3.26798445418964,3.95134776146213,32.009895207049));
#58844=CARTESIAN_POINT('Ctrl Pts',(0.975123784377534,5.03408433878279,32.149068664471));
#58845=CARTESIAN_POINT('Ctrl Pts',(-1.5561888248749,4.8858108708966,32.2882421218929));
#58846=CARTESIAN_POINT('Ctrl Pts',(-3.70695872829678,3.5427854170894,32.4274155793149));
#58847=CARTESIAN_POINT('Ctrl Pts',(-4.95124730868146,1.33342476844834,32.5665890367368));
#58848=CARTESIAN_POINT('Ctrl Pts',(-4.98478240082323,-1.20200496724427,
32.7057624941588));
#58849=CARTESIAN_POINT('Ctrl Pts',(-3.79936349942357,-3.44350236301427,
32.8449359515807));
#58850=CARTESIAN_POINT('Ctrl Pts',(-1.68486707003129,-4.84294275014284,
32.9841094090027));
#58851=CARTESIAN_POINT('Ctrl Pts',(0.841638405786343,-5.05811390922963,
33.1232828664246));
#58852=CARTESIAN_POINT('Ctrl Pts',(3.16233379535394,-4.03639895099572,33.2624563238466));
#58853=CARTESIAN_POINT('Ctrl Pts',(4.70972774489857,-2.02764298972218,33.4016297812685));
#58854=CARTESIAN_POINT('Ctrl Pts',(5.10542820383288,0.476942743256107,33.5408032386905));
#58855=CARTESIAN_POINT('Ctrl Pts',(4.25267254224057,2.86489926058667,33.6799766961124));
#58856=CARTESIAN_POINT('Ctrl Pts',(2.35998940503126,4.55228750552699,33.8191501535344));
#58857=CARTESIAN_POINT('Ctrl Pts',(-0.109793849828778,5.12648191602942,
33.9583236109563));
#58858=CARTESIAN_POINT('Ctrl Pts',(-2.55272866057358,4.44707183552539,34.0974970683783));
#58859=CARTESIAN_POINT('Ctrl Pts',(-4.37143185095318,2.68019683928419,34.2366705258002));
#58860=CARTESIAN_POINT('Ctrl Pts',(-5.12116675270024,0.257919785736935,
34.3758439832222));
#58861=CARTESIAN_POINT('Ctrl Pts',(-4.61859690714988,-2.22742769447237,
34.5150174406442));
#58862=CARTESIAN_POINT('Ctrl Pts',(-2.98661825458746,-4.16809104101649,
34.6541908980661));
#58863=CARTESIAN_POINT('Ctrl Pts',(-0.624306769841251,-5.08951005323373,
34.7933643554881));
#58864=CARTESIAN_POINT('Ctrl Pts',(1.89066959956818,-4.76636549061291,34.93253781291));
#58865=CARTESIAN_POINT('Ctrl Pts',(3.94331099153097,-3.27767752362979,35.071711270332));
#58866=CARTESIAN_POINT('Ctrl Pts',(5.03167464890124,-0.987482532727304,
35.2108847277539));
#58867=CARTESIAN_POINT('Ctrl Pts',(4.88961751469062,1.54418654471136,35.3500581851759));
#58868=CARTESIAN_POINT('Ctrl Pts',(3.55187753674385,3.69824789445101,35.4892316425978));
#58869=CARTESIAN_POINT('Ctrl Pts',(1.34557902206557,4.94795802530842,35.6284051000198));
#58870=CARTESIAN_POINT('Ctrl Pts',(-1.18976072063133,4.98771901298376,35.7675785574417));
#58871=CARTESIAN_POINT('Ctrl Pts',(-3.43416227081397,3.807807902528,35.9067520148637));
#58872=CARTESIAN_POINT('Ctrl Pts',(-4.83879079223079,1.69675431157828,36.0459254722857));
#58873=CARTESIAN_POINT('Ctrl Pts',(-5.0601653848247,-0.829215172954957,
36.1850989297076));
#58874=CARTESIAN_POINT('Ctrl Pts',(-4.04415220241896,-3.15241248704969,
36.3242723871296));
#58875=CARTESIAN_POINT('Ctrl Pts',(-2.0392020752804,-4.70473446870373,36.4634458445515));
#58876=CARTESIAN_POINT('Ctrl Pts',(0.464404425081292,-5.10658399077132,
36.6026193019735));
#58877=CARTESIAN_POINT('Ctrl Pts',(2.85444776800653,-4.25969476190013,36.7417927593954));
#58878=CARTESIAN_POINT('Ctrl Pts',(4.54647859476008,-2.3711608786047,36.8809662168174));
#58879=CARTESIAN_POINT('Ctrl Pts',(5.12673606933716,0.0972049391453199,
37.0201396742393));
#58880=CARTESIAN_POINT('Ctrl Pts',(4.45332690351699,2.5418007426328,37.1593131316613));
#58881=CARTESIAN_POINT('Ctrl Pts',(2.69092323862078,4.3648371846711,37.2984865890832));
#58882=CARTESIAN_POINT('Ctrl Pts',(0.270494535863632,5.12051796509932,37.4376600465052));
#58883=CARTESIAN_POINT('Ctrl Pts',(-2.21607956065588,4.62405264953592,37.576833503927));
#58884=CARTESIAN_POINT('Ctrl Pts',(-4.16074453993469,2.9968444067453,37.7160069613491));
#58885=CARTESIAN_POINT('Ctrl Pts',(-5.08796166186641,0.636802679182853,
37.855180418771));
#58886=CARTESIAN_POINT('Ctrl Pts',(-4.77099384491424,-1.87895962080811,
37.994353876193));
#58887=CARTESIAN_POINT('Ctrl Pts',(-3.28735082876793,-3.93525044354685,
38.1335273336149));
#58888=CARTESIAN_POINT('Ctrl Pts',(-0.999835326585605,-5.02923461816492,
38.2727007910369));
#58889=CARTESIAN_POINT('Ctrl Pts',(1.53217495314691,-4.89339467423037,38.4118742484588));
#58890=CARTESIAN_POINT('Ctrl Pts',(3.68951476027582,-3.56094823867799,38.5510477058808));
#58891=CARTESIAN_POINT('Ctrl Pts',(4.94463890588947,-1.35772516187962,38.6902211633027));
#58892=CARTESIAN_POINT('Ctrl Pts',(4.99062554934078,1.17750929979514,38.8293946207247));
#58893=CARTESIAN_POINT('Ctrl Pts',(3.81622934465927,3.42480147071306,38.9685680781466));
#58894=CARTESIAN_POINT('Ctrl Pts',(1.70863132174512,4.83460965654813,39.1077415355686));
#58895=CARTESIAN_POINT('Ctrl Pts',(-0.81678693997971,5.06218634776669,39.2469149929905));
#58896=CARTESIAN_POINT('Ctrl Pts',(-3.14247216978798,4.05188106771966,39.3860884504125));
#58897=CARTESIAN_POINT('Ctrl Pts',(-4.69971282309411,2.0507488645082,39.5252619078343));
#58898=CARTESIAN_POINT('Ctrl Pts',(-5.10770898515378,-0.451863306561025,
39.6644353652565));
#58899=CARTESIAN_POINT('Ctrl Pts',(-4.26669129572166,-2.84397906318768,
39.8036088226782));
#58900=CARTESIAN_POINT('Ctrl Pts',(-2.3823180541456,-4.54064226885678,39.9427822801004));
#58901=CARTESIAN_POINT('Ctrl Pts',(0.0846154423188459,-5.12695930857248,
40.0819557375222));
#58902=CARTESIAN_POINT('Ctrl Pts',(2.53085749770598,-4.45955511807427,40.2211291949443));
#58903=CARTESIAN_POINT('Ctrl Pts',(4.35821619854518,-2.70163341176691,40.3603026523661));
#58904=CARTESIAN_POINT('Ctrl Pts',(5.11983830092096,-0.283067654915984,
40.4994761097881));
#58905=CARTESIAN_POINT('Ctrl Pts',(4.62948050901625,2.20471806394278,40.6386495672101));
#58906=CARTESIAN_POINT('Ctrl Pts',(3.00705248801675,4.15337294968188,40.7778230246319));
#58907=CARTESIAN_POINT('Ctrl Pts',(0.649294748622445,5.08638259023525,40.916996482054));
#58908=CARTESIAN_POINT('Ctrl Pts',(-1.86723831197507,4.77559343025863,41.0561699394759));
#58909=CARTESIAN_POINT('Ctrl Pts',(-3.92716616611468,3.29700431127425,41.1953433968979));
#58910=CARTESIAN_POINT('Ctrl Pts',(-5.02676426128715,1.01218209146538,41.3345168543198));
#58911=CARTESIAN_POINT('Ctrl Pts',(-4.89714232673967,-1.52015412261115,
41.4736903117417));
#58912=CARTESIAN_POINT('Ctrl Pts',(-3.56999746819571,-3.68075937843173,
41.6128637691637));
#58913=CARTESIAN_POINT('Ctrl Pts',(-1.36986311464964,-4.94128997043882,
41.7520372265857));
#58914=CARTESIAN_POINT('Ctrl Pts',(1.16525077861143,-4.99350199236792,41.8912106840076));
#58915=CARTESIAN_POINT('Ctrl Pts',(3.4154200191569,-3.82462777503633,42.0303841414296));
#58916=CARTESIAN_POINT('Ctrl Pts',(4.83039936830708,-1.72049802891365,42.1695575988515));
#58917=CARTESIAN_POINT('Ctrl Pts',(5.06417678586922,0.804353781802734,42.3087310562735));
#58918=CARTESIAN_POINT('Ctrl Pts',(4.05958550029279,3.13251290350884,42.4479045136954));
#58919=CARTESIAN_POINT('Ctrl Pts',(2.06228328777852,4.69466283835021,42.5870779711175));
#58920=CARTESIAN_POINT('Ctrl Pts',(-0.439319463318189,5.10880318019658,
42.7262514285393));
#58921=CARTESIAN_POINT('Ctrl Pts',(-2.83349320925637,4.2736621015161,42.8654248859613));
#58922=CARTESIAN_POINT('Ctrl Pts',(-4.53477856301013,2.39346086437625,43.0045983433833));
#58923=CARTESIAN_POINT('Ctrl Pts',(-5.12715163238927,-0.0720254352639578,
43.1437718008051));
#58924=CARTESIAN_POINT('Ctrl Pts',(-4.4657564416411,-2.51989899178081,43.2829452582272));
#58925=CARTESIAN_POINT('Ctrl Pts',(-2.71232729414031,-4.35156893249991,
43.4221187156491));
#58926=CARTESIAN_POINT('Ctrl Pts',(-0.29563906707815,-5.11912776426357,
43.5612921730711));
#58927=CARTESIAN_POINT('Ctrl Pts',(2.19334327284283,-4.63488045286089,43.700465630493));
#58928=CARTESIAN_POINT('Ctrl Pts',(4.14597631470871,-3.01724243684715,43.8396390879149));
#58929=CARTESIAN_POINT('Ctrl Pts',(5.08477284786202,-0.661782902832914,
43.978812545337));
#58930=CARTESIAN_POINT('Ctrl Pts',(4.78016421891062,1.85550574374848,44.1179860027588));
#58931=CARTESIAN_POINT('Ctrl Pts',(3.30663791293829,3.91905820798263,44.2571594601809));
#58932=CARTESIAN_POINT('Ctrl Pts',(1.0245227529157,5.02426359316417,44.3963329176028));
#58933=CARTESIAN_POINT('Ctrl Pts',(-1.50812412558962,4.90086044962019,44.5355063750247));
#58934=CARTESIAN_POINT('Ctrl Pts',(-3.67198180171369,3.57902517073021,44.6746798324467));
#58935=CARTESIAN_POINT('Ctrl Pts',(-4.93791123915052,1.38199280718384,44.8138532898685));
#58936=CARTESIAN_POINT('Ctrl Pts',(-4.99634832472027,-1.15298523099901,
44.9530267472907));
#58937=CARTESIAN_POINT('Ctrl Pts',(-3.83300314301673,-3.40601797271547,
45.0922002047124));
#58938=CARTESIAN_POINT('Ctrl Pts',(-1.73235436152806,-4.82615995289543,
45.2313736621346));
#58939=CARTESIAN_POINT('Ctrl Pts',(0.791915773395165,-5.06613668713003,
45.3705471195564));
#58940=CARTESIAN_POINT('Ctrl Pts',(3.12253474826594,-4.06726545368122,45.5097205769784));
#58941=CARTESIAN_POINT('Ctrl Pts',(4.68958454492302,-2.07380527553964,45.6488940344003));
#58942=CARTESIAN_POINT('Ctrl Pts',(5.10986656930181,0.426772970991213,45.7880674918224));
#58943=CARTESIAN_POINT('Ctrl Pts',(4.28060713724999,2.82299026944149,45.9272409492442));
#58944=CARTESIAN_POINT('Ctrl Pts',(2.40458924210636,4.52888751257782,46.0664144066663));
#58945=CARTESIAN_POINT('Ctrl Pts',(-0.0594349938974569,5.12731303962781,
46.205587864088));
#58946=CARTESIAN_POINT('Ctrl Pts',(-2.50892529093627,4.47193083682398,46.3447613215102));
#58947=CARTESIAN_POINT('Ctrl Pts',(-4.34489542661782,2.72300482125766,46.4839347789319));
#58948=CARTESIAN_POINT('Ctrl Pts',(-5.1183863594116,0.308208696545455,46.6231082363541));
#58949=CARTESIAN_POINT('Ctrl Pts',(-4.64025244850859,-2.18195525594519,
46.7622816937759));
#58950=CARTESIAN_POINT('Ctrl Pts',(-3.02741419179187,-4.13855467961632,
46.901455151198));
#58951=CARTESIAN_POINT('Ctrl Pts',(-0.674267066511626,-5.08313244445339,
47.0406286086197));
#58952=CARTESIAN_POINT('Ctrl Pts',(1.84376198687486,-4.78470618330867,47.179802066042));
#58953=CARTESIAN_POINT('Ctrl Pts',(3.91092661804106,-3.31625157567016,47.3189755234636));
#58954=CARTESIAN_POINT('Ctrl Pts',(5.02173262887484,-1.03685723652329,47.4581489808859));
#58955=CARTESIAN_POINT('Ctrl Pts',(4.90454902045194,1.49608503462231,47.5973224383075));
#58956=CARTESIAN_POINT('Ctrl Pts',(3.58803129184512,3.66318208304981,47.7364958957298));
#58957=CARTESIAN_POINT('Ctrl Pts',(1.39411416634107,4.93450273239808,47.8756693531515));
#58958=CARTESIAN_POINT('Ctrl Pts',(-1.14071273091822,4.99916452923466,48.0148428105736));
#58959=CARTESIAN_POINT('Ctrl Pts',(-3.39659538808254,3.84135539809756,48.1540162679954));
#58960=CARTESIAN_POINT('Ctrl Pts',(-4.82189143587676,1.74420024809519,48.2931897254175));
#58961=CARTESIAN_POINT('Ctrl Pts',(-5.068066039731,-0.779472989758009,48.4323631828393));
#58962=CARTESIAN_POINT('Ctrl Pts',(-4.07492088157485,-3.11253776422747,
48.5715366402614));
#58963=CARTESIAN_POINT('Ctrl Pts',(-2.08531475831404,-4.68447797343466,
48.7107100976832));
#58964=CARTESIAN_POINT('Ctrl Pts',(0.414223905235385,-5.11089914605722,
48.8498835551053));
#58965=CARTESIAN_POINT('Ctrl Pts',(2.81247030707573,-4.28752636104482,48.9890570125271));
#58966=CARTESIAN_POINT('Ctrl Pts',(4.52296915308285,-2.41570312023185,49.1282304699492));
#58967=CARTESIAN_POINT('Ctrl Pts',(5.12744352931481,0.0468441941396368,
49.2674039273711));
#58968=CARTESIAN_POINT('Ctrl Pts',(4.47807826639135,2.49793646134371,49.4065773847931));
#58969=CARTESIAN_POINT('Ctrl Pts',(2.73366592873352,4.33819572114011,49.545750842215));
#58970=CARTESIAN_POINT('Ctrl Pts',(0.320776467523109,5.11761409083573,49.6849242996369));
#58971=CARTESIAN_POINT('Ctrl Pts',(-2.17055408191953,4.64559646356626,49.8240977570589));
#58972=CARTESIAN_POINT('Ctrl Pts',(-4.13110808915714,3.03756769151527,49.9632712144808));
#58973=CARTESIAN_POINT('Ctrl Pts',(-5.08146138990095,0.686747164379139,
50.1024446719028));
#58974=CARTESIAN_POINT('Ctrl Pts',(-4.78921929606477,-1.83200711216899,
50.2416181293247));
#58975=CARTESIAN_POINT('Ctrl Pts',(-3.32584524149952,-3.90277144532342,
50.3807915867467));
#58976=CARTESIAN_POINT('Ctrl Pts',(-1.0491854679113,-5.01917138368084,50.5199650441687));
#58977=CARTESIAN_POINT('Ctrl Pts',(1.48403692230487,-4.90820801699284,50.6591385015906));
#58978=CARTESIAN_POINT('Ctrl Pts',(3.65436027550235,-3.59701577723358,50.7983119590126));
#58979=CARTESIAN_POINT('Ctrl Pts',(4.93106447073476,-1.40622711902959,50.9374854164345));
#58980=CARTESIAN_POINT('Ctrl Pts',(5.00195058892939,1.12843335237216,51.0766588738565));
#58981=CARTESIAN_POINT('Ctrl Pts',(3.8496844899148,3.38715232207621,51.2158323312784));
#58982=CARTESIAN_POINT('Ctrl Pts',(1.75603561718453,4.81759384299012,51.3550057887004));
#58983=CARTESIAN_POINT('Ctrl Pts',(-0.767025505920936,5.06996483203814,
51.4941792461224));
#58984=CARTESIAN_POINT('Ctrl Pts',(-3.10252201167498,4.08255173781169,51.6333527035442));
#58985=CARTESIAN_POINT('Ctrl Pts',(-4.67934315467761,2.09681166669986,51.7725261609663));
#58986=CARTESIAN_POINT('Ctrl Pts',(-5.11190090423642,-0.401672341721206,
51.9116996183881));
#58987=CARTESIAN_POINT('Ctrl Pts',(-4.29441973117786,-2.80193338559416,
52.0508730758102));
#58988=CARTESIAN_POINT('Ctrl Pts',(-2.42680243173636,-4.51702352021277,
52.190046533232));
#58989=CARTESIAN_POINT('Ctrl Pts',(0.0342531119126611,-5.12754310066344,
52.3292199906541));
#58990=CARTESIAN_POINT('Ctrl Pts',(2.48693256926547,-4.48419869327436,52.468393448076));
#58991=CARTESIAN_POINT('Ctrl Pts',(4.33146985646582,-2.74431055228173,52.6075669054979));
#58992=CARTESIAN_POINT('Ctrl Pts',(5.1168109631927,-0.333342304227799,52.7467403629199));
#58993=CARTESIAN_POINT('Ctrl Pts',(4.65091246580963,2.15913981951461,52.8859138203419));
#58994=CARTESIAN_POINT('Ctrl Pts',(3.04770287479204,4.12363658823389,53.0250872777638));
#58995=CARTESIAN_POINT('Ctrl Pts',(0.699223121180822,5.07975969428112,53.1642607351858));
#58996=CARTESIAN_POINT('Ctrl Pts',(-1.82024119051244,4.79370352996499,53.3034341926077));
#58997=CARTESIAN_POINT('Ctrl Pts',(-3.89459273900518,3.33541885257685,53.4426076500297));
#58998=CARTESIAN_POINT('Ctrl Pts',(-5.01657987302642,1.06150737274083,53.5817811074516));
#58999=CARTESIAN_POINT('Ctrl Pts',(-4.91183741717926,-1.47197986128708,
53.7209545648736));
#59000=CARTESIAN_POINT('Ctrl Pts',(-3.6059785727194,-3.64551643226655,53.8601280222955));
#59001=CARTESIAN_POINT('Ctrl Pts',(-1.41833159220866,-4.92759647489319,
53.9993014797174));
#59002=CARTESIAN_POINT('Ctrl Pts',(1.11614716940514,-5.00470648700459,54.1384749371395));
#59003=CARTESIAN_POINT('Ctrl Pts',(3.3776888316379,-3.85799036824427,54.2776483945613));
#59004=CARTESIAN_POINT('Ctrl Pts',(4.81326720014988,-1.76786039742912,54.4168218519834));
#59005=CARTESIAN_POINT('Ctrl Pts',(5.07183305260184,0.754573396941915,54.5559953094052));
#59006=CARTESIAN_POINT('Ctrl Pts',(4.09015797637785,3.09248755100316,54.6951687668272));
#59007=CARTESIAN_POINT('Ctrl Pts',(2.10829593137106,4.6741801196147,54.8343422242492));
#59008=CARTESIAN_POINT('Ctrl Pts',(-0.389118356134408,5.11287183779883,
54.9735156816711));
#59009=CARTESIAN_POINT('Ctrl Pts',(-2.79137956853432,4.30128720608217,55.1126891390931));
#59010=CARTESIAN_POINT('Ctrl Pts',(-4.51105064981971,2.4378871096911,55.2518625965151));
#59011=CARTESIAN_POINT('Ctrl Pts',(-5.12761175307327,-0.0216618231406892,
55.391036053937));
#59012=CARTESIAN_POINT('Ctrl Pts',(-4.4902920805669,-2.47591368105495,55.530209511359));
#59013=CARTESIAN_POINT('Ctrl Pts',(-2.75493862771526,-4.32471787315188,
55.6693829687808));
#59014=CARTESIAN_POINT('Ctrl Pts',(-0.345906130887604,-5.11597698132539,
55.808556426203));
#59015=CARTESIAN_POINT('Ctrl Pts',(2.14771253755835,-4.65620042318322,55.9477298836247));
#59016=CARTESIAN_POINT('Ctrl Pts',(4.11614022189969,-3.05781968050709,56.0869033410469));
#59017=CARTESIAN_POINT('Ctrl Pts',(5.07802736785512,-0.711694861686717,
56.2260767984686));
#59018=CARTESIAN_POINT('Ctrl Pts',(4.79815885796941,1.80846429285365,56.3652502558907));
#59019=CARTESIAN_POINT('Ctrl Pts',(3.34497235117331,3.88639054840388,56.5044237133125));
#59020=CARTESIAN_POINT('Ctrl Pts',(1.07382287671086,5.01395811253837,56.6435971707346));
#59021=CARTESIAN_POINT('Ctrl Pts',(-1.45991392427294,4.91543719912591,56.7827706281565));
#59022=CARTESIAN_POINT('Ctrl Pts',(-3.63665060667076,3.61491962425697,56.9219440855785));
#59023=CARTESIAN_POINT('Ctrl Pts',(-4.92409876578536,1.43042751288836,57.0611175430004));
#59024=CARTESIAN_POINT('Ctrl Pts',(-5.00743220684222,-1.10385425610278,
57.2002910004224));
#59025=CARTESIAN_POINT('Ctrl Pts',(-3.86627298300154,-3.36820497383239,
57.3394644578443));
#59026=CARTESIAN_POINT('Ctrl Pts',(-1.77967451752562,-4.80891153344568,
57.4786379152663));
#59027=CARTESIAN_POINT('Ctrl Pts',(0.742116737907104,-5.07367069015669,
57.6178113726882));
#59028=CARTESIAN_POINT('Ctrl Pts',(3.08243444271975,-4.09773955140781,57.7569848301102));
#59029=CARTESIAN_POINT('Ctrl Pts',(4.66898889937891,-2.11976748307766,57.8961582875321));
#59030=CARTESIAN_POINT('Ctrl Pts',(5.1138119408897,0.376562024175001,58.0353317449541));
#59031=CARTESIAN_POINT('Ctrl Pts',(4.30812874434728,2.78080891953505,58.1745052023761));
#59032=CARTESIAN_POINT('Ctrl Pts',(2.4489570872563,4.50505057791964,58.313678659798));
#59033=CARTESIAN_POINT('Ctrl Pts',(-0.00907040374824587,5.12764948613034,
58.45285211722));
#59034=CARTESIAN_POINT('Ctrl Pts',(-2.46487986315524,4.49635839152627,58.5920255746418));
#59035=CARTESIAN_POINT('Ctrl Pts',(-4.31793981191222,2.76555009094761,58.7311990320639));
#59036=CARTESIAN_POINT('Ctrl Pts',(-5.11511215026264,0.358467871743584,
58.8703724894858));
#59037=CARTESIAN_POINT('Ctrl Pts',(-4.66146030380106,-2.13627230495643,
59.0095459469077));
#59038=CARTESIAN_POINT('Ctrl Pts',(-3.06791804765684,-4.10861903535706,
59.1487194043298));
#59039=CARTESIAN_POINT('Ctrl Pts',(-0.724162310693165,-5.07626442106874,
59.2878928617516));
#59040=CARTESIAN_POINT('Ctrl Pts',(1.79667649020643,-4.80258525321274,59.4270663191736));
#59041=CARTESIAN_POINT('Ctrl Pts',(3.87816492297812,-3.35450567968201,59.5662397765956));
#59042=CARTESIAN_POINT('Ctrl Pts',(5.01130611802573,-1.08613190555986,59.7054132340175));
#59043=CARTESIAN_POINT('Ctrl Pts',(4.91900734112638,1.44783918401923,59.8445866914394));
#59044=CARTESIAN_POINT('Ctrl Pts',(3.6238388779325,3.62776285217508,59.9837601488615));
#59045=CARTESIAN_POINT('Ctrl Pts',(1.44251480813104,4.92057136450247,60.1229336062833));
#59046=CARTESIAN_POINT('Ctrl Pts',(-1.09155468659011,5.01012773200588,60.2621070637055));
#59047=CARTESIAN_POINT('Ctrl Pts',(-3.35870080584726,3.87453228424406,60.4012805211271));
#59048=CARTESIAN_POINT('Ctrl Pts',(-4.80452686914066,1.79147790623387,60.5404539785494));
#59049=CARTESIAN_POINT('Ctrl Pts',(-5.07547773362422,-0.729655603925534,
60.6796274359711));
#59050=CARTESIAN_POINT('Ctrl Pts',(-4.10529641718065,-3.07236274745144,
60.8188008933932));
#59051=CARTESIAN_POINT('Ctrl Pts',(-2.13122625265585,-4.663769525259,60.957974350815));
#59052=CARTESIAN_POINT('Ctrl Pts',(0.364003421574487,-5.11472120786763,
61.0971478082371));
#59053=CARTESIAN_POINT('Ctrl Pts',(2.77022150230343,-4.31494430466559,61.236321265659));
#59054=CARTESIAN_POINT('Ctrl Pts',(4.49902334075878,-2.46001229778389,61.375494723081));
#59055=CARTESIAN_POINT('Ctrl Pts',(5.12765629947872,-0.00352107013592945,
61.5146681805029));
#59056=CARTESIAN_POINT('Ctrl Pts',(4.50239758982308,2.45383118170519,61.6538416379248));
#59057=CARTESIAN_POINT('Ctrl Pts',(2.77614487750337,4.31113571438885,61.7930150953468));
#59058=CARTESIAN_POINT('Ctrl Pts',(0.371027452000867,5.11421647371715,61.9321885527688));
#59059=CARTESIAN_POINT('Ctrl Pts',(-2.12481919255064,4.6666920788757,62.0713620101907));
#59060=CARTESIAN_POINT('Ctrl Pts',(-4.10107307033674,3.0779979096349,62.2105354676127));
#59061=CARTESIAN_POINT('Ctrl Pts',(-5.07447087161606,0.736625404163389,
62.3497089250346));
#59062=CARTESIAN_POINT('Ctrl Pts',(-4.80698267522873,-1.78487787537981,
62.4888823824566));
#59063=CARTESIAN_POINT('Ctrl Pts',(-3.36401880748098,-3.86991586995366,
62.6280558398784));
#59064=CARTESIAN_POINT('Ctrl Pts',(-1.09843433267496,-5.00862398811822,
62.7672292973006));
#59065=CARTESIAN_POINT('Ctrl Pts',(1.4357556111677,-4.92254766049344,62.9064027547223));
#59066=CARTESIAN_POINT('Ctrl Pts',(3.61885342162015,-3.63273659425221,63.0455762121445));
#59067=CARTESIAN_POINT('Ctrl Pts',(4.91701390374655,-1.45459279213023,63.1847496695662));
#59068=CARTESIAN_POINT('Ctrl Pts',(5.01279380401881,1.07924733972977,63.3239231269884));
#59069=CARTESIAN_POINT('Ctrl Pts',(3.88276674436703,3.34917871604949,63.4630965844101));
#59070=CARTESIAN_POINT('Ctrl Pts',(1.80327337436161,4.80010868768094,63.6022700418323));
#59071=CARTESIAN_POINT('Ctrl Pts',(-0.717195690581678,5.07726303778206,
63.741443499254));
#59072=CARTESIAN_POINT('Ctrl Pts',(-3.06226156438238,4.1128112366359,63.8806169566761));
#59073=CARTESIAN_POINT('Ctrl Pts',(-4.65854341282239,2.14270591183768,64.019790414098));
#59074=CARTESIAN_POINT('Ctrl Pts',(-5.11555785592785,-0.351508627023642,
64.15896387152));
#59075=CARTESIAN_POINT('Ctrl Pts',(-4.3218160990318,-2.75948654582595,64.2981373289419));
#59076=CARTESIAN_POINT('Ctrl Pts',(-2.47088410596534,-4.49324627465512,
64.437310786364));
#59077=CARTESIAN_POINT('Ctrl Pts',(-0.834646007515407,-4.91565157897533,
64.5300930913119));
#59078=CARTESIAN_POINT('Ctrl Pts',(-0.0154545066754591,-4.91822571876519,
64.5764842437858));
#59079=CARTESIAN_POINT('Ctrl Pts',(2.58415070483638,5.32291852118006,2.35922392732846E-16));
#59080=CARTESIAN_POINT('Ctrl Pts',(2.70511861947279,5.25165405591466,2.59308817902277E-16));
#59081=CARTESIAN_POINT('Ctrl Pts',(2.82328939759037,5.1761837259702,2.60954157596921E-16));
#59082=CARTESIAN_POINT('Ctrl Pts',(2.93842118606223,5.09659358068734,2.98372437868011E-16));
#59083=CARTESIAN_POINT('Ctrl Pts',(3.07402653614829,5.00285014407668,2.98974997602692E-16));
#59084=CARTESIAN_POINT('Ctrl Pts',(3.20541718868923,4.90339199696324,5.80189110088706E-16));
#59085=CARTESIAN_POINT('Ctrl Pts',(3.33231171324647,4.79857206961274,4.71844785465692E-16));
#59086=CARTESIAN_POINT('Ctrl Pts',(3.45942568888835,4.69357086693276,3.63313090429043E-16));
#59087=CARTESIAN_POINT('Ctrl Pts',(3.58202843978269,4.58318869192379,3.87064081949451E-16));
#59088=CARTESIAN_POINT('Ctrl Pts',(3.69979700370316,4.46774699683153,4.44089209850063E-16));
#59089=CARTESIAN_POINT('Ctrl Pts',(3.81278208592582,4.35699427150552,4.98798111360991E-16));
#59090=CARTESIAN_POINT('Ctrl Pts',(3.92131782119956,4.24158400211618,-1.6541059630567E-16));
#59091=CARTESIAN_POINT('Ctrl Pts',(4.02507848003065,4.12177931674072,-3.33066907387547E-16));
#59092=CARTESIAN_POINT('Ctrl Pts',(4.10629751893176,4.02800175680941,-4.64300504062582E-16));
#59093=CARTESIAN_POINT('Ctrl Pts',(4.18459012464176,3.93153124615902,4.15462027952972E-16));
#59094=CARTESIAN_POINT('Ctrl Pts',(4.25978084755203,3.83248837704811,5.27355936696949E-16));
#59095=CARTESIAN_POINT('Ctrl Pts',(4.27272403323478,3.81543932902945,5.46617137834363E-16));
#59096=CARTESIAN_POINT('Ctrl Pts',(4.28556975141914,3.79832128448063,-6.44283739800603E-17));
#59097=CARTESIAN_POINT('Ctrl Pts',(4.29831497568012,3.78113823514667,-5.55111512312578E-17));
#59098=CARTESIAN_POINT('Ctrl Pts',(4.39680707821293,3.64835166174689,1.33990538227478E-17));
#59099=CARTESIAN_POINT('Ctrl Pts',(4.48934874550704,3.51162388599325,2.0715226758615E-16));
#59100=CARTESIAN_POINT('Ctrl Pts',(4.57564112442567,3.37129841337389,1.94289029309402E-16));
#59101=CARTESIAN_POINT('Ctrl Pts',(4.66193350334431,3.23097294075453,1.81425791032655E-16));
#59102=CARTESIAN_POINT('Ctrl Pts',(4.74197706027285,3.08704906877042,-2.38966041326046E-16));
#59103=CARTESIAN_POINT('Ctrl Pts',(4.81542054559223,2.93984529382198,-2.77555756156289E-16));
#59104=CARTESIAN_POINT('Ctrl Pts',(4.88716990501125,2.79603707842097,-3.42113286361595E-16));
#59105=CARTESIAN_POINT('Ctrl Pts',(4.95261996588971,2.64909759657784,-3.28762512571199E-17));
#59106=CARTESIAN_POINT('Ctrl Pts',(5.01163872074466,2.49946141477762,2.22044604925031E-16));
#59107=CARTESIAN_POINT('Ctrl Pts',(5.07015933458441,2.35108821996683,4.74813830927776E-16));
#59108=CARTESIAN_POINT('Ctrl Pts',(5.12235677838181,2.200062894578,5.77849218589554E-17));
#59109=CARTESIAN_POINT('Ctrl Pts',(5.16805141111303,2.0468094574673,1.38777878078145E-16));
#59110=CARTESIAN_POINT('Ctrl Pts',(5.18023517309137,2.0059468158721,1.60373388130753E-16));
#59111=CARTESIAN_POINT('Ctrl Pts',(5.19195634089117,1.96492580600586,-4.18469453909966E-16));
#59112=CARTESIAN_POINT('Ctrl Pts',(5.20321088585858,1.92375457558523,-4.16333634234434E-16));
#59113=CARTESIAN_POINT('Ctrl Pts',(5.20842035550966,1.90469736127804,-4.15345012498763E-16));
#59114=CARTESIAN_POINT('Ctrl Pts',(5.21353051364629,1.88560539766239,4.06076581793497E-17));
#59115=CARTESIAN_POINT('Ctrl Pts',(5.21853870347985,1.86648807919458,2.77555756156289E-17));
#59116=CARTESIAN_POINT('Ctrl Pts',(5.25844125851643,1.71417159805777,-7.46428854803789E-17));
#59117=CARTESIAN_POINT('Ctrl Pts',(5.29180961247242,1.56050412240968,-2.4180069860195E-16));
#59118=CARTESIAN_POINT('Ctrl Pts',(5.31857341141684,1.40590440312336,-1.66533453693773E-16));
#59119=CARTESIAN_POINT('Ctrl Pts',(5.34526406646942,1.25172719579692,-9.14719097487536E-17));
#59120=CARTESIAN_POINT('Ctrl Pts',(5.36538625816212,1.09662206745273,-1.14443556055179E-15));
#59121=CARTESIAN_POINT('Ctrl Pts',(5.37881871749598,0.941000624308486,-9.43689570931383E-16));
#59122=CARTESIAN_POINT('Ctrl Pts',(5.39204517961296,0.787765757097624,-7.46022177279958E-16));
#59123=CARTESIAN_POINT('Ctrl Pts',(5.39878545820546,0.634029605395147,-2.06261628158008E-17));
#59124=CARTESIAN_POINT('Ctrl Pts',(5.3988741101366,0.480192238475125,0.));
#59125=CARTESIAN_POINT('Ctrl Pts',(5.398916119146,0.407294160455884,9.7740078128452E-18));
#59126=CARTESIAN_POINT('Ctrl Pts',(5.39746379985764,0.334373522025099,-1.09637651355696E-15));
#59127=CARTESIAN_POINT('Ctrl Pts',(5.39449561700532,0.26147412547058,-1.11022302462516E-15));
#59128=CARTESIAN_POINT('Ctrl Pts',(5.39000601196769,0.151208176808848,-1.12870294857941E-15));
#59129=CARTESIAN_POINT('Ctrl Pts',(5.3820487164881,0.0409904590914841,-5.4025619378067E-16));
#59130=CARTESIAN_POINT('Ctrl Pts',(5.37064145959088,-0.0690162522279109,
-4.9960036108132E-16));
#59131=CARTESIAN_POINT('Ctrl Pts',(5.36710034259144,-0.103165271489568,
-4.86979705511336E-16));
#59132=CARTESIAN_POINT('Ctrl Pts',(5.3632266913415,-0.137293906145545,-8.57200446937436E-16));
#59133=CARTESIAN_POINT('Ctrl Pts',(5.35902082468953,-0.171397139460776,
-8.88178419700125E-16));
#59134=CARTESIAN_POINT('Ctrl Pts',(5.35662614050457,-0.190814415431093,
-9.05816273582604E-16));
#59135=CARTESIAN_POINT('Ctrl Pts',(5.35412341958406,-0.210225943349712,
-1.22843111941016E-15));
#59136=CARTESIAN_POINT('Ctrl Pts',(5.35151382049558,-0.22962257030035,-1.22124532708767E-15));
#59137=CARTESIAN_POINT('Ctrl Pts',(5.33114339416283,-0.381031866136956,
-1.16515331901094E-15));
#59138=CARTESIAN_POINT('Ctrl Pts',(5.30430552073536,-0.531245332604996,
-4.64315052832525E-17));
#59139=CARTESIAN_POINT('Ctrl Pts',(5.27115359261857,-0.679863637652015,
-1.11022302462516E-16));
#59140=CARTESIAN_POINT('Ctrl Pts',(5.23793248804223,-0.828792057034796,
-1.75747878006781E-16));
#59141=CARTESIAN_POINT('Ctrl Pts',(5.19837064736214,-0.976119385505511,
-6.58930197271103E-16));
#59142=CARTESIAN_POINT('Ctrl Pts',(5.15257331214529,-1.12142719841327,-8.32667268468867E-16));
#59143=CARTESIAN_POINT('Ctrl Pts',(5.10717447600833,-1.26547063579635,-1.00489259094399E-15));
#59144=CARTESIAN_POINT('Ctrl Pts',(5.0556478273115,-1.40753020406774,-5.63971542161181E-16));
#59145=CARTESIAN_POINT('Ctrl Pts',(4.99805275028795,-1.54717172655174,-4.44089209850063E-16));
#59146=CARTESIAN_POINT('Ctrl Pts',(4.9480429007657,-1.6684225675503,-3.39995288822692E-16));
#59147=CARTESIAN_POINT('Ctrl Pts',(4.89345700852936,-1.78785018655589,-1.19778754206742E-15));
#59148=CARTESIAN_POINT('Ctrl Pts',(4.8343102366916,-1.90514816028807,-1.22124532708767E-15));
#59149=CARTESIAN_POINT('Ctrl Pts',(4.80473685077273,-1.96379714715416,-1.2329742195978E-15));
#59150=CARTESIAN_POINT('Ctrl Pts',(4.77402291520497,-2.02191336562227,-1.62336207194318E-16));
#59151=CARTESIAN_POINT('Ctrl Pts',(4.74216843424644,-2.0794561600232,-1.11022302462516E-16));
#59152=CARTESIAN_POINT('Ctrl Pts',(4.73104879031827,-2.09954298501978,-9.31098351419854E-17));
#59153=CARTESIAN_POINT('Ctrl Pts',(4.71979015531546,-2.11955992072199,-5.50505449287299E-16));
#59154=CARTESIAN_POINT('Ctrl Pts',(4.70839249529098,-2.13950518784205,-5.55111512312578E-16));
#59155=CARTESIAN_POINT('Ctrl Pts',(4.69713562314994,-2.15920408404594,-5.59660679636204E-16));
#59156=CARTESIAN_POINT('Ctrl Pts',(4.68574729156115,-2.17882575777773,-4.49902034763585E-16));
#59157=CARTESIAN_POINT('Ctrl Pts',(4.67423042538155,-2.19836423113908,-4.44089209850063E-16));
#59158=CARTESIAN_POINT('Ctrl Pts',(4.66400316177994,-2.21571488142219,-4.38927276757024E-16));
#59159=CARTESIAN_POINT('Ctrl Pts',(4.65367388210654,-2.23300106829952,-2.36408244836096E-16));
#59160=CARTESIAN_POINT('Ctrl Pts',(4.64324279625684,-2.25022178954521,-2.22044604925031E-16));
#59161=CARTESIAN_POINT('Ctrl Pts',(4.56566903431785,-2.37828862262268,-1.28577692735215E-16));
#59162=CARTESIAN_POINT('Ctrl Pts',(4.48246793624052,-2.50273777206833,-8.64751003178453E-16));
#59163=CARTESIAN_POINT('Ctrl Pts',(4.39395501715838,-2.62326605186807,-6.66133814775094E-16));
#59164=CARTESIAN_POINT('Ctrl Pts',(4.30552250169377,-2.74368484584573,-4.67697046819005E-16));
#59165=CARTESIAN_POINT('Ctrl Pts',(4.21178716587762,-2.86019038329772,-1.03847678039002E-15));
#59166=CARTESIAN_POINT('Ctrl Pts',(4.11303118505379,-2.97243998135549,-7.21644966006352E-16));
#59167=CARTESIAN_POINT('Ctrl Pts',(4.06811417427852,-3.02349427055824,-5.77540903630545E-16));
#59168=CARTESIAN_POINT('Ctrl Pts',(4.02215816382635,-3.07366754203135,-5.16430948201177E-16));
#59169=CARTESIAN_POINT('Ctrl Pts',(3.97518802543061,-3.12292436790974,-5.55111512312578E-16));
#59170=CARTESIAN_POINT('Ctrl Pts',(3.9540953692043,-3.14504389598732,-5.72481608916671E-16));
#59171=CARTESIAN_POINT('Ctrl Pts',(3.93279819227414,-3.16697858573548,-5.89160445509899E-16));
#59172=CARTESIAN_POINT('Ctrl Pts',(3.91129869242318,-3.18872508690685,-6.66133814775094E-16));
#59173=CARTESIAN_POINT('Ctrl Pts',(3.89425753665478,-3.20596202341459,-7.27145242239012E-16));
#59174=CARTESIAN_POINT('Ctrl Pts',(3.87708874107993,-3.22308115070843,-4.69465644281958E-16));
#59175=CARTESIAN_POINT('Ctrl Pts',(3.85980494844311,-3.24006967703212,-4.44089209850063E-16));
#59176=CARTESIAN_POINT('Ctrl Pts',(3.75513441850311,-3.34295207620028,-2.9040969657491E-16));
#59177=CARTESIAN_POINT('Ctrl Pts',(3.64615041630408,-3.44114871706017,-1.04632860102231E-16));
#59178=CARTESIAN_POINT('Ctrl Pts',(3.53313742783404,-3.53434970143845,0.));
#59179=CARTESIAN_POINT('Ctrl Pts',(3.4219903426573,-3.62601188902845,1.02905317092383E-16));
#59180=CARTESIAN_POINT('Ctrl Pts',(3.30694556827097,-3.71284232949852,-5.47072034414736E-16));
#59181=CARTESIAN_POINT('Ctrl Pts',(3.18825216084998,-3.79450149497552,-5.55111512312578E-16));
#59182=CARTESIAN_POINT('Ctrl Pts',(3.08078920485239,-3.86843428953528,-5.62390316404158E-16));
#59183=CARTESIAN_POINT('Ctrl Pts',(2.97033484176792,-3.93812777284464,5.67746719143187E-17));
#59184=CARTESIAN_POINT('Ctrl Pts',(2.85706463458441,-4.0032942355399,0.));
#59185=CARTESIAN_POINT('Ctrl Pts',(-5.9170192319132,-0.000147776431128344,
63.5633751922049));
#59186=CARTESIAN_POINT('Ctrl Pts',(-5.91623110189089,0.84993950459726,63.5233521849073));
#59187=CARTESIAN_POINT('Ctrl Pts',(-5.73107037269015,1.70039301271516,63.4833291776097));
#59188=CARTESIAN_POINT('Ctrl Pts',(-5.37589115391287,2.47263111983861,63.4433061703122));
#59189=CARTESIAN_POINT('Ctrl Pts',(-4.96419861988145,3.36774166231843,63.3969150178382));
#59190=CARTESIAN_POINT('Ctrl Pts',(-4.32407929378261,4.15776661567246,63.3505238653642));
#59191=CARTESIAN_POINT('Ctrl Pts',(-3.53382635369325,4.74615479151186,63.3041327128903));
#59192=CARTESIAN_POINT('Ctrl Pts',(-2.7435734136039,5.33454296735125,63.2577415604163));
#59193=CARTESIAN_POINT('Ctrl Pts',(-1.80318685952402,5.72129436567601,63.2113504079422));
#59194=CARTESIAN_POINT('Ctrl Pts',(-0.827631399458168,5.85909972305151,
63.1649592554683));
#59195=CARTESIAN_POINT('Ctrl Pts',(0.147924060607687,5.996905080427,63.1185681029943));
#59196=CARTESIAN_POINT('Ctrl Pts',(1.15864842665952,5.88576439685324,63.0721769505203));
#59197=CARTESIAN_POINT('Ctrl Pts',(2.08095574250639,5.53927791248008,63.0257857980463));
#59198=CARTESIAN_POINT('Ctrl Pts',(3.00326305835326,5.19279142810691,62.9793946455724));
#59199=CARTESIAN_POINT('Ctrl Pts',(3.83715332399518,4.61095914293436,62.9330034930984));
#59200=CARTESIAN_POINT('Ctrl Pts',(4.48067252974842,3.86491443257027,62.8866123406244));
#59201=CARTESIAN_POINT('Ctrl Pts',(5.1241917355017,3.11886972220613,62.8402211881504));
#59202=CARTESIAN_POINT('Ctrl Pts',(5.57733988136629,2.20861258665045,62.7938300356764));
#59203=CARTESIAN_POINT('Ctrl Pts',(5.78470977513812,1.24544089377108,62.7474388832024));
#59204=CARTESIAN_POINT('Ctrl Pts',(5.99207966890992,0.282269200891815,62.7010477307284));
#59205=CARTESIAN_POINT('Ctrl Pts',(5.95367131058902,-0.73381704931112,62.6546565782545));
#59206=CARTESIAN_POINT('Ctrl Pts',(5.67418176459349,-1.6785850372942,62.6082654257805));
#59207=CARTESIAN_POINT('Ctrl Pts',(5.39469221859793,-2.62335302527734,62.5618742733065));
#59208=CARTESIAN_POINT('Ctrl Pts',(4.87412148492771,-3.49680275104061,62.5154831208325));
#59209=CARTESIAN_POINT('Ctrl Pts',(4.17611796055031,-4.1921388959224,62.4690919683585));
#59210=CARTESIAN_POINT('Ctrl Pts',(3.47811443617291,-4.88747504080418,62.4227008158845));
#59211=CARTESIAN_POINT('Ctrl Pts',(2.60267812108833,-5.40469760480448,62.3763096634105));
#59212=CARTESIAN_POINT('Ctrl Pts',(1.65684670001291,-5.68056746832837,62.3299185109365));
#59213=CARTESIAN_POINT('Ctrl Pts',(0.711015278937486,-5.95643733185225,
62.2835273584626));
#59214=CARTESIAN_POINT('Ctrl Pts',(-0.305211248128781,-5.99095449489973,
62.2371362059886));
#59215=CARTESIAN_POINT('Ctrl Pts',(-1.26758151165544,-5.77989842323892,
62.1907450535146));
#59216=CARTESIAN_POINT('Ctrl Pts',(-2.2299517751821,-5.56884235157811,62.1443539010407));
#59217=CARTESIAN_POINT('Ctrl Pts',(-3.13846577516915,-5.112213045209,62.0979627485666));
#59218=CARTESIAN_POINT('Ctrl Pts',(-3.88204168820752,-4.46584154408076,
62.0515715960926));
#59219=CARTESIAN_POINT('Ctrl Pts',(-4.62561760124594,-3.81947004295248,
62.0051804436187));
#59220=CARTESIAN_POINT('Ctrl Pts',(-5.20425542733567,-2.98335634706504,
61.9587892911447));
#59221=CARTESIAN_POINT('Ctrl Pts',(-5.54720658714768,-2.05972995272988,
61.9123981386707));
#59222=CARTESIAN_POINT('Ctrl Pts',(-5.79121887920067,-1.40256292753042,
61.8793904898488));
#59223=CARTESIAN_POINT('Ctrl Pts',(-5.91591649412851,-0.701093229105765,
61.8463828410268));
#59224=CARTESIAN_POINT('Ctrl Pts',(-5.91657547456529,0.000148352692112552,
61.8133751922048));
#59225=CARTESIAN_POINT('Origin',(0.,0.,0.));
#59226=CARTESIAN_POINT('Origin',(0.,0.,79.));
#59227=CARTESIAN_POINT('',(-10.,-1.22464679914735E-15,79.));
#59228=CARTESIAN_POINT('Origin',(0.,0.,79.));
#59229=CARTESIAN_POINT('Origin',(0.,0.,79.));
#59230=CARTESIAN_POINT('',(-10.,-1.22464679914735E-15,91.));
#59231=CARTESIAN_POINT('Origin',(0.,0.,91.));
#59232=CARTESIAN_POINT('',(-10.,-1.22464679914735E-15,79.));
#59233=CARTESIAN_POINT('Origin',(0.,0.,91.));
#59234=CARTESIAN_POINT('Origin',(0.,0.,0.));
#69471=UNCERTAINTY_MEASURE_WITH_UNIT(LENGTH_MEASURE(0.01),#69492,
'DISTANCE_ACCURACY_VALUE',
'Maximum model space distance between geometric entities at asserted c
onnectivities');
#69478=UNCERTAINTY_MEASURE_WITH_UNIT(LENGTH_MEASURE(0.01),#69492,
'DISTANCE_ACCURACY_VALUE',
'Maximum model space distance between geometric entities at asserted c
onnectivities');
#69484=(
GEOMETRIC_REPRESENTATION_CONTEXT(3)
GLOBAL_UNCERTAINTY_ASSIGNED_CONTEXT((#69471))
GLOBAL_UNIT_ASSIGNED_CONTEXT((#69492,#69494,#69495))
REPRESENTATION_CONTEXT('','3D')
);
#69491=(
GEOMETRIC_REPRESENTATION_CONTEXT(3)
GLOBAL_UNCERTAINTY_ASSIGNED_CONTEXT((#69478))
GLOBAL_UNIT_ASSIGNED_CONTEXT((#69492,#69494,#69495))
REPRESENTATION_CONTEXT('','3D')
);
#69492=(
LENGTH_UNIT()
NAMED_UNIT(*)
SI_UNIT(.MILLI.,.METRE.)
);
#69494=(
NAMED_UNIT(*)
PLANE_ANGLE_UNIT()
SI_UNIT($,.RADIAN.)
);
#69495=(
NAMED_UNIT(*)
SI_UNIT($,.STERADIAN.)
SOLID_ANGLE_UNIT()
);
#69501=SHAPE_DEFINITION_REPRESENTATION(#69513,#69575);
#69513=PRODUCT_DEFINITION_SHAPE('',$,#69588);
#69575=SHAPE_REPRESENTATION('',(#15482),#69484);
#69582=PRODUCT_DEFINITION_CONTEXT('part definition',#69620,'design');
#69588=PRODUCT_DEFINITION('Jaw adjustment screw','Jaw adjustment screw',
#69600,#69582);
#69600=PRODUCT_DEFINITION_FORMATION('',$,#69627);
#69620=APPLICATION_CONTEXT(
'Core Data for Automotive Mechanical Design Process');
#69621=PRODUCT_CONTEXT('part definition',#69620,'mechanical');
#69627=PRODUCT('Jaw adjustment screw','Jaw adjustment screw',$,(#69621));
#69639=PRESENTATION_STYLE_ASSIGNMENT((#69649));
#69649=SURFACE_STYLE_USAGE(.BOTH.,#69659);
#69659=SURFACE_SIDE_STYLE('',(#69669));
#69669=SURFACE_STYLE_FILL_AREA(#69679);
#69679=FILL_AREA_STYLE('Screw gray',(#69689));
#69689=FILL_AREA_STYLE_COLOUR('Screw gray',#69699);
#69699=COLOUR_RGB('Screw gray',0.576470588235294,0.615686274509804,0.666666666666667);
ENDSEC;
END-ISO-10303-21;
